ISO-10303-21;
HEADER;
/* Generated by software containing ST-Developer
 * from STEP Tools, Inc. (www.steptools.com) 
 */

FILE_DESCRIPTION(
/* description */ (''),
/* implementation_level */ '2;1');

FILE_NAME(
/* name */ 'Assembly Screw 1.step',
/* time_stamp */ '2026-10-28T16:47:13+01:00',
/* author */ (''),
/* organization */ (''),
/* preprocessor_version */ 'ST-DEVELOPER v20.2',
/* originating_system */ 'Autodesk Translation Framework v15.17.0.0',
/* authorisation */ '');

FILE_SCHEMA (('AUTOMOTIVE_DESIGN { 1 0 10303 214 3 1 1 }'));
ENDSEC;

DATA;
#10=MECHANICAL_DESIGN_GEOMETRIC_PRESENTATION_REPRESENTATION('',(#4605),#459242);
#155=SPHERICAL_SURFACE('',#99285,3.10691712599126);
#2315=(
BOUNDED_SURFACE()
B_SPLINE_SURFACE(1,2,((#368140,#368141,#368142,#368143,#368144,#368145,
#368146,#368147,#368148,#368149,#368150,#368151,#368152,#368153,#368154,
#368155,#368156,#368157,#368158,#368159,#368160,#368161,#368162,#368163,
#368164,#368165,#368166,#368167,#368168,#368169,#368170,#368171,#368172,
#368173,#368174,#368175,#368176,#368177,#368178,#368179,#368180,#368181,
#368182,#368183,#368184,#368185,#368186,#368187,#368188,#368189,#368190,
#368191,#368192,#368193,#368194,#368195,#368196,#368197,#368198,#368199,
#368200,#368201,#368202,#368203,#368204,#368205,#368206,#368207,#368208,
#368209,#368210,#368211,#368212,#368213,#368214,#368215,#368216,#368217,
#368218,#368219,#368220,#368221,#368222,#368223,#368224,#368225,#368226,
#368227,#368228,#368229,#368230,#368231,#368232,#368233,#368234,#368235,
#368236,#368237,#368238,#368239,#368240,#368241,#368242,#368243,#368244,
#368245,#368246,#368247,#368248,#368249,#368250,#368251,#368252,#368253,
#368254,#368255,#368256,#368257,#368258,#368259,#368260,#368261,#368262,
#368263,#368264,#368265,#368266,#368267,#368268,#368269,#368270,#368271,
#368272,#368273,#368274,#368275,#368276,#368277,#368278,#368279,#368280,
#368281,#368282,#368283,#368284,#368285,#368286,#368287,#368288,#368289,
#368290,#368291,#368292,#368293,#368294,#368295,#368296,#368297,#368298,
#368299,#368300,#368301,#368302,#368303,#368304,#368305,#368306,#368307,
#368308,#368309,#368310,#368311,#368312,#368313,#368314,#368315,#368316,
#368317,#368318,#368319,#368320,#368321,#368322,#368323,#368324,#368325,
#368326,#368327,#368328,#368329,#368330,#368331,#368332,#368333,#368334,
#368335,#368336,#368337,#368338,#368339,#368340,#368341,#368342,#368343,
#368344),(#368345,#368346,#368347,#368348,#368349,#368350,#368351,#368352,
#368353,#368354,#368355,#368356,#368357,#368358,#368359,#368360,#368361,
#368362,#368363,#368364,#368365,#368366,#368367,#368368,#368369,#368370,
#368371,#368372,#368373,#368374,#368375,#368376,#368377,#368378,#368379,
#368380,#368381,#368382,#368383,#368384,#368385,#368386,#368387,#368388,
#368389,#368390,#368391,#368392,#368393,#368394,#368395,#368396,#368397,
#368398,#368399,#368400,#368401,#368402,#368403,#368404,#368405,#368406,
#368407,#368408,#368409,#368410,#368411,#368412,#368413,#368414,#368415,
#368416,#368417,#368418,#368419,#368420,#368421,#368422,#368423,#368424,
#368425,#368426,#368427,#368428,#368429,#368430,#368431,#368432,#368433,
#368434,#368435,#368436,#368437,#368438,#368439,#368440,#368441,#368442,
#368443,#368444,#368445,#368446,#368447,#368448,#368449,#368450,#368451,
#368452,#368453,#368454,#368455,#368456,#368457,#368458,#368459,#368460,
#368461,#368462,#368463,#368464,#368465,#368466,#368467,#368468,#368469,
#368470,#368471,#368472,#368473,#368474,#368475,#368476,#368477,#368478,
#368479,#368480,#368481,#368482,#368483,#368484,#368485,#368486,#368487,
#368488,#368489,#368490,#368491,#368492,#368493,#368494,#368495,#368496,
#368497,#368498,#368499,#368500,#368501,#368502,#368503,#368504,#368505,
#368506,#368507,#368508,#368509,#368510,#368511,#368512,#368513,#368514,
#368515,#368516,#368517,#368518,#368519,#368520,#368521,#368522,#368523,
#368524,#368525,#368526,#368527,#368528,#368529,#368530,#368531,#368532,
#368533,#368534,#368535,#368536,#368537,#368538,#368539,#368540,#368541,
#368542,#368543,#368544,#368545,#368546,#368547,#368548,#368549)),
 .UNSPECIFIED.,.F.,.F.,.F.)
B_SPLINE_SURFACE_WITH_KNOTS((2,2),(3,2,2,2,2,2,2,2,2,2,2,2,2,2,2,2,2,2,
2,2,2,2,2,2,2,2,2,2,2,2,2,2,2,2,2,2,2,2,2,2,2,2,2,2,2,2,2,2,2,2,2,2,2,2,
2,2,2,2,2,2,2,2,2,2,2,2,2,2,2,2,2,2,2,2,2,2,2,2,2,2,2,2,2,2,2,2,2,2,2,2,
2,2,2,2,2,2,2,2,2,2,2,2,3),(0.,1.),(0.,0.00980392156862745,0.0196078431372549,
0.0294117647058824,0.0392156862745098,0.0490196078431373,0.0588235294117647,
0.0686274509803922,0.0784313725490196,0.0882352941176471,0.0980392156862745,
0.107843137254902,0.117647058823529,0.127450980392157,0.137254901960784,
0.147058823529412,0.156862745098039,0.166666666666667,0.176470588235294,
0.186274509803922,0.196078431372549,0.205882352941176,0.215686274509804,
0.225490196078431,0.235294117647059,0.245098039215686,0.254901960784314,
0.264705882352941,0.274509803921569,0.284313725490196,0.294117647058824,
0.303921568627451,0.313725490196078,0.323529411764706,0.333333333333333,
0.343137254901961,0.352941176470588,0.362745098039216,0.372549019607843,
0.382352941176471,0.392156862745098,0.401960784313726,0.411764705882353,
0.42156862745098,0.431372549019608,0.441176470588235,0.450980392156863,
0.46078431372549,0.470588235294118,0.480392156862745,0.490196078431373,
0.5,0.509803921568627,0.519607843137255,0.529411764705882,0.53921568627451,
0.549019607843137,0.558823529411765,0.568627450980392,0.57843137254902,
0.588235294117647,0.598039215686274,0.607843137254902,0.617647058823529,
0.627450980392157,0.637254901960784,0.647058823529412,0.656862745098039,
0.666666666666667,0.676470588235294,0.686274509803922,0.696078431372549,
0.705882352941177,0.715686274509804,0.725490196078431,0.735294117647059,
0.745098039215686,0.754901960784314,0.764705882352941,0.774509803921569,
0.784313725490196,0.794117647058823,0.803921568627451,0.813725490196078,
0.823529411764706,0.833333333333333,0.843137254901961,0.852941176470588,
0.862745098039216,0.872549019607843,0.882352941176471,0.892156862745098,
0.901960784313726,0.911764705882353,0.92156862745098,0.931372549019608,
0.941176470588235,0.950980392156863,0.96078431372549,0.970588235294118,
0.980392156862745,0.990196078431373,1.),.UNSPECIFIED.)
GEOMETRIC_REPRESENTATION_ITEM()
RATIONAL_B_SPLINE_SURFACE(((1.,0.866025403784439,1.,0.866025403784439,1.,
0.866025403784439,1.,0.866025403784439,1.,0.866025403784439,1.,0.866025403784439,
1.,0.866025403784439,1.,0.866025403784439,1.,0.866025403784439,1.,0.866025403784439,
1.,0.866025403784439,1.,0.866025403784439,1.,0.866025403784439,1.,0.866025403784439,
1.,0.866025403784439,1.,0.866025403784439,1.,0.866025403784439,1.,0.866025403784439,
1.,0.866025403784439,1.,0.866025403784439,1.,0.866025403784439,1.,0.866025403784439,
1.,0.866025403784439,1.,0.866025403784439,1.,0.866025403784439,1.,0.866025403784439,
1.,0.866025403784439,1.,0.866025403784439,1.,0.866025403784439,1.,0.866025403784439,
1.,0.866025403784439,1.,0.866025403784439,1.,0.866025403784439,1.,0.866025403784439,
1.,0.866025403784439,1.,0.866025403784439,1.,0.866025403784439,1.,0.866025403784439,
1.,0.866025403784439,1.,0.866025403784439,1.,0.866025403784439,1.,0.866025403784439,
1.,0.866025403784439,1.,0.866025403784439,1.,0.866025403784439,1.,0.866025403784439,
1.,0.866025403784439,1.,0.866025403784439,1.,0.866025403784439,1.,0.866025403784439,
1.,0.866025403784439,1.,0.866025403784439,1.,0.866025403784439,1.,0.866025403784439,
1.,0.866025403784439,1.,0.866025403784439,1.,0.866025403784439,1.,0.866025403784439,
1.,0.866025403784439,1.,0.866025403784439,1.,0.866025403784439,1.,0.866025403784439,
1.,0.866025403784439,1.,0.866025403784439,1.,0.866025403784439,1.,0.866025403784439,
1.,0.866025403784439,1.,0.866025403784439,1.,0.866025403784439,1.,0.866025403784439,
1.,0.866025403784439,1.,0.866025403784439,1.,0.866025403784439,1.,0.866025403784439,
1.,0.866025403784439,1.,0.866025403784439,1.,0.866025403784439,1.,0.866025403784439,
1.,0.866025403784439,1.,0.866025403784439,1.,0.866025403784439,1.,0.866025403784439,
1.,0.866025403784439,1.,0.866025403784439,1.,0.866025403784439,1.,0.866025403784439,
1.,0.866025403784439,1.,0.866025403784439,1.,0.866025403784439,1.,0.866025403784439,
1.,0.866025403784439,1.,0.866025403784439,1.,0.866025403784439,1.,0.866025403784439,
1.,0.866025403784439,1.,0.866025403784439,1.,0.866025403784439,1.,0.866025403784439,
1.,0.866025403784439,1.,0.866025403784439,1.,0.866025403784439,1.,0.866025403784439,
1.),(1.,0.866025403784439,1.,0.866025403784439,1.,0.866025403784439,1.,
0.866025403784439,1.,0.866025403784439,1.,0.866025403784439,1.,0.866025403784439,
1.,0.866025403784439,1.,0.866025403784439,1.,0.866025403784439,1.,0.866025403784439,
1.,0.866025403784439,1.,0.866025403784439,1.,0.866025403784439,1.,0.866025403784439,
1.,0.866025403784439,1.,0.866025403784439,1.,0.866025403784439,1.,0.866025403784439,
1.,0.866025403784439,1.,0.866025403784439,1.,0.866025403784439,1.,0.866025403784439,
1.,0.866025403784439,1.,0.866025403784439,1.,0.866025403784439,1.,0.866025403784439,
1.,0.866025403784439,1.,0.866025403784439,1.,0.866025403784439,1.,0.866025403784439,
1.,0.866025403784439,1.,0.866025403784439,1.,0.866025403784439,1.,0.866025403784439,
1.,0.866025403784439,1.,0.866025403784439,1.,0.866025403784439,1.,0.866025403784439,
1.,0.866025403784439,1.,0.866025403784439,1.,0.866025403784439,1.,0.866025403784439,
1.,0.866025403784439,1.,0.866025403784439,1.,0.866025403784439,1.,0.866025403784439,
1.,0.866025403784439,1.,0.866025403784439,1.,0.866025403784439,1.,0.866025403784439,
1.,0.866025403784439,1.,0.866025403784439,1.,0.866025403784439,1.,0.866025403784439,
1.,0.866025403784439,1.,0.866025403784439,1.,0.866025403784439,1.,0.866025403784439,
1.,0.866025403784439,1.,0.866025403784439,1.,0.866025403784439,1.,0.866025403784439,
1.,0.866025403784439,1.,0.866025403784439,1.,0.866025403784439,1.,0.866025403784439,
1.,0.866025403784439,1.,0.866025403784439,1.,0.866025403784439,1.,0.866025403784439,
1.,0.866025403784439,1.,0.866025403784439,1.,0.866025403784439,1.,0.866025403784439,
1.,0.866025403784439,1.,0.866025403784439,1.,0.866025403784439,1.,0.866025403784439,
1.,0.866025403784439,1.,0.866025403784439,1.,0.866025403784439,1.,0.866025403784439,
1.,0.866025403784439,1.,0.866025403784439,1.,0.866025403784439,1.,0.866025403784439,
1.,0.866025403784439,1.,0.866025403784439,1.,0.866025403784439,1.,0.866025403784439,
1.,0.866025403784439,1.,0.866025403784439,1.,0.866025403784439,1.,0.866025403784439,
1.,0.866025403784439,1.,0.866025403784439,1.,0.866025403784439,1.,0.866025403784439,
1.,0.866025403784439,1.,0.866025403784439,1.,0.866025403784439,1.)))
REPRESENTATION_ITEM('')
SURFACE()
);
#2316=(
BOUNDED_SURFACE()
B_SPLINE_SURFACE(1,2,((#368577,#368578,#368579,#368580,#368581,#368582,
#368583,#368584,#368585,#368586,#368587,#368588,#368589,#368590,#368591,
#368592,#368593,#368594,#368595,#368596,#368597,#368598,#368599,#368600,
#368601,#368602,#368603,#368604,#368605,#368606,#368607,#368608,#368609,
#368610,#368611,#368612,#368613,#368614,#368615,#368616,#368617,#368618,
#368619,#368620,#368621,#368622,#368623,#368624,#368625,#368626,#368627,
#368628,#368629,#368630,#368631,#368632,#368633,#368634,#368635,#368636,
#368637,#368638,#368639,#368640,#368641,#368642,#368643,#368644,#368645,
#368646,#368647,#368648,#368649,#368650,#368651,#368652,#368653,#368654,
#368655,#368656,#368657,#368658,#368659,#368660,#368661,#368662,#368663,
#368664,#368665,#368666,#368667,#368668,#368669,#368670,#368671,#368672,
#368673,#368674,#368675,#368676,#368677,#368678,#368679,#368680,#368681,
#368682,#368683,#368684,#368685,#368686,#368687,#368688,#368689,#368690,
#368691,#368692,#368693,#368694,#368695,#368696,#368697,#368698,#368699,
#368700,#368701,#368702,#368703,#368704,#368705,#368706,#368707,#368708,
#368709,#368710,#368711,#368712,#368713,#368714,#368715,#368716,#368717,
#368718,#368719,#368720,#368721,#368722,#368723,#368724,#368725,#368726,
#368727,#368728,#368729,#368730,#368731,#368732,#368733,#368734,#368735,
#368736,#368737,#368738,#368739,#368740,#368741,#368742,#368743,#368744,
#368745,#368746,#368747,#368748,#368749,#368750,#368751,#368752,#368753,
#368754,#368755,#368756,#368757,#368758,#368759,#368760,#368761,#368762,
#368763,#368764,#368765,#368766,#368767,#368768,#368769,#368770,#368771,
#368772,#368773,#368774,#368775,#368776,#368777,#368778,#368779,#368780,
#368781),(#368782,#368783,#368784,#368785,#368786,#368787,#368788,#368789,
#368790,#368791,#368792,#368793,#368794,#368795,#368796,#368797,#368798,
#368799,#368800,#368801,#368802,#368803,#368804,#368805,#368806,#368807,
#368808,#368809,#368810,#368811,#368812,#368813,#368814,#368815,#368816,
#368817,#368818,#368819,#368820,#368821,#368822,#368823,#368824,#368825,
#368826,#368827,#368828,#368829,#368830,#368831,#368832,#368833,#368834,
#368835,#368836,#368837,#368838,#368839,#368840,#368841,#368842,#368843,
#368844,#368845,#368846,#368847,#368848,#368849,#368850,#368851,#368852,
#368853,#368854,#368855,#368856,#368857,#368858,#368859,#368860,#368861,
#368862,#368863,#368864,#368865,#368866,#368867,#368868,#368869,#368870,
#368871,#368872,#368873,#368874,#368875,#368876,#368877,#368878,#368879,
#368880,#368881,#368882,#368883,#368884,#368885,#368886,#368887,#368888,
#368889,#368890,#368891,#368892,#368893,#368894,#368895,#368896,#368897,
#368898,#368899,#368900,#368901,#368902,#368903,#368904,#368905,#368906,
#368907,#368908,#368909,#368910,#368911,#368912,#368913,#368914,#368915,
#368916,#368917,#368918,#368919,#368920,#368921,#368922,#368923,#368924,
#368925,#368926,#368927,#368928,#368929,#368930,#368931,#368932,#368933,
#368934,#368935,#368936,#368937,#368938,#368939,#368940,#368941,#368942,
#368943,#368944,#368945,#368946,#368947,#368948,#368949,#368950,#368951,
#368952,#368953,#368954,#368955,#368956,#368957,#368958,#368959,#368960,
#368961,#368962,#368963,#368964,#368965,#368966,#368967,#368968,#368969,
#368970,#368971,#368972,#368973,#368974,#368975,#368976,#368977,#368978,
#368979,#368980,#368981,#368982,#368983,#368984,#368985,#368986)),
 .UNSPECIFIED.,.F.,.F.,.F.)
B_SPLINE_SURFACE_WITH_KNOTS((2,2),(3,2,2,2,2,2,2,2,2,2,2,2,2,2,2,2,2,2,
2,2,2,2,2,2,2,2,2,2,2,2,2,2,2,2,2,2,2,2,2,2,2,2,2,2,2,2,2,2,2,2,2,2,2,2,
2,2,2,2,2,2,2,2,2,2,2,2,2,2,2,2,2,2,2,2,2,2,2,2,2,2,2,2,2,2,2,2,2,2,2,2,
2,2,2,2,2,2,2,2,2,2,2,2,3),(-2.36351427691722E-5,1.),(0.,0.00980392156862745,
0.0196078431372549,0.0294117647058824,0.0392156862745098,0.0490196078431373,
0.0588235294117647,0.0686274509803922,0.0784313725490196,0.0882352941176471,
0.0980392156862745,0.107843137254902,0.117647058823529,0.127450980392157,
0.137254901960784,0.147058823529412,0.156862745098039,0.166666666666667,
0.176470588235294,0.186274509803922,0.196078431372549,0.205882352941176,
0.215686274509804,0.225490196078431,0.235294117647059,0.245098039215686,
0.254901960784314,0.264705882352941,0.274509803921569,0.284313725490196,
0.294117647058824,0.303921568627451,0.313725490196078,0.323529411764706,
0.333333333333333,0.343137254901961,0.352941176470588,0.362745098039216,
0.372549019607843,0.382352941176471,0.392156862745098,0.401960784313726,
0.411764705882353,0.42156862745098,0.431372549019608,0.441176470588235,
0.450980392156863,0.46078431372549,0.470588235294118,0.480392156862745,
0.490196078431373,0.5,0.509803921568627,0.519607843137255,0.529411764705882,
0.53921568627451,0.549019607843137,0.558823529411765,0.568627450980392,
0.57843137254902,0.588235294117647,0.598039215686274,0.607843137254902,
0.617647058823529,0.627450980392157,0.637254901960784,0.647058823529412,
0.656862745098039,0.666666666666667,0.676470588235294,0.686274509803922,
0.696078431372549,0.705882352941177,0.715686274509804,0.725490196078431,
0.735294117647059,0.745098039215686,0.754901960784314,0.764705882352941,
0.774509803921569,0.784313725490196,0.794117647058823,0.803921568627451,
0.813725490196078,0.823529411764706,0.833333333333333,0.843137254901961,
0.852941176470588,0.862745098039216,0.872549019607843,0.882352941176471,
0.892156862745098,0.901960784313726,0.911764705882353,0.92156862745098,
0.931372549019608,0.941176470588235,0.950980392156863,0.96078431372549,
0.970588235294118,0.980392156862745,0.990196078431373,1.),.UNSPECIFIED.)
GEOMETRIC_REPRESENTATION_ITEM()
RATIONAL_B_SPLINE_SURFACE(((1.,0.866025403784439,1.,0.866025403784439,1.,
0.866025403784439,1.,0.866025403784439,1.,0.866025403784439,1.,0.866025403784439,
1.,0.866025403784439,1.,0.866025403784439,1.,0.866025403784439,1.,0.866025403784439,
1.,0.866025403784439,1.,0.866025403784439,1.,0.866025403784439,1.,0.866025403784439,
1.,0.866025403784439,1.,0.866025403784439,1.,0.866025403784439,1.,0.866025403784439,
1.,0.866025403784439,1.,0.866025403784439,1.,0.866025403784439,1.,0.866025403784439,
1.,0.866025403784439,1.,0.866025403784439,1.,0.866025403784439,1.,0.866025403784439,
1.,0.866025403784439,1.,0.866025403784439,1.,0.866025403784439,1.,0.866025403784439,
1.,0.866025403784439,1.,0.866025403784439,1.,0.866025403784439,1.,0.866025403784439,
1.,0.866025403784439,1.,0.866025403784439,1.,0.866025403784439,1.,0.866025403784439,
1.,0.866025403784439,1.,0.866025403784439,1.,0.866025403784439,1.,0.866025403784439,
1.,0.866025403784439,1.,0.866025403784439,1.,0.866025403784439,1.,0.866025403784439,
1.,0.866025403784439,1.,0.866025403784439,1.,0.866025403784439,1.,0.866025403784439,
1.,0.866025403784439,1.,0.866025403784439,1.,0.866025403784439,1.,0.866025403784439,
1.,0.866025403784439,1.,0.866025403784439,1.,0.866025403784439,1.,0.866025403784439,
1.,0.866025403784439,1.,0.866025403784439,1.,0.866025403784439,1.,0.866025403784439,
1.,0.866025403784439,1.,0.866025403784439,1.,0.866025403784439,1.,0.866025403784439,
1.,0.866025403784439,1.,0.866025403784439,1.,0.866025403784439,1.,0.866025403784439,
1.,0.866025403784439,1.,0.866025403784439,1.,0.866025403784439,1.,0.866025403784439,
1.,0.866025403784439,1.,0.866025403784439,1.,0.866025403784439,1.,0.866025403784439,
1.,0.866025403784439,1.,0.866025403784439,1.,0.866025403784439,1.,0.866025403784439,
1.,0.866025403784439,1.,0.866025403784439,1.,0.866025403784439,1.,0.866025403784439,
1.,0.866025403784439,1.,0.866025403784439,1.,0.866025403784439,1.,0.866025403784439,
1.,0.866025403784439,1.,0.866025403784439,1.,0.866025403784439,1.,0.866025403784439,
1.,0.866025403784439,1.,0.866025403784439,1.,0.866025403784439,1.,0.866025403784439,
1.,0.866025403784439,1.,0.866025403784439,1.,0.866025403784439,1.,0.866025403784439,
1.),(1.,0.866025403784439,1.,0.866025403784439,1.,0.866025403784439,1.,
0.866025403784439,1.,0.866025403784439,1.,0.866025403784439,1.,0.866025403784439,
1.,0.866025403784439,1.,0.866025403784439,1.,0.866025403784439,1.,0.866025403784439,
1.,0.866025403784439,1.,0.866025403784439,1.,0.866025403784439,1.,0.866025403784439,
1.,0.866025403784439,1.,0.866025403784439,1.,0.866025403784439,1.,0.866025403784439,
1.,0.866025403784439,1.,0.866025403784439,1.,0.866025403784439,1.,0.866025403784439,
1.,0.866025403784439,1.,0.866025403784439,1.,0.866025403784439,1.,0.866025403784439,
1.,0.866025403784439,1.,0.866025403784439,1.,0.866025403784439,1.,0.866025403784439,
1.,0.866025403784439,1.,0.866025403784439,1.,0.866025403784439,1.,0.866025403784439,
1.,0.866025403784439,1.,0.866025403784439,1.,0.866025403784439,1.,0.866025403784439,
1.,0.866025403784439,1.,0.866025403784439,1.,0.866025403784439,1.,0.866025403784439,
1.,0.866025403784439,1.,0.866025403784439,1.,0.866025403784439,1.,0.866025403784439,
1.,0.866025403784439,1.,0.866025403784439,1.,0.866025403784439,1.,0.866025403784439,
1.,0.866025403784439,1.,0.866025403784439,1.,0.866025403784439,1.,0.866025403784439,
1.,0.866025403784439,1.,0.866025403784439,1.,0.866025403784439,1.,0.866025403784439,
1.,0.866025403784439,1.,0.866025403784439,1.,0.866025403784439,1.,0.866025403784439,
1.,0.866025403784439,1.,0.866025403784439,1.,0.866025403784439,1.,0.866025403784439,
1.,0.866025403784439,1.,0.866025403784439,1.,0.866025403784439,1.,0.866025403784439,
1.,0.866025403784439,1.,0.866025403784439,1.,0.866025403784439,1.,0.866025403784439,
1.,0.866025403784439,1.,0.866025403784439,1.,0.866025403784439,1.,0.866025403784439,
1.,0.866025403784439,1.,0.866025403784439,1.,0.866025403784439,1.,0.866025403784439,
1.,0.866025403784439,1.,0.866025403784439,1.,0.866025403784439,1.,0.866025403784439,
1.,0.866025403784439,1.,0.866025403784439,1.,0.866025403784439,1.,0.866025403784439,
1.,0.866025403784439,1.,0.866025403784439,1.,0.866025403784439,1.,0.866025403784439,
1.,0.866025403784439,1.,0.866025403784439,1.,0.866025403784439,1.,0.866025403784439,
1.,0.866025403784439,1.,0.866025403784439,1.,0.866025403784439,1.)))
REPRESENTATION_ITEM('')
SURFACE()
);
#4185=(
BOUNDED_CURVE()
B_SPLINE_CURVE(2,(#366331,#366332,#366333),.UNSPECIFIED.,.F.,.F.)
B_SPLINE_CURVE_WITH_KNOTS((3,3),(0.0278449963604202,0.0294117647058824),
 .UNSPECIFIED.)
CURVE()
GEOMETRIC_REPRESENTATION_ITEM()
RATIONAL_B_SPLINE_CURVE((0.964022189566693,0.978589470042446,1.))
REPRESENTATION_ITEM('')
);
#4186=(
BOUNDED_CURVE()
B_SPLINE_CURVE(2,(#366339,#366340,#366341,#366342,#366343,#366344,#366345,
#366346,#366347,#366348,#366349,#366350,#366351),.UNSPECIFIED.,.F.,.F.)
B_SPLINE_CURVE_WITH_KNOTS((3,2,2,2,2,2,3),(0.0294117647058824,0.0392156862745098,
0.0490196078431373,0.0588235294117647,0.0686274509803922,0.0784313725490196,
0.0882352941176471),.UNSPECIFIED.)
CURVE()
GEOMETRIC_REPRESENTATION_ITEM()
RATIONAL_B_SPLINE_CURVE((1.,0.866025403784439,1.,0.866025403784439,1.,0.866025403784439,
1.,0.866025403784439,1.,0.866025403784439,1.,0.866025403784439,1.))
REPRESENTATION_ITEM('')
);
#4187=(
BOUNDED_CURVE()
B_SPLINE_CURVE(2,(#366354,#366355,#366356,#366357,#366358,#366359,#366360,
#366361,#366362,#366363,#366364,#366365,#366366),.UNSPECIFIED.,.F.,.F.)
B_SPLINE_CURVE_WITH_KNOTS((3,2,2,2,2,2,3),(0.035257343498756,0.0392156862745098,
0.0490196078431373,0.0588235294117647,0.0686274509803922,0.0784313725490196,
0.0882352941176471),.UNSPECIFIED.)
CURVE()
GEOMETRIC_REPRESENTATION_ITEM()
RATIONAL_B_SPLINE_CURVE((0.935494950279678,0.945907627743432,1.,0.866025403784439,
1.,0.866025403784439,1.,0.866025403784439,1.,0.866025403784439,1.,0.866025403784439,
1.))
REPRESENTATION_ITEM('')
);
#4188=(
BOUNDED_CURVE()
B_SPLINE_CURVE(2,(#366371,#366372,#366373,#366374,#366375,#366376,#366377,
#366378,#366379,#366380,#366381,#366382,#366383),.UNSPECIFIED.,.F.,.F.)
B_SPLINE_CURVE_WITH_KNOTS((3,2,2,2,2,2,3),(0.0882352941176471,0.0980392156862745,
0.107843137254902,0.117647058823529,0.127450980392157,0.137254901960784,
0.147058823529412),.UNSPECIFIED.)
CURVE()
GEOMETRIC_REPRESENTATION_ITEM()
RATIONAL_B_SPLINE_CURVE((1.,0.866025403784439,1.,0.866025403784439,1.,0.866025403784439,
1.,0.866025403784439,1.,0.866025403784439,1.,0.866025403784439,1.))
REPRESENTATION_ITEM('')
);
#4189=(
BOUNDED_CURVE()
B_SPLINE_CURVE(2,(#366384,#366385,#366386,#366387,#366388,#366389,#366390,
#366391,#366392,#366393,#366394,#366395,#366396),.UNSPECIFIED.,.F.,.F.)
B_SPLINE_CURVE_WITH_KNOTS((3,2,2,2,2,2,3),(0.0882352941176471,0.0980392156862745,
0.107843137254902,0.117647058823529,0.127450980392157,0.137254901960784,
0.147058823529412),.UNSPECIFIED.)
CURVE()
GEOMETRIC_REPRESENTATION_ITEM()
RATIONAL_B_SPLINE_CURVE((1.,0.866025403784439,1.,0.866025403784439,1.,0.866025403784439,
1.,0.866025403784439,1.,0.866025403784439,1.,0.866025403784439,1.))
REPRESENTATION_ITEM('')
);
#4190=(
BOUNDED_CURVE()
B_SPLINE_CURVE(2,(#366401,#366402,#366403,#366404,#366405,#366406,#366407,
#366408,#366409,#366410,#366411,#366412,#366413),.UNSPECIFIED.,.F.,.F.)
B_SPLINE_CURVE_WITH_KNOTS((3,2,2,2,2,2,3),(0.147058823529412,0.156862745098039,
0.166666666666667,0.176470588235294,0.186274509803922,0.196078431372549,
0.205882352941176),.UNSPECIFIED.)
CURVE()
GEOMETRIC_REPRESENTATION_ITEM()
RATIONAL_B_SPLINE_CURVE((1.,0.866025403784439,1.,0.866025403784439,1.,0.866025403784439,
1.,0.866025403784439,1.,0.866025403784439,1.,0.866025403784439,1.))
REPRESENTATION_ITEM('')
);
#4191=(
BOUNDED_CURVE()
B_SPLINE_CURVE(2,(#366414,#366415,#366416,#366417,#366418,#366419,#366420,
#366421,#366422,#366423,#366424,#366425,#366426),.UNSPECIFIED.,.F.,.F.)
B_SPLINE_CURVE_WITH_KNOTS((3,2,2,2,2,2,3),(0.147058823529412,0.156862745098039,
0.166666666666667,0.176470588235294,0.186274509803922,0.196078431372549,
0.205882352941177),.UNSPECIFIED.)
CURVE()
GEOMETRIC_REPRESENTATION_ITEM()
RATIONAL_B_SPLINE_CURVE((1.,0.866025403784439,1.,0.866025403784439,1.,0.866025403784439,
1.,0.866025403784439,1.,0.866025403784439,1.,0.866025403784439,1.))
REPRESENTATION_ITEM('')
);
#4192=(
BOUNDED_CURVE()
B_SPLINE_CURVE(2,(#366431,#366432,#366433,#366434,#366435,#366436,#366437,
#366438,#366439,#366440,#366441,#366442,#366443),.UNSPECIFIED.,.F.,.F.)
B_SPLINE_CURVE_WITH_KNOTS((3,2,2,2,2,2,3),(0.205882352941176,0.215686274509804,
0.225490196078431,0.235294117647059,0.245098039215686,0.254901960784314,
0.264705882352941),.UNSPECIFIED.)
CURVE()
GEOMETRIC_REPRESENTATION_ITEM()
RATIONAL_B_SPLINE_CURVE((1.,0.866025403784439,1.,0.866025403784439,1.,0.866025403784439,
1.,0.866025403784439,1.,0.866025403784439,1.,0.866025403784439,1.))
REPRESENTATION_ITEM('')
);
#4193=(
BOUNDED_CURVE()
B_SPLINE_CURVE(2,(#366444,#366445,#366446,#366447,#366448,#366449,#366450,
#366451,#366452,#366453,#366454,#366455,#366456),.UNSPECIFIED.,.F.,.F.)
B_SPLINE_CURVE_WITH_KNOTS((3,2,2,2,2,2,3),(0.205882352941177,0.215686274509804,
0.225490196078431,0.235294117647059,0.245098039215686,0.254901960784314,
0.264705882352941),.UNSPECIFIED.)
CURVE()
GEOMETRIC_REPRESENTATION_ITEM()
RATIONAL_B_SPLINE_CURVE((1.,0.866025403784439,1.,0.866025403784439,1.,0.866025403784439,
1.,0.866025403784439,1.,0.866025403784439,1.,0.866025403784439,1.))
REPRESENTATION_ITEM('')
);
#4194=(
BOUNDED_CURVE()
B_SPLINE_CURVE(2,(#366461,#366462,#366463,#366464,#366465,#366466,#366467,
#366468,#366469,#366470,#366471,#366472,#366473),.UNSPECIFIED.,.F.,.F.)
B_SPLINE_CURVE_WITH_KNOTS((3,2,2,2,2,2,3),(0.264705882352941,0.274509803921569,
0.284313725490196,0.294117647058824,0.303921568627451,0.313725490196078,
0.323529411764706),.UNSPECIFIED.)
CURVE()
GEOMETRIC_REPRESENTATION_ITEM()
RATIONAL_B_SPLINE_CURVE((1.,0.866025403784439,1.,0.866025403784439,1.,0.866025403784439,
1.,0.866025403784439,1.,0.866025403784439,1.,0.866025403784439,1.))
REPRESENTATION_ITEM('')
);
#4195=(
BOUNDED_CURVE()
B_SPLINE_CURVE(2,(#366474,#366475,#366476,#366477,#366478,#366479,#366480,
#366481,#366482,#366483,#366484,#366485,#366486),.UNSPECIFIED.,.F.,.F.)
B_SPLINE_CURVE_WITH_KNOTS((3,2,2,2,2,2,3),(0.264705882352941,0.274509803921569,
0.284313725490196,0.294117647058824,0.303921568627451,0.313725490196078,
0.323529411764706),.UNSPECIFIED.)
CURVE()
GEOMETRIC_REPRESENTATION_ITEM()
RATIONAL_B_SPLINE_CURVE((1.,0.866025403784439,1.,0.866025403784439,1.,0.866025403784439,
1.,0.866025403784439,1.,0.866025403784439,1.,0.866025403784439,1.))
REPRESENTATION_ITEM('')
);
#4196=(
BOUNDED_CURVE()
B_SPLINE_CURVE(2,(#366491,#366492,#366493,#366494,#366495,#366496,#366497,
#366498,#366499,#366500,#366501,#366502,#366503),.UNSPECIFIED.,.F.,.F.)
B_SPLINE_CURVE_WITH_KNOTS((3,2,2,2,2,2,3),(0.323529411764706,0.333333333333333,
0.343137254901961,0.352941176470588,0.362745098039216,0.372549019607843,
0.382352941176471),.UNSPECIFIED.)
CURVE()
GEOMETRIC_REPRESENTATION_ITEM()
RATIONAL_B_SPLINE_CURVE((1.,0.866025403784439,1.,0.866025403784439,1.,0.866025403784439,
1.,0.866025403784439,1.,0.866025403784439,1.,0.866025403784439,1.))
REPRESENTATION_ITEM('')
);
#4197=(
BOUNDED_CURVE()
B_SPLINE_CURVE(2,(#366504,#366505,#366506,#366507,#366508,#366509,#366510,
#366511,#366512,#366513,#366514,#366515,#366516),.UNSPECIFIED.,.F.,.F.)
B_SPLINE_CURVE_WITH_KNOTS((3,2,2,2,2,2,3),(0.323529411764706,0.333333333333333,
0.343137254901961,0.352941176470588,0.362745098039216,0.372549019607843,
0.382352941176471),.UNSPECIFIED.)
CURVE()
GEOMETRIC_REPRESENTATION_ITEM()
RATIONAL_B_SPLINE_CURVE((1.,0.866025403784439,1.,0.866025403784439,1.,0.866025403784439,
1.,0.866025403784439,1.,0.866025403784439,1.,0.866025403784439,1.))
REPRESENTATION_ITEM('')
);
#4198=(
BOUNDED_CURVE()
B_SPLINE_CURVE(2,(#366521,#366522,#366523,#366524,#366525,#366526,#366527,
#366528,#366529,#366530,#366531,#366532,#366533),.UNSPECIFIED.,.F.,.F.)
B_SPLINE_CURVE_WITH_KNOTS((3,2,2,2,2,2,3),(0.382352941176471,0.392156862745098,
0.401960784313726,0.411764705882353,0.42156862745098,0.431372549019608,
0.441176470588235),.UNSPECIFIED.)
CURVE()
GEOMETRIC_REPRESENTATION_ITEM()
RATIONAL_B_SPLINE_CURVE((1.,0.866025403784439,1.,0.866025403784439,1.,0.866025403784439,
1.,0.866025403784439,1.,0.866025403784439,1.,0.866025403784439,1.))
REPRESENTATION_ITEM('')
);
#4199=(
BOUNDED_CURVE()
B_SPLINE_CURVE(2,(#366534,#366535,#366536,#366537,#366538,#366539,#366540,
#366541,#366542,#366543,#366544,#366545,#366546),.UNSPECIFIED.,.F.,.F.)
B_SPLINE_CURVE_WITH_KNOTS((3,2,2,2,2,2,3),(0.382352941176471,0.392156862745098,
0.401960784313726,0.411764705882353,0.421568627450981,0.431372549019608,
0.441176470588235),.UNSPECIFIED.)
CURVE()
GEOMETRIC_REPRESENTATION_ITEM()
RATIONAL_B_SPLINE_CURVE((1.,0.866025403784439,1.,0.866025403784439,1.,0.866025403784439,
1.,0.866025403784439,1.,0.866025403784439,1.,0.866025403784439,1.))
REPRESENTATION_ITEM('')
);
#4200=(
BOUNDED_CURVE()
B_SPLINE_CURVE(2,(#366551,#366552,#366553,#366554,#366555,#366556,#366557,
#366558,#366559,#366560,#366561,#366562,#366563),.UNSPECIFIED.,.F.,.F.)
B_SPLINE_CURVE_WITH_KNOTS((3,2,2,2,2,2,3),(0.441176470588235,0.450980392156863,
0.46078431372549,0.470588235294118,0.480392156862745,0.490196078431373,
0.5),.UNSPECIFIED.)
CURVE()
GEOMETRIC_REPRESENTATION_ITEM()
RATIONAL_B_SPLINE_CURVE((1.,0.866025403784439,1.,0.866025403784439,1.,0.866025403784439,
1.,0.866025403784439,1.,0.866025403784439,1.,0.866025403784439,1.))
REPRESENTATION_ITEM('')
);
#4201=(
BOUNDED_CURVE()
B_SPLINE_CURVE(2,(#366564,#366565,#366566,#366567,#366568,#366569,#366570,
#366571,#366572,#366573,#366574,#366575,#366576),.UNSPECIFIED.,.F.,.F.)
B_SPLINE_CURVE_WITH_KNOTS((3,2,2,2,2,2,3),(0.441176470588235,0.450980392156863,
0.46078431372549,0.470588235294118,0.480392156862745,0.490196078431373,
0.5),.UNSPECIFIED.)
CURVE()
GEOMETRIC_REPRESENTATION_ITEM()
RATIONAL_B_SPLINE_CURVE((1.,0.866025403784439,1.,0.866025403784439,1.,0.866025403784439,
1.,0.866025403784439,1.,0.866025403784439,1.,0.866025403784439,1.))
REPRESENTATION_ITEM('')
);
#4202=(
BOUNDED_CURVE()
B_SPLINE_CURVE(2,(#366581,#366582,#366583,#366584,#366585,#366586,#366587,
#366588,#366589,#366590,#366591,#366592,#366593),.UNSPECIFIED.,.F.,.F.)
B_SPLINE_CURVE_WITH_KNOTS((3,2,2,2,2,2,3),(0.5,0.509803921568627,0.519607843137255,
0.529411764705882,0.53921568627451,0.549019607843137,0.558823529411765),
 .UNSPECIFIED.)
CURVE()
GEOMETRIC_REPRESENTATION_ITEM()
RATIONAL_B_SPLINE_CURVE((1.,0.866025403784439,1.,0.866025403784439,1.,0.866025403784439,
1.,0.866025403784439,1.,0.866025403784439,1.,0.866025403784439,1.))
REPRESENTATION_ITEM('')
);
#4203=(
BOUNDED_CURVE()
B_SPLINE_CURVE(2,(#366594,#366595,#366596,#366597,#366598,#366599,#366600,
#366601,#366602,#366603,#366604,#366605,#366606),.UNSPECIFIED.,.F.,.F.)
B_SPLINE_CURVE_WITH_KNOTS((3,2,2,2,2,2,3),(0.5,0.509803921568628,0.519607843137255,
0.529411764705882,0.53921568627451,0.549019607843137,0.558823529411765),
 .UNSPECIFIED.)
CURVE()
GEOMETRIC_REPRESENTATION_ITEM()
RATIONAL_B_SPLINE_CURVE((1.,0.866025403784439,1.,0.866025403784439,1.,0.866025403784439,
1.,0.866025403784439,1.,0.866025403784439,1.,0.866025403784439,1.))
REPRESENTATION_ITEM('')
);
#4204=(
BOUNDED_CURVE()
B_SPLINE_CURVE(2,(#366611,#366612,#366613,#366614,#366615,#366616,#366617,
#366618,#366619,#366620,#366621,#366622,#366623),.UNSPECIFIED.,.F.,.F.)
B_SPLINE_CURVE_WITH_KNOTS((3,2,2,2,2,2,3),(0.558823529411765,0.568627450980392,
0.57843137254902,0.588235294117647,0.598039215686274,0.607843137254902,
0.617647058823529),.UNSPECIFIED.)
CURVE()
GEOMETRIC_REPRESENTATION_ITEM()
RATIONAL_B_SPLINE_CURVE((1.,0.866025403784439,1.,0.866025403784439,1.,0.866025403784439,
1.,0.866025403784439,1.,0.866025403784439,1.,0.866025403784439,1.))
REPRESENTATION_ITEM('')
);
#4205=(
BOUNDED_CURVE()
B_SPLINE_CURVE(2,(#366624,#366625,#366626,#366627,#366628,#366629,#366630,
#366631,#366632,#366633,#366634,#366635,#366636),.UNSPECIFIED.,.F.,.F.)
B_SPLINE_CURVE_WITH_KNOTS((3,2,2,2,2,2,3),(0.558823529411765,0.568627450980392,
0.57843137254902,0.588235294117647,0.598039215686275,0.607843137254902,
0.61764705882353),.UNSPECIFIED.)
CURVE()
GEOMETRIC_REPRESENTATION_ITEM()
RATIONAL_B_SPLINE_CURVE((1.,0.866025403784439,1.,0.866025403784439,1.,0.866025403784439,
1.,0.866025403784439,1.,0.866025403784439,1.,0.866025403784439,1.))
REPRESENTATION_ITEM('')
);
#4206=(
BOUNDED_CURVE()
B_SPLINE_CURVE(2,(#366641,#366642,#366643,#366644,#366645,#366646,#366647,
#366648,#366649,#366650,#366651,#366652,#366653),.UNSPECIFIED.,.F.,.F.)
B_SPLINE_CURVE_WITH_KNOTS((3,2,2,2,2,2,3),(0.617647058823529,0.627450980392157,
0.637254901960784,0.647058823529412,0.656862745098039,0.666666666666667,
0.676470588235294),.UNSPECIFIED.)
CURVE()
GEOMETRIC_REPRESENTATION_ITEM()
RATIONAL_B_SPLINE_CURVE((1.,0.866025403784439,1.,0.866025403784439,1.,0.866025403784439,
1.,0.866025403784439,1.,0.866025403784439,1.,0.866025403784439,1.))
REPRESENTATION_ITEM('')
);
#4207=(
BOUNDED_CURVE()
B_SPLINE_CURVE(2,(#366654,#366655,#366656,#366657,#366658,#366659,#366660,
#366661,#366662,#366663,#366664,#366665,#366666),.UNSPECIFIED.,.F.,.F.)
B_SPLINE_CURVE_WITH_KNOTS((3,2,2,2,2,2,3),(0.61764705882353,0.627450980392157,
0.637254901960784,0.647058823529412,0.656862745098039,0.666666666666667,
0.676470588235294),.UNSPECIFIED.)
CURVE()
GEOMETRIC_REPRESENTATION_ITEM()
RATIONAL_B_SPLINE_CURVE((1.,0.866025403784439,1.,0.866025403784439,1.,0.866025403784439,
1.,0.866025403784439,1.,0.866025403784439,1.,0.866025403784439,1.))
REPRESENTATION_ITEM('')
);
#4208=(
BOUNDED_CURVE()
B_SPLINE_CURVE(2,(#366671,#366672,#366673,#366674,#366675,#366676,#366677,
#366678,#366679,#366680,#366681,#366682,#366683),.UNSPECIFIED.,.F.,.F.)
B_SPLINE_CURVE_WITH_KNOTS((3,2,2,2,2,2,3),(0.676470588235294,0.686274509803922,
0.696078431372549,0.705882352941177,0.715686274509804,0.725490196078431,
0.735294117647059),.UNSPECIFIED.)
CURVE()
GEOMETRIC_REPRESENTATION_ITEM()
RATIONAL_B_SPLINE_CURVE((1.,0.866025403784439,1.,0.866025403784439,1.,0.866025403784439,
1.,0.866025403784439,1.,0.866025403784439,1.,0.866025403784439,1.))
REPRESENTATION_ITEM('')
);
#4209=(
BOUNDED_CURVE()
B_SPLINE_CURVE(2,(#366684,#366685,#366686,#366687,#366688,#366689,#366690,
#366691,#366692,#366693,#366694,#366695,#366696),.UNSPECIFIED.,.F.,.F.)
B_SPLINE_CURVE_WITH_KNOTS((3,2,2,2,2,2,3),(0.676470588235294,0.686274509803922,
0.696078431372549,0.705882352941177,0.715686274509804,0.725490196078431,
0.735294117647059),.UNSPECIFIED.)
CURVE()
GEOMETRIC_REPRESENTATION_ITEM()
RATIONAL_B_SPLINE_CURVE((1.,0.866025403784439,1.,0.866025403784439,1.,0.866025403784439,
1.,0.866025403784439,1.,0.866025403784439,1.,0.866025403784439,1.))
REPRESENTATION_ITEM('')
);
#4210=(
BOUNDED_CURVE()
B_SPLINE_CURVE(2,(#366701,#366702,#366703,#366704,#366705,#366706,#366707,
#366708,#366709,#366710,#366711,#366712,#366713),.UNSPECIFIED.,.F.,.F.)
B_SPLINE_CURVE_WITH_KNOTS((3,2,2,2,2,2,3),(0.735294117647059,0.745098039215686,
0.754901960784314,0.764705882352941,0.774509803921569,0.784313725490196,
0.794117647058823),.UNSPECIFIED.)
CURVE()
GEOMETRIC_REPRESENTATION_ITEM()
RATIONAL_B_SPLINE_CURVE((1.,0.866025403784439,1.,0.866025403784439,1.,0.866025403784439,
1.,0.866025403784439,1.,0.866025403784439,1.,0.866025403784439,1.))
REPRESENTATION_ITEM('')
);
#4211=(
BOUNDED_CURVE()
B_SPLINE_CURVE(2,(#366714,#366715,#366716,#366717,#366718,#366719,#366720,
#366721,#366722,#366723,#366724,#366725,#366726),.UNSPECIFIED.,.F.,.F.)
B_SPLINE_CURVE_WITH_KNOTS((3,2,2,2,2,2,3),(0.735294117647059,0.745098039215686,
0.754901960784314,0.764705882352941,0.774509803921569,0.784313725490196,
0.794117647058824),.UNSPECIFIED.)
CURVE()
GEOMETRIC_REPRESENTATION_ITEM()
RATIONAL_B_SPLINE_CURVE((1.,0.866025403784439,1.,0.866025403784439,1.,0.866025403784439,
1.,0.866025403784439,1.,0.866025403784439,1.,0.866025403784439,1.))
REPRESENTATION_ITEM('')
);
#4212=(
BOUNDED_CURVE()
B_SPLINE_CURVE(2,(#366731,#366732,#366733,#366734,#366735,#366736,#366737,
#366738,#366739,#366740,#366741,#366742,#366743),.UNSPECIFIED.,.F.,.F.)
B_SPLINE_CURVE_WITH_KNOTS((3,2,2,2,2,2,3),(0.794117647058823,0.803921568627451,
0.813725490196078,0.823529411764706,0.833333333333333,0.843137254901961,
0.852941176470588),.UNSPECIFIED.)
CURVE()
GEOMETRIC_REPRESENTATION_ITEM()
RATIONAL_B_SPLINE_CURVE((1.,0.866025403784439,1.,0.866025403784439,1.,0.866025403784439,
1.,0.866025403784439,1.,0.866025403784439,1.,0.866025403784439,1.))
REPRESENTATION_ITEM('')
);
#4213=(
BOUNDED_CURVE()
B_SPLINE_CURVE(2,(#366744,#366745,#366746,#366747,#366748,#366749,#366750,
#366751,#366752,#366753,#366754,#366755,#366756),.UNSPECIFIED.,.F.,.F.)
B_SPLINE_CURVE_WITH_KNOTS((3,2,2,2,2,2,3),(0.794117647058824,0.803921568627451,
0.813725490196079,0.823529411764706,0.833333333333333,0.843137254901961,
0.852941176470588),.UNSPECIFIED.)
CURVE()
GEOMETRIC_REPRESENTATION_ITEM()
RATIONAL_B_SPLINE_CURVE((1.,0.866025403784439,1.,0.866025403784439,1.,0.866025403784439,
1.,0.866025403784439,1.,0.866025403784439,1.,0.866025403784439,1.))
REPRESENTATION_ITEM('')
);
#4214=(
BOUNDED_CURVE()
B_SPLINE_CURVE(2,(#366761,#366762,#366763,#366764,#366765,#366766,#366767,
#366768,#366769,#366770,#366771,#366772,#366773),.UNSPECIFIED.,.F.,.F.)
B_SPLINE_CURVE_WITH_KNOTS((3,2,2,2,2,2,3),(0.852941176470588,0.862745098039216,
0.872549019607843,0.882352941176471,0.892156862745098,0.901960784313726,
0.911764705882353),.UNSPECIFIED.)
CURVE()
GEOMETRIC_REPRESENTATION_ITEM()
RATIONAL_B_SPLINE_CURVE((1.,0.866025403784439,1.,0.866025403784439,1.,0.866025403784439,
1.,0.866025403784439,1.,0.866025403784439,1.,0.866025403784439,1.))
REPRESENTATION_ITEM('')
);
#4215=(
BOUNDED_CURVE()
B_SPLINE_CURVE(2,(#366774,#366775,#366776,#366777,#366778,#366779,#366780,
#366781,#366782,#366783,#366784,#366785,#366786),.UNSPECIFIED.,.F.,.F.)
B_SPLINE_CURVE_WITH_KNOTS((3,2,2,2,2,2,3),(0.852941176470588,0.862745098039216,
0.872549019607843,0.882352941176471,0.892156862745098,0.901960784313726,
0.911764705882353),.UNSPECIFIED.)
CURVE()
GEOMETRIC_REPRESENTATION_ITEM()
RATIONAL_B_SPLINE_CURVE((1.,0.866025403784439,1.,0.866025403784439,1.,0.866025403784439,
1.,0.866025403784439,1.,0.866025403784439,1.,0.866025403784439,1.))
REPRESENTATION_ITEM('')
);
#4216=(
BOUNDED_CURVE()
B_SPLINE_CURVE(2,(#367905,#367906,#367907),.UNSPECIFIED.,.F.,.F.)
B_SPLINE_CURVE_WITH_KNOTS((3,3),(0.124274873543865,0.321867155116299),
 .UNSPECIFIED.)
CURVE()
GEOMETRIC_REPRESENTATION_ITEM()
RATIONAL_B_SPLINE_CURVE((1.46410161513778,1.69059892324148,1.46410161513778))
REPRESENTATION_ITEM('')
);
#4217=(
BOUNDED_CURVE()
B_SPLINE_CURVE(2,(#368096,#368097,#368098),.UNSPECIFIED.,.F.,.F.)
B_SPLINE_CURVE_WITH_KNOTS((3,3),(-0.3218671551163,-0.124274873543866),
 .UNSPECIFIED.)
CURVE()
GEOMETRIC_REPRESENTATION_ITEM()
RATIONAL_B_SPLINE_CURVE((1.46410161513778,1.69059892324148,1.46410161513778))
REPRESENTATION_ITEM('')
);
#4218=(
BOUNDED_CURVE()
B_SPLINE_CURVE(2,(#368100,#368101,#368102),.UNSPECIFIED.,.F.,.F.)
B_SPLINE_CURVE_WITH_KNOTS((3,3),(-0.321867155116299,-0.124274873543865),
 .UNSPECIFIED.)
CURVE()
GEOMETRIC_REPRESENTATION_ITEM()
RATIONAL_B_SPLINE_CURVE((1.46410161513778,1.69059892324148,1.46410161513778))
REPRESENTATION_ITEM('')
);
#4219=(
BOUNDED_CURVE()
B_SPLINE_CURVE(2,(#368104,#368105,#368106),.UNSPECIFIED.,.F.,.F.)
B_SPLINE_CURVE_WITH_KNOTS((3,3),(-0.321867155116299,-0.124274873543865),
 .UNSPECIFIED.)
CURVE()
GEOMETRIC_REPRESENTATION_ITEM()
RATIONAL_B_SPLINE_CURVE((1.46410161513778,1.69059892324148,1.46410161513778))
REPRESENTATION_ITEM('')
);
#4220=(
BOUNDED_CURVE()
B_SPLINE_CURVE(2,(#368108,#368109,#368110),.UNSPECIFIED.,.F.,.F.)
B_SPLINE_CURVE_WITH_KNOTS((3,3),(-0.321867155116299,-0.124274873543865),
 .UNSPECIFIED.)
CURVE()
GEOMETRIC_REPRESENTATION_ITEM()
RATIONAL_B_SPLINE_CURVE((1.46410161513778,1.69059892324148,1.46410161513778))
REPRESENTATION_ITEM('')
);
#4221=(
BOUNDED_CURVE()
B_SPLINE_CURVE(2,(#368112,#368113,#368114),.UNSPECIFIED.,.F.,.F.)
B_SPLINE_CURVE_WITH_KNOTS((3,3),(-0.321867155116299,-0.124274873543865),
 .UNSPECIFIED.)
CURVE()
GEOMETRIC_REPRESENTATION_ITEM()
RATIONAL_B_SPLINE_CURVE((1.46410161513778,1.69059892324148,1.46410161513778))
REPRESENTATION_ITEM('')
);
#4222=(
BOUNDED_CURVE()
B_SPLINE_CURVE(2,(#368550,#368551,#368552,#368553,#368554,#368555,#368556,
#368557,#368558,#368559,#368560,#368561,#368562),.UNSPECIFIED.,.F.,.F.)
B_SPLINE_CURVE_WITH_KNOTS((3,2,2,2,2,2,3),(0.911764705882353,0.921568627450981,
0.931372549019608,0.941176470588236,0.950980392156863,0.96078431372549,
0.970588235294118),.UNSPECIFIED.)
CURVE()
GEOMETRIC_REPRESENTATION_ITEM()
RATIONAL_B_SPLINE_CURVE((1.,0.866025403784439,1.,0.866025403784439,1.,0.866025403784439,
1.,0.866025403784439,1.,0.866025403784439,1.,0.866025403784436,1.))
REPRESENTATION_ITEM('')
);
#4223=(
BOUNDED_CURVE()
B_SPLINE_CURVE(2,(#368564,#368565,#368566,#368567,#368568,#368569,#368570,
#368571,#368572,#368573,#368574,#368575,#368576),.UNSPECIFIED.,.F.,.F.)
B_SPLINE_CURVE_WITH_KNOTS((3,2,2,2,2,2,3),(0.911764705882353,0.92156862745098,
0.931372549019608,0.941176470588235,0.950980392156863,0.96078431372549,
0.963362585267837),.UNSPECIFIED.)
CURVE()
GEOMETRIC_REPRESENTATION_ITEM()
RATIONAL_B_SPLINE_CURVE((1.,0.866025403784439,1.,0.866025403784439,1.,0.866025403784439,
1.,0.866025403784439,1.,0.866025403784439,1.,0.964766865340364,0.948065210722612))
REPRESENTATION_ITEM('')
);
#4417=SHAPE_REPRESENTATION_RELATIONSHIP('SRR','None',#459343,#4438);
#4438=ADVANCED_BREP_SHAPE_REPRESENTATION('',(#4485),#459232);
#4485=MANIFOLD_SOLID_BREP('Body',#94663);
#4605=STYLED_ITEM('',(#459533),#4485);
#4888=CONICAL_SURFACE('',#99283,1.15470053837925,0.78539816339745);
#4889=CONICAL_SURFACE('',#99291,1.125,0.785398163397446);
#4890=CONICAL_SURFACE('',#99305,1.15470053837925,0.78539816339745);
#4891=CONICAL_SURFACE('',#99306,1.15470053837925,0.78539816339745);
#4892=CONICAL_SURFACE('',#99307,1.15470053837925,0.78539816339745);
#4893=CONICAL_SURFACE('',#99308,1.15470053837925,0.78539816339745);
#4894=CONICAL_SURFACE('',#99309,1.15470053837925,0.78539816339745);
#5221=FACE_BOUND('',#14393,.T.);
#5222=FACE_BOUND('',#14399,.T.);
#5223=FACE_BOUND('',#14401,.T.);
#5224=FACE_BOUND('',#14403,.T.);
#5705=PLANE('',#99295);
#5706=PLANE('',#99296);
#5707=PLANE('',#99298);
#5708=PLANE('',#99299);
#5709=PLANE('',#99310);
#5710=PLANE('',#99311);
#5711=PLANE('',#99312);
#5712=PLANE('',#99313);
#5713=PLANE('',#99314);
#5714=PLANE('',#99315);
#5715=PLANE('',#99316);
#8444=FACE_OUTER_BOUND('',#14360,.T.);
#8445=FACE_OUTER_BOUND('',#14361,.T.);
#8446=FACE_OUTER_BOUND('',#14362,.T.);
#8447=FACE_OUTER_BOUND('',#14363,.T.);
#8448=FACE_OUTER_BOUND('',#14364,.T.);
#8449=FACE_OUTER_BOUND('',#14365,.T.);
#8450=FACE_OUTER_BOUND('',#14366,.T.);
#8451=FACE_OUTER_BOUND('',#14367,.T.);
#8452=FACE_OUTER_BOUND('',#14368,.T.);
#8453=FACE_OUTER_BOUND('',#14369,.T.);
#8454=FACE_OUTER_BOUND('',#14370,.T.);
#8455=FACE_OUTER_BOUND('',#14371,.T.);
#8456=FACE_OUTER_BOUND('',#14372,.T.);
#8457=FACE_OUTER_BOUND('',#14373,.T.);
#8458=FACE_OUTER_BOUND('',#14374,.T.);
#8459=FACE_OUTER_BOUND('',#14375,.T.);
#8460=FACE_OUTER_BOUND('',#14376,.T.);
#8461=FACE_OUTER_BOUND('',#14377,.T.);
#8462=FACE_OUTER_BOUND('',#14378,.T.);
#8463=FACE_OUTER_BOUND('',#14379,.T.);
#8464=FACE_OUTER_BOUND('',#14380,.T.);
#8465=FACE_OUTER_BOUND('',#14381,.T.);
#8466=FACE_OUTER_BOUND('',#14382,.T.);
#8467=FACE_OUTER_BOUND('',#14383,.T.);
#8468=FACE_OUTER_BOUND('',#14384,.T.);
#8469=FACE_OUTER_BOUND('',#14385,.T.);
#8470=FACE_OUTER_BOUND('',#14386,.T.);
#8471=FACE_OUTER_BOUND('',#14387,.T.);
#8472=FACE_OUTER_BOUND('',#14388,.T.);
#8473=FACE_OUTER_BOUND('',#14389,.T.);
#8474=FACE_OUTER_BOUND('',#14390,.T.);
#8475=FACE_OUTER_BOUND('',#14391,.T.);
#8476=FACE_OUTER_BOUND('',#14392,.T.);
#8477=FACE_OUTER_BOUND('',#14394,.T.);
#8478=FACE_OUTER_BOUND('',#14395,.T.);
#8479=FACE_OUTER_BOUND('',#14396,.T.);
#8480=FACE_OUTER_BOUND('',#14397,.T.);
#8481=FACE_OUTER_BOUND('',#14398,.T.);
#8482=FACE_OUTER_BOUND('',#14400,.T.);
#8483=FACE_OUTER_BOUND('',#14402,.T.);
#8484=FACE_OUTER_BOUND('',#14404,.T.);
#8485=FACE_OUTER_BOUND('',#14405,.T.);
#8486=FACE_OUTER_BOUND('',#14406,.T.);
#8487=FACE_OUTER_BOUND('',#14407,.T.);
#8488=FACE_OUTER_BOUND('',#14408,.T.);
#8489=FACE_OUTER_BOUND('',#14409,.T.);
#8490=FACE_OUTER_BOUND('',#14410,.T.);
#8491=FACE_OUTER_BOUND('',#14411,.T.);
#8492=FACE_OUTER_BOUND('',#14412,.T.);
#8493=FACE_OUTER_BOUND('',#14413,.T.);
#8494=FACE_OUTER_BOUND('',#14414,.T.);
#8495=FACE_OUTER_BOUND('',#14415,.T.);
#8496=FACE_OUTER_BOUND('',#14416,.T.);
#8497=FACE_OUTER_BOUND('',#14417,.T.);
#8498=FACE_OUTER_BOUND('',#14418,.T.);
#14360=EDGE_LOOP('',(#69382,#69383,#69384));
#14361=EDGE_LOOP('',(#69385,#69386,#69387,#69388,#69389));
#14362=EDGE_LOOP('',(#69390,#69391,#69392,#69393));
#14363=EDGE_LOOP('',(#69394,#69395,#69396,#69397));
#14364=EDGE_LOOP('',(#69398,#69399,#69400,#69401));
#14365=EDGE_LOOP('',(#69402,#69403,#69404,#69405));
#14366=EDGE_LOOP('',(#69406,#69407,#69408,#69409));
#14367=EDGE_LOOP('',(#69410,#69411,#69412,#69413));
#14368=EDGE_LOOP('',(#69414,#69415,#69416,#69417));
#14369=EDGE_LOOP('',(#69418,#69419,#69420,#69421));
#14370=EDGE_LOOP('',(#69422,#69423,#69424,#69425));
#14371=EDGE_LOOP('',(#69426,#69427,#69428,#69429));
#14372=EDGE_LOOP('',(#69430,#69431,#69432,#69433));
#14373=EDGE_LOOP('',(#69434,#69435,#69436,#69437));
#14374=EDGE_LOOP('',(#69438,#69439,#69440,#69441));
#14375=EDGE_LOOP('',(#69442,#69443,#69444,#69445));
#14376=EDGE_LOOP('',(#69446,#69447,#69448,#69449));
#14377=EDGE_LOOP('',(#69450,#69451,#69452,#69453));
#14378=EDGE_LOOP('',(#69454,#69455,#69456,#69457));
#14379=EDGE_LOOP('',(#69458,#69459,#69460,#69461));
#14380=EDGE_LOOP('',(#69462,#69463,#69464,#69465));
#14381=EDGE_LOOP('',(#69466,#69467,#69468,#69469));
#14382=EDGE_LOOP('',(#69470,#69471,#69472,#69473));
#14383=EDGE_LOOP('',(#69474,#69475,#69476,#69477));
#14384=EDGE_LOOP('',(#69478,#69479,#69480,#69481));
#14385=EDGE_LOOP('',(#69482,#69483,#69484,#69485));
#14386=EDGE_LOOP('',(#69486,#69487,#69488,#69489));
#14387=EDGE_LOOP('',(#69490,#69491,#69492,#69493));
#14388=EDGE_LOOP('',(#69494,#69495,#69496,#69497));
#14389=EDGE_LOOP('',(#69498,#69499,#69500,#69501));
#14390=EDGE_LOOP('',(#69502,#69503,#69504,#69505));
#14391=EDGE_LOOP('',(#69506,#69507));
#14392=EDGE_LOOP('',(#69508));
#14393=EDGE_LOOP('',(#69509));
#14394=EDGE_LOOP('',(#69510,#69511,#69512,#69513));
#14395=EDGE_LOOP('',(#69514,#69515,#69516,#69517,#69518,#69519,#69520,#69521,
#69522));
#14396=EDGE_LOOP('',(#69523,#69524,#69525,#69526));
#14397=EDGE_LOOP('',(#69527));
#14398=EDGE_LOOP('',(#69528));
#14399=EDGE_LOOP('',(#69529,#69530,#69531,#69532));
#14400=EDGE_LOOP('',(#69533));
#14401=EDGE_LOOP('',(#69534));
#14402=EDGE_LOOP('',(#69535));
#14403=EDGE_LOOP('',(#69536,#69537,#69538,#69539,#69540,#69541));
#14404=EDGE_LOOP('',(#69542,#69543));
#14405=EDGE_LOOP('',(#69544,#69545));
#14406=EDGE_LOOP('',(#69546,#69547));
#14407=EDGE_LOOP('',(#69548,#69549));
#14408=EDGE_LOOP('',(#69550,#69551));
#14409=EDGE_LOOP('',(#69552,#69553,#69554,#69555,#69556,#69557));
#14410=EDGE_LOOP('',(#69558,#69559,#69560,#69561));
#14411=EDGE_LOOP('',(#69562,#69563,#69564,#69565));
#14412=EDGE_LOOP('',(#69566,#69567,#69568,#69569));
#14413=EDGE_LOOP('',(#69570,#69571,#69572,#69573));
#14414=EDGE_LOOP('',(#69574,#69575,#69576,#69577));
#14415=EDGE_LOOP('',(#69578,#69579,#69580,#69581));
#14416=EDGE_LOOP('',(#69582,#69583,#69584,#69585,#69586,#69587,#69588,#69589,
#69590,#69591,#69592,#69593,#69594,#69595,#69596,#69597,#69598,#69599,#69600,
#69601,#69602,#69603,#69604,#69605,#69606,#69607,#69608,#69609,#69610,#69611,
#69612,#69613,#69614,#69615,#69616));
#14417=EDGE_LOOP('',(#69617,#69618,#69619,#69620));
#14418=EDGE_LOOP('',(#69621,#69622,#69623,#69624,#69625,#69626,#69627,#69628,
#69629,#69630,#69631,#69632,#69633,#69634,#69635,#69636,#69637,#69638,#69639,
#69640,#69641,#69642,#69643,#69644,#69645,#69646,#69647,#69648,#69649,#69650,
#69651,#69652,#69653,#69654,#69655));
#20574=CIRCLE('',#99250,1.17524047358089);
#20575=CIRCLE('',#99252,1.17524047358089);
#20576=CIRCLE('',#99268,1.5);
#20577=CIRCLE('',#99284,1.15470053837925);
#20578=CIRCLE('',#99286,2.75);
#20579=CIRCLE('',#99287,1.5);
#20580=CIRCLE('',#99289,3.5);
#20581=CIRCLE('',#99290,3.5);
#20582=CIRCLE('',#99292,1.5);
#20583=CIRCLE('',#99293,1.125);
#20584=CIRCLE('',#99297,1.17524047358083);
#20585=CIRCLE('',#99300,1.15470053837925);
#20586=CIRCLE('',#99301,1.15470053837925);
#20587=CIRCLE('',#99302,1.15470053837925);
#20588=CIRCLE('',#99303,1.15470053837925);
#20589=CIRCLE('',#99304,1.15470053837925);
#24637=B_SPLINE_CURVE_WITH_KNOTS('',3,(#366792,#366793,#366794,#366795,
#366796,#366797,#366798,#366799,#366800,#366801,#366802,#366803,#366804,
#366805,#366806,#366807,#366808,#366809,#366810,#366811),.UNSPECIFIED.,
 .F.,.F.,(4,2,2,2,2,2,2,2,2,4),(-0.472935221504104,-0.468281727374519,-0.40861909809339,
-0.350099286965046,-0.292852212802115,-0.232709468647884,-0.174861617189299,
-0.116285936215957,-0.057358849632408,-1.00000015934576E-6),
 .UNSPECIFIED.);
#24638=B_SPLINE_CURVE_WITH_KNOTS('',3,(#366814,#366815,#366816,#366817,
#366818,#366819,#366820,#366821,#366822,#366823,#366824,#366825,#366826,
#366827,#366828,#366829),.UNSPECIFIED.,.F.,.F.,(4,2,2,2,2,2,2,4),(-14.4244566354324,
-14.3874883625153,-14.3508960651526,-14.2924027349825,-14.2326831946865,
-14.1756382437387,-14.1164979545906,-14.0682546416151),.UNSPECIFIED.);
#24639=B_SPLINE_CURVE_WITH_KNOTS('',3,(#366834,#366835,#366836,#366837,
#366838,#366839,#366840,#366841,#366842,#366843,#366844,#366845,#366846,
#366847,#366848,#366849,#366850,#366851,#366852,#366853,#366854,#366855,
#366856,#366857,#366858,#366859,#366860,#366861,#366862,#366863,#366864,
#366865,#366866,#366867,#366868,#366869),.UNSPECIFIED.,.F.,.F.,(4,2,2,2,
2,2,2,2,2,2,2,2,2,2,2,2,2,4),(-1.4182683932457,-1.40482153675579,-1.34515976227263,
-1.28699062464975,-1.22927287309242,-1.16951868844722,-1.1120201872427,
-1.05243602696549,-0.993461412427311,-0.93650728968302,-0.876859278600447,
-0.818532079283255,-0.761095127096905,-0.701163911011217,-0.643506626123397,
-0.584472913219241,-0.525307825223644,-0.472935221504104),.UNSPECIFIED.);
#24640=B_SPLINE_CURVE_WITH_KNOTS('',3,(#366870,#366871,#366872,#366873,
#366874,#366875,#366876,#366877,#366878,#366879,#366880,#366881,#366882,
#366883,#366884,#366885,#366886,#366887,#366888,#366889,#366890,#366891,
#366892,#366893,#366894,#366895,#366896,#366897,#366898,#366899,#366900,
#366901,#366902,#366903,#366904,#366905),.UNSPECIFIED.,.F.,.F.,(4,2,2,2,
2,2,2,2,2,2,2,2,2,2,2,2,2,4),(-14.0682546416151,-14.0571544660327,-13.9995094275063,
-13.9395966573438,-13.8819763204238,-13.8236606522955,-13.7639424951785,
-13.7069245007115,-13.6479596977281,-13.5880326674721,-13.5305303753149,
-13.4707771853322,-13.4128404091712,-13.3546653789508,-13.2949209937328,
-13.2378385489244,-13.1790120528285,-13.1217523389391),.UNSPECIFIED.);
#24641=B_SPLINE_CURVE_WITH_KNOTS('',3,(#366910,#366911,#366912,#366913,
#366914,#366915,#366916,#366917,#366918,#366919,#366920,#366921,#366922,
#366923,#366924,#366925,#366926,#366927,#366928,#366929,#366930,#366931,
#366932,#366933,#366934,#366935,#366936,#366937,#366938,#366939,#366940,
#366941,#366942,#366943,#366944,#366945),.UNSPECIFIED.,.F.,.F.,(4,2,2,2,
2,2,2,2,2,2,2,2,2,2,2,2,2,4),(-2.36378944550582,-2.34137896891538,-2.2812945893873,
-2.22350291328147,-2.16498583386054,-2.10565909540148,-2.04851852095586,
-1.98886851842519,-1.9301835034246,-1.87308085031929,-1.81337506824985,
-1.75534263888906,-1.69722393727412,-1.63762800227697,-1.58027065314222,
-1.52061845232211,-1.46179970044729,-1.4182683932457),.UNSPECIFIED.);
#24642=B_SPLINE_CURVE_WITH_KNOTS('',3,(#366946,#366947,#366948,#366949,
#366950,#366951,#366952,#366953,#366954,#366955,#366956,#366957,#366958,
#366959,#366960,#366961,#366962,#366963,#366964,#366965,#366966,#366967,
#366968,#366969,#366970,#366971,#366972,#366973,#366974,#366975,#366976,
#366977,#366978,#366979,#366980,#366981,#366982,#366983),.UNSPECIFIED.,
 .F.,.F.,(4,2,2,2,2,2,2,2,2,2,2,2,2,2,2,2,2,2,4),(-13.1217523389391,-13.119283714129,
-13.0619141558394,-13.0023102136998,-12.943917103158,-12.8858683733419,
-12.8255073497059,-12.7682721708645,-12.7095482508193,-12.6497981540076,
-12.5926117849825,-12.5332438298209,-12.4744661438345,-12.4166269551953,
-12.3564978650863,-12.2991396139021,-12.240628743601,-12.1809136964986,
-12.1747564163304),.UNSPECIFIED.);
#24643=B_SPLINE_CURVE_WITH_KNOTS('',3,(#366988,#366989,#366990,#366991,
#366992,#366993,#366994,#366995,#366996,#366997,#366998,#366999,#367000,
#367001,#367002,#367003,#367004,#367005,#367006,#367007,#367008,#367009,
#367010,#367011,#367012,#367013,#367014,#367015,#367016,#367017,#367018,
#367019,#367020,#367021,#367022,#367023),.UNSPECIFIED.,.F.,.F.,(4,2,2,2,
2,2,2,2,2,2,2,2,2,2,2,2,2,4),(-3.30827342425045,-3.27687972744449,-3.21718384712782,
-3.15974147950733,-3.10021755192438,-3.04130042987265,-2.98440223902953,
-2.92481287203565,-2.86654252262006,-2.8091627094274,-2.74928986692013,
-2.69168877540808,-2.63271453390828,-2.57360703640158,-2.51663665270488,
-2.45703247238319,-2.39856948678001,-2.36378944550582),.UNSPECIFIED.);
#24644=B_SPLINE_CURVE_WITH_KNOTS('',3,(#367024,#367025,#367026,#367027,
#367028,#367029,#367030,#367031,#367032,#367033,#367034,#367035,#367036,
#367037,#367038,#367039,#367040,#367041,#367042,#367043,#367044,#367045,
#367046,#367047,#367048,#367049,#367050,#367051,#367052,#367053,#367054,
#367055,#367056,#367057,#367058,#367059),.UNSPECIFIED.,.F.,.F.,(4,2,2,2,
2,2,2,2,2,2,2,2,2,2,2,2,2,4),(-12.1747564163304,-12.1238650424603,-12.064707563846,
-12.0054373680747,-11.9477788345207,-11.8878505439664,-11.8302701344871,
-11.771941095994,-11.7122309526739,-11.6552211790534,-11.5962433434009,
-11.536397643427,-11.4788862588776,-11.4191223407857,-11.361234396967,-11.3030507704824,
-11.2433176900185,-11.2284495394774),.UNSPECIFIED.);
#24645=B_SPLINE_CURVE_WITH_KNOTS('',3,(#367064,#367065,#367066,#367067,
#367068,#367069,#367070,#367071,#367072,#367073,#367074,#367075,#367076,
#367077,#367078,#367079,#367080,#367081,#367082,#367083,#367084,#367085,
#367086,#367087,#367088,#367089,#367090,#367091,#367092,#367093,#367094,
#367095,#367096,#367097,#367098,#367099),.UNSPECIFIED.,.F.,.F.,(4,2,2,2,
2,2,2,2,2,2,2,2,2,2,2,2,2,4),(-4.25326910634686,-4.21251454639597,-4.15309289586531,
-4.09589408206557,-4.03627301194829,-3.97762776411373,-3.92059880643218,
-3.86095544391126,-3.80296175193752,-3.74495194469459,-3.68539344318783,
-3.62807342906873,-3.56793846932016,-3.50917716188511,-3.45225521027217,
-3.3926521707181,-3.33453983230326,-3.30827342425045),.UNSPECIFIED.);
#24646=B_SPLINE_CURVE_WITH_KNOTS('',3,(#367100,#367101,#367102,#367103,
#367104,#367105,#367106,#367107,#367108,#367109,#367110,#367111,#367112,
#367113,#367114,#367115,#367116,#367117,#367118,#367119,#367120,#367121,
#367122,#367123,#367124,#367125,#367126,#367127,#367128,#367129,#367130,
#367131,#367132,#367133,#367134,#367135),.UNSPECIFIED.,.F.,.F.,(4,2,2,2,
2,2,2,2,2,2,2,2,2,2,2,2,2,4),(-11.2284495394774,-11.1862539313897,-11.1274192209345,
-11.0677005448575,-11.0103242661127,-10.9507121374681,-10.8923823346891,
-10.8343279213107,-10.7739591575687,-10.7167546877142,-10.6580247804181,
-10.5982913927564,-10.5411030669475,-10.4817297521307,-10.4230303926228,
-10.3651887976557,-10.3050554630025,-10.2816571097042),.UNSPECIFIED.);
#24647=B_SPLINE_CURVE_WITH_KNOTS('',3,(#367140,#367141,#367142,#367143,
#367144,#367145,#367146,#367147,#367148,#367149,#367150,#367151,#367152,
#367153,#367154,#367155,#367156,#367157,#367158,#367159,#367160,#367161,
#367162,#367163,#367164,#367165,#367166,#367167,#367168,#367169,#367170,
#367171,#367172,#367173,#367174,#367175),.UNSPECIFIED.,.F.,.F.,(4,2,2,2,
2,2,2,2,2,2,2,2,2,2,2,2,2,4),(-5.19889150766547,-5.14881365823251,-5.08980980299638,
-5.03284693005632,-4.97319371313394,-4.91483702785059,-4.85742729771692,
-4.7974638444269,-4.73977725885472,-4.68080804808204,-4.62160937476519,
-4.56456081276647,-4.50488872766924,-4.44633491517977,-4.38910134791393,
-4.32892185865653,-4.2710405265478,-4.25326910634686),.UNSPECIFIED.);
#24648=B_SPLINE_CURVE_WITH_KNOTS('',3,(#367176,#367177,#367178,#367179,
#367180,#367181,#367182,#367183,#367184,#367185,#367186,#367187,#367188,
#367189,#367190,#367191,#367192,#367193,#367194,#367195,#367196,#367197,
#367198,#367199,#367200,#367201,#367202,#367203,#367204,#367205,#367206,
#367207,#367208,#367209,#367210,#367211),.UNSPECIFIED.,.F.,.F.,(4,2,2,2,
2,2,2,2,2,2,2,2,2,2,2,2,2,4),(-10.2816571097042,-10.2477410641564,-10.1892277178352,
-10.1295333942322,-10.0724951191448,-10.0133357139472,-9.95415661279037,
-9.8964995248753,-9.83657116169116,-9.77904666811989,-9.72071934329227,
-9.66103360979029,-9.60404666701626,-9.54507107346665,-9.48532550181212,
-9.42782001815589,-9.36806087538511,-9.33568992122532),.UNSPECIFIED.);
#24649=B_SPLINE_CURVE_WITH_KNOTS('',3,(#367216,#367217,#367218,#367219,
#367220,#367221,#367222,#367223,#367224,#367225,#367226,#367227,#367228,
#367229,#367230,#367231,#367232,#367233,#367234,#367235,#367236,#367237,
#367238,#367239,#367240,#367241,#367242,#367243,#367244,#367245,#367246,
#367247,#367248,#367249,#367250,#367251),.UNSPECIFIED.,.F.,.F.,(4,2,2,2,
2,2,2,2,2,2,2,2,2,2,2,2,2,4),(-6.14456421576452,-6.08570958308235,-6.02698853788712,
-5.9699174554043,-5.91021744604823,-5.85214826557745,-5.79412704547714,
-5.73448887961226,-5.67709342547849,-5.61697940243931,-5.55813653734526,
-5.50116233608994,-5.44149916775544,-5.3833056527042,-5.32562667315605,
-5.26584536369006,-5.20832226100928,-5.19889150766547),.UNSPECIFIED.);
#24650=B_SPLINE_CURVE_WITH_KNOTS('',3,(#367252,#367253,#367254,#367255,
#367256,#367257,#367258,#367259,#367260,#367261,#367262,#367263,#367264,
#367265,#367266,#367267,#367268,#367269,#367270,#367271,#367272,#367273,
#367274,#367275,#367276,#367277,#367278,#367279,#367280,#367281,#367282,
#367283,#367284,#367285,#367286,#367287),.UNSPECIFIED.,.F.,.F.,(4,2,2,2,
2,2,2,2,2,2,2,2,2,2,2,2,2,4),(-9.33568992122532,-9.31068519693683,-9.25063120253579,
-9.19286127678687,-9.1340053853449,-9.07471389558202,-9.01759257466977,
-8.95787936125444,-8.89923227045455,-8.84200302383332,-8.78172385728799,
-8.72375069837283,-8.66530546515211,-8.60578351513382,-8.54849080424378,
-8.48881207353315,-8.43006692171669,-8.3892918312322),.UNSPECIFIED.);
#24651=B_SPLINE_CURVE_WITH_KNOTS('',3,(#367292,#367293,#367294,#367295,
#367296,#367297,#367298,#367299,#367300,#367301,#367302,#367303,#367304,
#367305,#367306,#367307,#367308,#367309,#367310,#367311,#367312,#367313,
#367314,#367315,#367316,#367317,#367318,#367319,#367320,#367321,#367322,
#367323,#367324,#367325,#367326,#367327,#367328,#367329),.UNSPECIFIED.,
 .F.,.F.,(4,2,2,2,2,2,2,2,2,2,2,2,2,2,2,2,2,2,4),(-7.09111164764165,-7.08318036416534,
-7.02348003126206,-6.96505465777705,-6.90762820237831,-6.84759239829551,
-6.7898378115135,-6.73088509922959,-6.67161346650712,-6.6145025289804,-6.55477946680844,
-6.49615286724619,-6.43888999233079,-6.37863405000312,-6.32068091409213,
-6.26215787945088,-6.20265987977463,-6.14538870527694,-6.14456421576452),
 .UNSPECIFIED.);
#24652=B_SPLINE_CURVE_WITH_KNOTS('',3,(#367330,#367331,#367332,#367333,
#367334,#367335,#367336,#367337,#367338,#367339,#367340,#367341,#367342,
#367343,#367344,#367345,#367346,#367347,#367348,#367349,#367350,#367351,
#367352,#367353,#367354,#367355,#367356,#367357,#367358,#367359,#367360,
#367361,#367362,#367363,#367364,#367365),.UNSPECIFIED.,.F.,.F.,(4,2,2,2,
2,2,2,2,2,2,2,2,2,2,2,2,2,4),(-8.3892918312322,-8.37301252043267,-8.31331490309094,
-8.2552211998388,-8.19725815925277,-8.13759205793883,-8.08017135706559,
-8.02016045184272,-7.96128628900145,-7.90431503125115,-7.84464966750369,
-7.78642452640327,-7.72879292598016,-7.66897651712038,-7.6114215848653,
-7.55200710016729,-7.49296560778789,-7.44370351434638),.UNSPECIFIED.);
#24653=B_SPLINE_CURVE_WITH_KNOTS('',3,(#367370,#367371,#367372,#367373,
#367374,#367375,#367376,#367377,#367378,#367379,#367380,#367381,#367382,
#367383,#367384,#367385,#367386,#367387,#367388,#367389,#367390,#367391,
#367392,#367393,#367394,#367395,#367396,#367397,#367398,#367399,#367400,
#367401,#367402,#367403,#367404,#367405),.UNSPECIFIED.,.F.,.F.,(4,2,2,2,
2,2,2,2,2,2,2,2,2,2,2,2,2,4),(-8.03735473147222,-8.02087464960411,-7.9611343773927,
-7.9030065244771,-7.84498694102494,-7.78528651218867,-7.72783232454958,
-7.66775115919979,-7.60884413001691,-7.55183217733595,-7.49212543402685,
-7.43386797250469,-7.37618308062694,-7.31633417516343,-7.25874744107932,
-7.19926567335177,-7.14019290496742,-7.09111164764165),.UNSPECIFIED.);
#24654=B_SPLINE_CURVE_WITH_KNOTS('',3,(#367406,#367407,#367408,#367409,
#367410,#367411,#367412,#367413,#367414,#367415,#367416,#367417,#367418,
#367419,#367420,#367421,#367422,#367423,#367424,#367425,#367426,#367427,
#367428,#367429,#367430,#367431,#367432,#367433,#367434,#367435,#367436,
#367437,#367438,#367439,#367440,#367441,#367442,#367443),.UNSPECIFIED.,
 .F.,.F.,(4,2,2,2,2,2,2,2,2,2,2,2,2,2,2,2,2,2,4),(-7.44370351434638,-7.43598926663215,
-7.37632897618584,-7.31793433550879,-7.26055680051354,-7.20055191970967,
-7.14282768443292,-7.0839377587198,-7.02469610678344,-6.96761672070063,
-6.9079322695684,-6.84933508841591,-6.79211623975549,-6.73188992322172,
-6.67396592905681,-6.61550012837161,-6.55603108184469,-6.49878820169375,
-6.49776578706861),.UNSPECIFIED.);
#24655=B_SPLINE_CURVE_WITH_KNOTS('',3,(#367448,#367449,#367450,#367451,
#367452,#367453,#367454,#367455,#367456,#367457,#367458,#367459,#367460,
#367461,#367462,#367463,#367464,#367465,#367466,#367467,#367468,#367469,
#367470,#367471,#367472,#367473,#367474,#367475,#367476,#367477,#367478,
#367479,#367480,#367481,#367482,#367483),.UNSPECIFIED.,.F.,.F.,(4,2,2,2,
2,2,2,2,2,2,2,2,2,2,2,2,2,4),(-8.98445161616762,-8.95921638570029,-8.89912516429285,
-8.8413188294932,-8.7823951007912,-8.72306736360276,-8.6659089173167,-8.60615099812978,
-8.54746829055918,-8.49018974871482,-8.42987456712495,-8.37186613263263,
-8.31335863269924,-8.2538013865138,-8.19647428240418,-8.13675347140136,
-8.07797359942355,-8.03735473147222),.UNSPECIFIED.);
#24656=B_SPLINE_CURVE_WITH_KNOTS('',3,(#367484,#367485,#367486,#367487,
#367488,#367489,#367490,#367491,#367492,#367493,#367494,#367495,#367496,
#367497,#367498,#367499,#367500,#367501,#367502,#367503,#367504,#367505,
#367506,#367507,#367508,#367509,#367510,#367511,#367512,#367513,#367514,
#367515,#367516,#367517,#367518,#367519),.UNSPECIFIED.,.F.,.F.,(4,2,2,2,
2,2,2,2,2,2,2,2,2,2,2,2,2,4),(-6.49776578706861,-6.43914500581034,-6.38045238997202,
-6.3234204168521,-6.26375689717225,-6.20571563565091,-6.14774582037313,
-6.08813554490324,-6.03076739211196,-5.97071874702609,-5.91190232887527,
-5.85496333454488,-5.79533533481046,-5.73716778380854,-5.67953701682865,
-5.61978163527879,-5.56228402810339,-5.55265580416904),.UNSPECIFIED.);
#24657=B_SPLINE_CURVE_WITH_KNOTS('',3,(#367524,#367525,#367526,#367527,
#367528,#367529,#367530,#367531,#367532,#367533,#367534,#367535,#367536,
#367537,#367538,#367539,#367540,#367541,#367542,#367543,#367544,#367545,
#367546,#367547,#367548,#367549,#367550,#367551,#367552,#367553,#367554,
#367555,#367556,#367557,#367558,#367559),.UNSPECIFIED.,.F.,.F.,(4,2,2,2,
2,2,2,2,2,2,2,2,2,2,2,2,2,4),(-9.93112270433081,-9.89704456919083,-9.83848209313174,
-9.77874344022364,-9.72166028386723,-9.66245135212457,-9.60324573067881,
-9.54554119238533,-9.48556311336624,-9.42800470870366,-9.36810484432635,
-9.31047046348868,-9.25102823330278,-9.19190312444107,-9.13485529115929,
-9.07512386137383,-9.01664620276166,-8.98445161616762),.UNSPECIFIED.);
#24658=B_SPLINE_CURVE_WITH_KNOTS('',3,(#367560,#367561,#367562,#367563,
#367564,#367565,#367566,#367567,#367568,#367569,#367570,#367571,#367572,
#367573,#367574,#367575,#367576,#367577,#367578,#367579,#367580,#367581,
#367582,#367583,#367584,#367585,#367586,#367587,#367588,#367589,#367590,
#367591,#367592,#367593,#367594,#367595),.UNSPECIFIED.,.F.,.F.,(4,2,2,2,
2,2,2,2,2,2,2,2,2,2,2,2,2,4),(-5.55265580416904,-5.50283799464443,-5.44385886442445,
-5.38692656343666,-5.3273071294198,-5.26897469201179,-5.21160876172262,
-5.15166953125696,-5.09400687100007,-5.0350957859107,-4.97592041893457,
-4.91889754803401,-4.85925776188592,-4.80072676094053,-4.74353195103695,
-4.68337526350125,-4.62551653539798,-4.60754988443217),.UNSPECIFIED.);
#24659=B_SPLINE_CURVE_WITH_KNOTS('',3,(#367600,#367601,#367602,#367603,
#367604,#367605,#367606,#367607,#367608,#367609,#367610,#367611,#367612,
#367613,#367614,#367615,#367616,#367617,#367618,#367619,#367620,#367621,
#367622,#367623,#367624,#367625,#367626,#367627,#367628,#367629,#367630,
#367631,#367632,#367633,#367634,#367635),.UNSPECIFIED.,.F.,.F.,(4,2,2,2,
2,2,2,2,2,2,2,2,2,2,2,2,2,4),(-10.8786408780219,-10.8362900188463,-10.7774045193324,
-10.7176387373802,-10.6602132403304,-10.6005496747681,-10.5421870475221,
-10.4840831015066,-10.4236623739244,-10.3664179393046,-10.3076378611891,
-10.2478591049355,-10.1906227194181,-10.1311988593382,-10.072470136304,
-10.0145799907407,-9.95439574519051,-9.93112270433081),.UNSPECIFIED.);
#24660=B_SPLINE_CURVE_WITH_KNOTS('',3,(#367636,#367637,#367638,#367639,
#367640,#367641,#367642,#367643,#367644,#367645,#367646,#367647,#367648,
#367649,#367650,#367651,#367652,#367653,#367654,#367655,#367656,#367657,
#367658,#367659,#367660,#367661,#367662,#367663,#367664,#367665,#367666,
#367667,#367668,#367669,#367670,#367671),.UNSPECIFIED.,.F.,.F.,(4,2,2,2,
2,2,2,2,2,2,2,2,2,2,2,2,2,4),(-4.60754988443217,-4.56704304466917,-4.507643564291,
-4.45046653171621,-4.39087495730951,-4.33225140646798,-4.275256004067,-4.2156426957743,
-4.15767024985269,-4.0997068740148,-4.04016935074741,-3.98287000564575,
-3.9227960098371,-3.86405423063106,-3.80716180627627,-3.74758742087661,
-3.68949419100672,-3.66302281083744),.UNSPECIFIED.);
#24661=B_SPLINE_CURVE_WITH_KNOTS('',3,(#367676,#367677,#367678,#367679,
#367680,#367681,#367682,#367683,#367684,#367685,#367686,#367687,#367688,
#367689,#367690,#367691,#367692,#367693,#367694,#367695,#367696,#367697,
#367698,#367699,#367700,#367701,#367702,#367703,#367704,#367705,#367706,
#367707,#367708,#367709,#367710,#367711),.UNSPECIFIED.,.F.,.F.,(4,2,2,2,
2,2,2,2,2,2,2,2,2,2,2,2,2,4),(-11.8257014074602,-11.7746324045687,-11.7154216905502,
-11.6561202632027,-11.5984106352401,-11.5384288683135,-11.4808104074964,
-11.4224297436371,-11.3626721032327,-11.3056169669095,-11.246587051771,
-11.1867116959658,-11.1291504097255,-11.0693343169958,-11.011410332405,
-10.9531763630212,-10.8933965781418,-10.8786408780219),.UNSPECIFIED.);
#24662=B_SPLINE_CURVE_WITH_KNOTS('',3,(#367712,#367713,#367714,#367715,
#367716,#367717,#367718,#367719,#367720,#367721,#367722,#367723,#367724,
#367725,#367726,#367727,#367728,#367729,#367730,#367731,#367732,#367733,
#367734,#367735,#367736,#367737,#367738,#367739,#367740,#367741,#367742,
#367743,#367744,#367745,#367746,#367747),.UNSPECIFIED.,.F.,.F.,(4,2,2,2,
2,2,2,2,2,2,2,2,2,2,2,2,2,4),(-3.66302281083744,-3.63187733807794,-3.57220028358447,
-3.51477660438808,-3.45531097923445,-3.39641147727633,-3.33953793696864,
-3.27997575463458,-3.22172261505027,-3.1643815174916,-3.10452560936109,
-3.04694146598837,-2.9880210703399,-2.9289296021329,-2.87197863419305,-2.81240006452607,
-2.75395268194537,-2.7189587610551),.UNSPECIFIED.);
#24663=B_SPLINE_CURVE_WITH_KNOTS('',3,(#367752,#367753,#367754,#367755,
#367756,#367757,#367758,#367759,#367760,#367761,#367762,#367763,#367764,
#367765,#367766,#367767,#367768,#367769,#367770,#367771,#367772,#367773,
#367774,#367775,#367776,#367777,#367778,#367779,#367780,#367781,#367782,
#367783,#367784,#367785,#367786,#367787,#367788,#367789),.UNSPECIFIED.,
 .F.,.F.,(4,2,2,2,2,2,2,2,2,2,2,2,2,2,2,2,2,2,4),(-12.7734810909064,-12.7708880798203,
-12.7134657322968,-12.6538066602905,-12.5953765749201,-12.5372747014855,
-12.4768579845627,-12.4195791202852,-12.360801383851,-12.3010019386788,
-12.2437641789621,-12.1843419798448,-12.1255305150722,-12.0676391518563,
-12.0074554104525,-11.9500564718063,-11.89149281404,-11.831729396117,-11.8257014074602),
 .UNSPECIFIED.);
#24664=B_SPLINE_CURVE_WITH_KNOTS('',3,(#367790,#367791,#367792,#367793,
#367794,#367795,#367796,#367797,#367798,#367799,#367800,#367801,#367802,
#367803,#367804,#367805,#367806,#367807,#367808,#367809,#367810,#367811,
#367812,#367813,#367814,#367815,#367816,#367817,#367818,#367819,#367820,
#367821,#367822,#367823,#367824,#367825),.UNSPECIFIED.,.F.,.F.,(4,2,2,2,
2,2,2,2,2,2,2,2,2,2,2,2,2,4),(-2.7189587610551,-2.69679557934989,-2.63672654084043,
-2.57895033520473,-2.52048127345029,-2.46116927811905,-2.40404315464007,
-2.34441705383858,-2.28574632003949,-2.22867155763538,-2.16898900265649,
-2.11097046107922,-2.05289358459059,-1.99331097554254,-1.93596696793388,
-1.87574108507994,-1.81695797180762,-1.77380203185272),.UNSPECIFIED.);
#24665=B_SPLINE_CURVE_WITH_KNOTS('',3,(#367830,#367831,#367832,#367833,
#367834,#367835,#367836,#367837,#367838,#367839,#367840,#367841,#367842,
#367843,#367844,#367845,#367846,#367847,#367848,#367849,#367850,#367851,
#367852,#367853,#367854,#367855,#367856,#367857,#367858,#367859,#367860,
#367861,#367862,#367863,#367864,#367865),.UNSPECIFIED.,.F.,.F.,(4,2,2,2,
2,2,2,2,2,2,2,2,2,2,2,2,2,4),(-13.7207949142504,-13.7095635100018,-13.6518638060279,
-13.5918938652479,-13.5342317348891,-13.4758608361514,-13.4160912900698,
-13.3590244568557,-13.3000039242801,-13.2400428544059,-13.1824870816294,
-13.1226780144681,-13.0647012309748,-13.0064722417789,-12.9466772279908,
-12.8895483636782,-12.8306674186845,-12.7734810909064),.UNSPECIFIED.);
#24666=B_SPLINE_CURVE_WITH_KNOTS('',3,(#367866,#367867,#367868,#367869,
#367870,#367871,#367872,#367873,#367874,#367875,#367876,#367877,#367878,
#367879,#367880,#367881,#367882,#367883,#367884,#367885,#367886,#367887,
#367888,#367889,#367890,#367891,#367892,#367893,#367894,#367895,#367896,
#367897,#367898,#367899,#367900,#367901),.UNSPECIFIED.,.F.,.F.,(4,2,2,2,
2,2,2,2,2,2,2,2,2,2,2,2,2,4),(-1.77380203185272,-1.75999682284082,-1.70035692226662,
-1.64222336071123,-1.58450128192949,-1.52478495274704,-1.46732195812214,
-1.4077112263667,-1.34877556108029,-1.29184626088159,-1.23222248252541,
-1.17393415405485,-1.11649978042292,-1.05660972626645,-0.998990984886199,
-0.939937104231028,-0.880813803640254,-0.828855918263461),.UNSPECIFIED.);
#24667=B_SPLINE_CURVE_WITH_KNOTS('',3,(#367922,#367923,#367924,#367925,
#367926,#367927,#367928,#367929,#367930,#367931,#367932,#367933),
 .UNSPECIFIED.,.F.,.F.,(4,2,2,2,2,4),(-0.17346262697256,-0.144399563151948,
-0.113776683209733,-0.0827144356874581,-0.0458811973302938,-9.99999999945489E-7),
 .UNSPECIFIED.);
#24668=B_SPLINE_CURVE_WITH_KNOTS('',3,(#367937,#367938,#367939,#367940,
#367941,#367942,#367943,#367944,#367945,#367946,#367947,#367948,#367949,
#367950,#367951,#367952,#367953,#367954,#367955,#367956,#367957,#367958,
#367959,#367960,#367961,#367962),.UNSPECIFIED.,.F.,.F.,(4,2,2,2,2,2,2,2,
2,2,2,2,4),(-1.02018564821439,-0.975662064295862,-0.931763813839812,-0.852134429154344,
-0.755247005225842,-0.6619508555074,-0.580085930087374,-0.508496324409023,
-0.441275520650989,-0.407325938090968,-0.339348399346137,-0.274302988628325,
-0.24661014220574),.UNSPECIFIED.);
#24669=B_SPLINE_CURVE_WITH_KNOTS('',3,(#367966,#367967,#367968,#367969,
#367970,#367971,#367972,#367973,#367974,#367975,#367976,#367977,#367978,
#367979,#367980,#367981),.UNSPECIFIED.,.F.,.F.,(4,2,2,2,2,2,2,4),(-0.24661014220574,
-0.2267185418882,-0.192167788882823,-0.155378136435479,-0.119884038074694,
-0.0860669040899276,-0.0458325307501637,0.),.UNSPECIFIED.);
#24670=B_SPLINE_CURVE_WITH_KNOTS('',3,(#367983,#367984,#367985,#367986,
#367987,#367988,#367989,#367990,#367991,#367992,#367993,#367994,#367995,
#367996,#367997,#367998,#367999,#368000,#368001,#368002,#368003,#368004,
#368005,#368006,#368007,#368008,#368009,#368010,#368011,#368012,#368013,
#368014,#368015,#368016),.UNSPECIFIED.,.F.,.F.,(4,2,2,2,2,2,2,2,2,2,2,2,
2,2,2,2,4),(-0.828855918263461,-0.823821086481886,-0.76418512040139,-0.705706920149708,
-0.648470618047626,-0.588371772381769,-0.530564989186055,-0.471977820133801,
-0.412637508461358,-0.355483018030889,-0.295804085119263,-0.237106144384037,
-0.179966956442961,-0.119629528710579,-0.0616069572388075,-0.031150014909439,
0.),.UNSPECIFIED.);
#24671=B_SPLINE_CURVE_WITH_KNOTS('',3,(#368017,#368018,#368019,#368020,
#368021,#368022,#368023,#368024,#368025,#368026,#368027,#368028,#368029,
#368030,#368031,#368032,#368033,#368034,#368035,#368036,#368037,#368038,
#368039,#368040,#368041,#368042,#368043,#368044),.UNSPECIFIED.,.F.,.F.,
(4,2,2,2,2,2,2,2,2,2,2,2,2,4),(-14.4312618797178,-14.3922640324926,-14.3545407029447,
-14.2973154490866,-14.2379103131024,-14.1790334897097,-14.1211559666463,
-14.0609882938093,-14.0035573096291,-13.9450076696767,-13.8852359857398,
-13.8281394143352,-13.7689423216674,-13.7207949142504),.UNSPECIFIED.);
#24672=B_SPLINE_CURVE_WITH_KNOTS('',3,(#368048,#368049,#368050,#368051,
#368052,#368053,#368054,#368055,#368056,#368057,#368058,#368059,#368060,
#368061,#368062,#368063,#368064,#368065),.UNSPECIFIED.,.F.,.F.,(4,2,2,2,
2,2,2,2,4),(0.,0.0314990983415605,0.0537157834318906,0.0796765738993867,
0.104184920565216,0.128404183892005,0.152339319821176,0.164876349211554,
0.178501629664245),.UNSPECIFIED.);
#24673=B_SPLINE_CURVE_WITH_KNOTS('',3,(#368068,#368069,#368070,#368071,
#368072,#368073,#368074,#368075,#368076,#368077,#368078,#368079,#368080,
#368081,#368082,#368083),.UNSPECIFIED.,.F.,.F.,(4,2,2,2,2,2,2,4),(0.,0.049039335524975,
0.0900736384682671,0.132971048637076,0.166666317630351,0.191811791938321,
0.208306699924898,0.225483082815066),.UNSPECIFIED.);
#28989=LINE('',#366329,#32791);
#28990=LINE('',#366338,#32792);
#28991=LINE('',#366370,#32793);
#28992=LINE('',#366400,#32794);
#28993=LINE('',#366430,#32795);
#28994=LINE('',#366460,#32796);
#28995=LINE('',#366490,#32797);
#28996=LINE('',#366520,#32798);
#28997=LINE('',#366550,#32799);
#28998=LINE('',#366580,#32800);
#28999=LINE('',#366610,#32801);
#29000=LINE('',#366640,#32802);
#29001=LINE('',#366670,#32803);
#29002=LINE('',#366700,#32804);
#29003=LINE('',#366730,#32805);
#29004=LINE('',#366760,#32806);
#29005=LINE('',#366790,#32807);
#29006=LINE('',#366833,#32808);
#29007=LINE('',#366909,#32809);
#29008=LINE('',#366987,#32810);
#29009=LINE('',#367063,#32811);
#29010=LINE('',#367139,#32812);
#29011=LINE('',#367215,#32813);
#29012=LINE('',#367291,#32814);
#29013=LINE('',#367369,#32815);
#29014=LINE('',#367447,#32816);
#29015=LINE('',#367523,#32817);
#29016=LINE('',#367599,#32818);
#29017=LINE('',#367675,#32819);
#29018=LINE('',#367751,#32820);
#29019=LINE('',#367829,#32821);
#29020=LINE('',#367918,#32822);
#29021=LINE('',#367964,#32823);
#29022=LINE('',#368118,#32824);
#29023=LINE('',#368120,#32825);
#29024=LINE('',#368122,#32826);
#29025=LINE('',#368124,#32827);
#29026=LINE('',#368126,#32828);
#29027=LINE('',#368127,#32829);
#29028=LINE('',#368129,#32830);
#29029=LINE('',#368130,#32831);
#29030=LINE('',#368132,#32832);
#29031=LINE('',#368134,#32833);
#29032=LINE('',#368136,#32834);
#29033=LINE('',#368138,#32835);
#32791=VECTOR('',#116209,1.17524047358091);
#32792=VECTOR('',#116214,1.17524047358091);
#32793=VECTOR('',#116219,1.17524047358091);
#32794=VECTOR('',#116222,1.17524047358091);
#32795=VECTOR('',#116225,1.17524047358091);
#32796=VECTOR('',#116228,1.17524047358091);
#32797=VECTOR('',#116231,1.17524047358091);
#32798=VECTOR('',#116234,1.17524047358091);
#32799=VECTOR('',#116237,1.17524047358091);
#32800=VECTOR('',#116240,1.17524047358091);
#32801=VECTOR('',#116243,1.17524047358091);
#32802=VECTOR('',#116246,1.17524047358091);
#32803=VECTOR('',#116249,1.17524047358091);
#32804=VECTOR('',#116252,1.17524047358091);
#32805=VECTOR('',#116255,1.17524047358091);
#32806=VECTOR('',#116258,1.17524047358091);
#32807=VECTOR('',#116261,1.5);
#32808=VECTOR('',#116266,1.5);
#32809=VECTOR('',#116269,1.5);
#32810=VECTOR('',#116272,1.5);
#32811=VECTOR('',#116275,1.5);
#32812=VECTOR('',#116278,1.5);
#32813=VECTOR('',#116281,1.5);
#32814=VECTOR('',#116284,1.5);
#32815=VECTOR('',#116287,1.5);
#32816=VECTOR('',#116290,1.5);
#32817=VECTOR('',#116293,1.5);
#32818=VECTOR('',#116296,1.5);
#32819=VECTOR('',#116299,1.5);
#32820=VECTOR('',#116302,1.5);
#32821=VECTOR('',#116305,1.5);
#32822=VECTOR('',#116320,3.5);
#32823=VECTOR('',#116327,1.125);
#32824=VECTOR('',#116364,1000.);
#32825=VECTOR('',#116365,1000.);
#32826=VECTOR('',#116366,1000.);
#32827=VECTOR('',#116367,1000.);
#32828=VECTOR('',#116368,1000.);
#32829=VECTOR('',#116369,1000.);
#32830=VECTOR('',#116372,1000.);
#32831=VECTOR('',#116373,1000.);
#32832=VECTOR('',#116376,1000.);
#32833=VECTOR('',#116379,1000.);
#32834=VECTOR('',#116382,1000.);
#32835=VECTOR('',#116385,1000.);
#38343=VERTEX_POINT('',#366327);
#38344=VERTEX_POINT('',#366328);
#38345=VERTEX_POINT('',#366330);
#38346=VERTEX_POINT('',#366336);
#38347=VERTEX_POINT('',#366337);
#38348=VERTEX_POINT('',#366352);
#38349=VERTEX_POINT('',#366368);
#38350=VERTEX_POINT('',#366369);
#38351=VERTEX_POINT('',#366398);
#38352=VERTEX_POINT('',#366399);
#38353=VERTEX_POINT('',#366428);
#38354=VERTEX_POINT('',#366429);
#38355=VERTEX_POINT('',#366458);
#38356=VERTEX_POINT('',#366459);
#38357=VERTEX_POINT('',#366488);
#38358=VERTEX_POINT('',#366489);
#38359=VERTEX_POINT('',#366518);
#38360=VERTEX_POINT('',#366519);
#38361=VERTEX_POINT('',#366548);
#38362=VERTEX_POINT('',#366549);
#38363=VERTEX_POINT('',#366578);
#38364=VERTEX_POINT('',#366579);
#38365=VERTEX_POINT('',#366608);
#38366=VERTEX_POINT('',#366609);
#38367=VERTEX_POINT('',#366638);
#38368=VERTEX_POINT('',#366639);
#38369=VERTEX_POINT('',#366668);
#38370=VERTEX_POINT('',#366669);
#38371=VERTEX_POINT('',#366698);
#38372=VERTEX_POINT('',#366699);
#38373=VERTEX_POINT('',#366728);
#38374=VERTEX_POINT('',#366729);
#38375=VERTEX_POINT('',#366758);
#38376=VERTEX_POINT('',#366759);
#38377=VERTEX_POINT('',#366788);
#38378=VERTEX_POINT('',#366789);
#38379=VERTEX_POINT('',#366791);
#38380=VERTEX_POINT('',#366812);
#38381=VERTEX_POINT('',#366831);
#38382=VERTEX_POINT('',#366832);
#38383=VERTEX_POINT('',#366907);
#38384=VERTEX_POINT('',#366908);
#38385=VERTEX_POINT('',#366985);
#38386=VERTEX_POINT('',#366986);
#38387=VERTEX_POINT('',#367061);
#38388=VERTEX_POINT('',#367062);
#38389=VERTEX_POINT('',#367137);
#38390=VERTEX_POINT('',#367138);
#38391=VERTEX_POINT('',#367213);
#38392=VERTEX_POINT('',#367214);
#38393=VERTEX_POINT('',#367289);
#38394=VERTEX_POINT('',#367290);
#38395=VERTEX_POINT('',#367367);
#38396=VERTEX_POINT('',#367368);
#38397=VERTEX_POINT('',#367445);
#38398=VERTEX_POINT('',#367446);
#38399=VERTEX_POINT('',#367521);
#38400=VERTEX_POINT('',#367522);
#38401=VERTEX_POINT('',#367597);
#38402=VERTEX_POINT('',#367598);
#38403=VERTEX_POINT('',#367673);
#38404=VERTEX_POINT('',#367674);
#38405=VERTEX_POINT('',#367749);
#38406=VERTEX_POINT('',#367750);
#38407=VERTEX_POINT('',#367827);
#38408=VERTEX_POINT('',#367828);
#38409=VERTEX_POINT('',#367903);
#38410=VERTEX_POINT('',#367904);
#38411=VERTEX_POINT('',#367910);
#38412=VERTEX_POINT('',#367912);
#38413=VERTEX_POINT('',#367915);
#38414=VERTEX_POINT('',#367917);
#38415=VERTEX_POINT('',#367921);
#38416=VERTEX_POINT('',#367934);
#38417=VERTEX_POINT('',#367936);
#38418=VERTEX_POINT('',#367963);
#38419=VERTEX_POINT('',#368047);
#38420=VERTEX_POINT('',#368066);
#38421=VERTEX_POINT('',#368086);
#38422=VERTEX_POINT('',#368087);
#38423=VERTEX_POINT('',#368089);
#38424=VERTEX_POINT('',#368092);
#38425=VERTEX_POINT('',#368116);
#38426=VERTEX_POINT('',#368117);
#38427=VERTEX_POINT('',#368119);
#38428=VERTEX_POINT('',#368121);
#38429=VERTEX_POINT('',#368123);
#38430=VERTEX_POINT('',#368125);
#49193=EDGE_CURVE('',#38343,#38344,#28989,.T.);
#49194=EDGE_CURVE('',#38345,#38343,#4185,.T.);
#49195=EDGE_CURVE('',#38344,#38345,#20574,.T.);
#49196=EDGE_CURVE('',#38346,#38347,#28990,.T.);
#49197=EDGE_CURVE('',#38343,#38346,#4186,.T.);
#49198=EDGE_CURVE('',#38348,#38344,#20575,.T.);
#49199=EDGE_CURVE('',#38348,#38347,#4187,.T.);
#49200=EDGE_CURVE('',#38349,#38350,#28991,.T.);
#49201=EDGE_CURVE('',#38346,#38349,#4188,.T.);
#49202=EDGE_CURVE('',#38347,#38350,#4189,.T.);
#49203=EDGE_CURVE('',#38351,#38352,#28992,.T.);
#49204=EDGE_CURVE('',#38349,#38351,#4190,.T.);
#49205=EDGE_CURVE('',#38350,#38352,#4191,.T.);
#49206=EDGE_CURVE('',#38353,#38354,#28993,.T.);
#49207=EDGE_CURVE('',#38351,#38353,#4192,.T.);
#49208=EDGE_CURVE('',#38352,#38354,#4193,.T.);
#49209=EDGE_CURVE('',#38355,#38356,#28994,.T.);
#49210=EDGE_CURVE('',#38353,#38355,#4194,.T.);
#49211=EDGE_CURVE('',#38354,#38356,#4195,.T.);
#49212=EDGE_CURVE('',#38357,#38358,#28995,.T.);
#49213=EDGE_CURVE('',#38355,#38357,#4196,.T.);
#49214=EDGE_CURVE('',#38356,#38358,#4197,.T.);
#49215=EDGE_CURVE('',#38359,#38360,#28996,.T.);
#49216=EDGE_CURVE('',#38357,#38359,#4198,.T.);
#49217=EDGE_CURVE('',#38358,#38360,#4199,.T.);
#49218=EDGE_CURVE('',#38361,#38362,#28997,.T.);
#49219=EDGE_CURVE('',#38359,#38361,#4200,.T.);
#49220=EDGE_CURVE('',#38360,#38362,#4201,.T.);
#49221=EDGE_CURVE('',#38363,#38364,#28998,.T.);
#49222=EDGE_CURVE('',#38361,#38363,#4202,.T.);
#49223=EDGE_CURVE('',#38362,#38364,#4203,.T.);
#49224=EDGE_CURVE('',#38365,#38366,#28999,.T.);
#49225=EDGE_CURVE('',#38363,#38365,#4204,.T.);
#49226=EDGE_CURVE('',#38364,#38366,#4205,.T.);
#49227=EDGE_CURVE('',#38367,#38368,#29000,.T.);
#49228=EDGE_CURVE('',#38365,#38367,#4206,.T.);
#49229=EDGE_CURVE('',#38366,#38368,#4207,.T.);
#49230=EDGE_CURVE('',#38369,#38370,#29001,.T.);
#49231=EDGE_CURVE('',#38367,#38369,#4208,.T.);
#49232=EDGE_CURVE('',#38368,#38370,#4209,.T.);
#49233=EDGE_CURVE('',#38371,#38372,#29002,.T.);
#49234=EDGE_CURVE('',#38369,#38371,#4210,.T.);
#49235=EDGE_CURVE('',#38370,#38372,#4211,.T.);
#49236=EDGE_CURVE('',#38373,#38374,#29003,.T.);
#49237=EDGE_CURVE('',#38371,#38373,#4212,.T.);
#49238=EDGE_CURVE('',#38372,#38374,#4213,.T.);
#49239=EDGE_CURVE('',#38375,#38376,#29004,.T.);
#49240=EDGE_CURVE('',#38373,#38375,#4214,.T.);
#49241=EDGE_CURVE('',#38374,#38376,#4215,.T.);
#49242=EDGE_CURVE('',#38377,#38378,#29005,.T.);
#49243=EDGE_CURVE('',#38377,#38379,#24637,.T.);
#49244=EDGE_CURVE('',#38379,#38380,#20576,.T.);
#49245=EDGE_CURVE('',#38378,#38380,#24638,.F.);
#49246=EDGE_CURVE('',#38381,#38382,#29006,.T.);
#49247=EDGE_CURVE('',#38381,#38377,#24639,.T.);
#49248=EDGE_CURVE('',#38382,#38378,#24640,.F.);
#49249=EDGE_CURVE('',#38383,#38384,#29007,.T.);
#49250=EDGE_CURVE('',#38383,#38381,#24641,.T.);
#49251=EDGE_CURVE('',#38384,#38382,#24642,.F.);
#49252=EDGE_CURVE('',#38385,#38386,#29008,.T.);
#49253=EDGE_CURVE('',#38385,#38383,#24643,.T.);
#49254=EDGE_CURVE('',#38386,#38384,#24644,.F.);
#49255=EDGE_CURVE('',#38387,#38388,#29009,.T.);
#49256=EDGE_CURVE('',#38387,#38385,#24645,.T.);
#49257=EDGE_CURVE('',#38388,#38386,#24646,.F.);
#49258=EDGE_CURVE('',#38389,#38390,#29010,.T.);
#49259=EDGE_CURVE('',#38389,#38387,#24647,.T.);
#49260=EDGE_CURVE('',#38390,#38388,#24648,.F.);
#49261=EDGE_CURVE('',#38391,#38392,#29011,.T.);
#49262=EDGE_CURVE('',#38391,#38389,#24649,.T.);
#49263=EDGE_CURVE('',#38392,#38390,#24650,.F.);
#49264=EDGE_CURVE('',#38393,#38394,#29012,.T.);
#49265=EDGE_CURVE('',#38393,#38391,#24651,.T.);
#49266=EDGE_CURVE('',#38394,#38392,#24652,.F.);
#49267=EDGE_CURVE('',#38395,#38396,#29013,.T.);
#49268=EDGE_CURVE('',#38395,#38393,#24653,.T.);
#49269=EDGE_CURVE('',#38396,#38394,#24654,.F.);
#49270=EDGE_CURVE('',#38397,#38398,#29014,.T.);
#49271=EDGE_CURVE('',#38397,#38395,#24655,.T.);
#49272=EDGE_CURVE('',#38398,#38396,#24656,.F.);
#49273=EDGE_CURVE('',#38399,#38400,#29015,.T.);
#49274=EDGE_CURVE('',#38399,#38397,#24657,.T.);
#49275=EDGE_CURVE('',#38400,#38398,#24658,.F.);
#49276=EDGE_CURVE('',#38401,#38402,#29016,.T.);
#49277=EDGE_CURVE('',#38401,#38399,#24659,.T.);
#49278=EDGE_CURVE('',#38402,#38400,#24660,.F.);
#49279=EDGE_CURVE('',#38403,#38404,#29017,.T.);
#49280=EDGE_CURVE('',#38403,#38401,#24661,.T.);
#49281=EDGE_CURVE('',#38404,#38402,#24662,.F.);
#49282=EDGE_CURVE('',#38405,#38406,#29018,.T.);
#49283=EDGE_CURVE('',#38405,#38403,#24663,.T.);
#49284=EDGE_CURVE('',#38406,#38404,#24664,.F.);
#49285=EDGE_CURVE('',#38407,#38408,#29019,.T.);
#49286=EDGE_CURVE('',#38407,#38405,#24665,.T.);
#49287=EDGE_CURVE('',#38408,#38406,#24666,.F.);
#49288=EDGE_CURVE('',#38409,#38410,#4216,.F.);
#49289=EDGE_CURVE('',#38409,#38410,#20577,.T.);
#49290=EDGE_CURVE('',#38411,#38411,#20578,.T.);
#49291=EDGE_CURVE('',#38412,#38412,#20579,.T.);
#49292=EDGE_CURVE('',#38413,#38413,#20580,.T.);
#49293=EDGE_CURVE('',#38413,#38414,#29020,.T.);
#49294=EDGE_CURVE('',#38414,#38414,#20581,.T.);
#49295=EDGE_CURVE('',#38345,#38415,#24667,.T.);
#49296=EDGE_CURVE('',#38416,#38415,#20582,.T.);
#49297=EDGE_CURVE('',#38416,#38417,#24668,.T.);
#49298=EDGE_CURVE('',#38417,#38418,#29021,.T.);
#49299=EDGE_CURVE('',#38418,#38418,#20583,.T.);
#49300=EDGE_CURVE('',#38417,#38348,#24669,.T.);
#49301=EDGE_CURVE('',#38416,#38408,#24670,.F.);
#49302=EDGE_CURVE('',#38415,#38407,#24671,.T.);
#49303=EDGE_CURVE('',#38419,#38379,#24672,.T.);
#49304=EDGE_CURVE('',#38420,#38419,#20584,.T.);
#49305=EDGE_CURVE('',#38380,#38420,#24673,.T.);
#49306=EDGE_CURVE('',#38421,#38422,#20585,.T.);
#49307=EDGE_CURVE('',#38423,#38421,#20586,.T.);
#49308=EDGE_CURVE('',#38410,#38423,#20587,.T.);
#49309=EDGE_CURVE('',#38424,#38409,#20588,.T.);
#49310=EDGE_CURVE('',#38422,#38424,#20589,.T.);
#49311=EDGE_CURVE('',#38410,#38423,#4217,.T.);
#49312=EDGE_CURVE('',#38423,#38421,#4218,.T.);
#49313=EDGE_CURVE('',#38421,#38422,#4219,.T.);
#49314=EDGE_CURVE('',#38422,#38424,#4220,.T.);
#49315=EDGE_CURVE('',#38424,#38409,#4221,.T.);
#49316=EDGE_CURVE('',#38425,#38426,#29022,.T.);
#49317=EDGE_CURVE('',#38426,#38427,#29023,.T.);
#49318=EDGE_CURVE('',#38427,#38428,#29024,.T.);
#49319=EDGE_CURVE('',#38428,#38429,#29025,.T.);
#49320=EDGE_CURVE('',#38429,#38430,#29026,.T.);
#49321=EDGE_CURVE('',#38430,#38425,#29027,.T.);
#49322=EDGE_CURVE('',#38426,#38409,#29028,.T.);
#49323=EDGE_CURVE('',#38427,#38410,#29029,.T.);
#49324=EDGE_CURVE('',#38428,#38423,#29030,.T.);
#49325=EDGE_CURVE('',#38429,#38421,#29031,.T.);
#49326=EDGE_CURVE('',#38430,#38422,#29032,.T.);
#49327=EDGE_CURVE('',#38425,#38424,#29033,.T.);
#49328=EDGE_CURVE('',#38376,#38420,#4222,.T.);
#49329=EDGE_CURVE('',#38375,#38419,#4223,.T.);
#69382=ORIENTED_EDGE('',*,*,#49193,.F.);
#69383=ORIENTED_EDGE('',*,*,#49194,.F.);
#69384=ORIENTED_EDGE('',*,*,#49195,.F.);
#69385=ORIENTED_EDGE('',*,*,#49196,.F.);
#69386=ORIENTED_EDGE('',*,*,#49197,.F.);
#69387=ORIENTED_EDGE('',*,*,#49193,.T.);
#69388=ORIENTED_EDGE('',*,*,#49198,.F.);
#69389=ORIENTED_EDGE('',*,*,#49199,.T.);
#69390=ORIENTED_EDGE('',*,*,#49200,.F.);
#69391=ORIENTED_EDGE('',*,*,#49201,.F.);
#69392=ORIENTED_EDGE('',*,*,#49196,.T.);
#69393=ORIENTED_EDGE('',*,*,#49202,.T.);
#69394=ORIENTED_EDGE('',*,*,#49203,.F.);
#69395=ORIENTED_EDGE('',*,*,#49204,.F.);
#69396=ORIENTED_EDGE('',*,*,#49200,.T.);
#69397=ORIENTED_EDGE('',*,*,#49205,.T.);
#69398=ORIENTED_EDGE('',*,*,#49206,.F.);
#69399=ORIENTED_EDGE('',*,*,#49207,.F.);
#69400=ORIENTED_EDGE('',*,*,#49203,.T.);
#69401=ORIENTED_EDGE('',*,*,#49208,.T.);
#69402=ORIENTED_EDGE('',*,*,#49209,.F.);
#69403=ORIENTED_EDGE('',*,*,#49210,.F.);
#69404=ORIENTED_EDGE('',*,*,#49206,.T.);
#69405=ORIENTED_EDGE('',*,*,#49211,.T.);
#69406=ORIENTED_EDGE('',*,*,#49212,.F.);
#69407=ORIENTED_EDGE('',*,*,#49213,.F.);
#69408=ORIENTED_EDGE('',*,*,#49209,.T.);
#69409=ORIENTED_EDGE('',*,*,#49214,.T.);
#69410=ORIENTED_EDGE('',*,*,#49215,.F.);
#69411=ORIENTED_EDGE('',*,*,#49216,.F.);
#69412=ORIENTED_EDGE('',*,*,#49212,.T.);
#69413=ORIENTED_EDGE('',*,*,#49217,.T.);
#69414=ORIENTED_EDGE('',*,*,#49218,.F.);
#69415=ORIENTED_EDGE('',*,*,#49219,.F.);
#69416=ORIENTED_EDGE('',*,*,#49215,.T.);
#69417=ORIENTED_EDGE('',*,*,#49220,.T.);
#69418=ORIENTED_EDGE('',*,*,#49221,.F.);
#69419=ORIENTED_EDGE('',*,*,#49222,.F.);
#69420=ORIENTED_EDGE('',*,*,#49218,.T.);
#69421=ORIENTED_EDGE('',*,*,#49223,.T.);
#69422=ORIENTED_EDGE('',*,*,#49224,.F.);
#69423=ORIENTED_EDGE('',*,*,#49225,.F.);
#69424=ORIENTED_EDGE('',*,*,#49221,.T.);
#69425=ORIENTED_EDGE('',*,*,#49226,.T.);
#69426=ORIENTED_EDGE('',*,*,#49227,.F.);
#69427=ORIENTED_EDGE('',*,*,#49228,.F.);
#69428=ORIENTED_EDGE('',*,*,#49224,.T.);
#69429=ORIENTED_EDGE('',*,*,#49229,.T.);
#69430=ORIENTED_EDGE('',*,*,#49230,.F.);
#69431=ORIENTED_EDGE('',*,*,#49231,.F.);
#69432=ORIENTED_EDGE('',*,*,#49227,.T.);
#69433=ORIENTED_EDGE('',*,*,#49232,.T.);
#69434=ORIENTED_EDGE('',*,*,#49233,.F.);
#69435=ORIENTED_EDGE('',*,*,#49234,.F.);
#69436=ORIENTED_EDGE('',*,*,#49230,.T.);
#69437=ORIENTED_EDGE('',*,*,#49235,.T.);
#69438=ORIENTED_EDGE('',*,*,#49236,.F.);
#69439=ORIENTED_EDGE('',*,*,#49237,.F.);
#69440=ORIENTED_EDGE('',*,*,#49233,.T.);
#69441=ORIENTED_EDGE('',*,*,#49238,.T.);
#69442=ORIENTED_EDGE('',*,*,#49239,.F.);
#69443=ORIENTED_EDGE('',*,*,#49240,.F.);
#69444=ORIENTED_EDGE('',*,*,#49236,.T.);
#69445=ORIENTED_EDGE('',*,*,#49241,.T.);
#69446=ORIENTED_EDGE('',*,*,#49242,.F.);
#69447=ORIENTED_EDGE('',*,*,#49243,.T.);
#69448=ORIENTED_EDGE('',*,*,#49244,.T.);
#69449=ORIENTED_EDGE('',*,*,#49245,.F.);
#69450=ORIENTED_EDGE('',*,*,#49246,.F.);
#69451=ORIENTED_EDGE('',*,*,#49247,.T.);
#69452=ORIENTED_EDGE('',*,*,#49242,.T.);
#69453=ORIENTED_EDGE('',*,*,#49248,.F.);
#69454=ORIENTED_EDGE('',*,*,#49249,.F.);
#69455=ORIENTED_EDGE('',*,*,#49250,.T.);
#69456=ORIENTED_EDGE('',*,*,#49246,.T.);
#69457=ORIENTED_EDGE('',*,*,#49251,.F.);
#69458=ORIENTED_EDGE('',*,*,#49252,.F.);
#69459=ORIENTED_EDGE('',*,*,#49253,.T.);
#69460=ORIENTED_EDGE('',*,*,#49249,.T.);
#69461=ORIENTED_EDGE('',*,*,#49254,.F.);
#69462=ORIENTED_EDGE('',*,*,#49255,.F.);
#69463=ORIENTED_EDGE('',*,*,#49256,.T.);
#69464=ORIENTED_EDGE('',*,*,#49252,.T.);
#69465=ORIENTED_EDGE('',*,*,#49257,.F.);
#69466=ORIENTED_EDGE('',*,*,#49258,.F.);
#69467=ORIENTED_EDGE('',*,*,#49259,.T.);
#69468=ORIENTED_EDGE('',*,*,#49255,.T.);
#69469=ORIENTED_EDGE('',*,*,#49260,.F.);
#69470=ORIENTED_EDGE('',*,*,#49261,.F.);
#69471=ORIENTED_EDGE('',*,*,#49262,.T.);
#69472=ORIENTED_EDGE('',*,*,#49258,.T.);
#69473=ORIENTED_EDGE('',*,*,#49263,.F.);
#69474=ORIENTED_EDGE('',*,*,#49264,.F.);
#69475=ORIENTED_EDGE('',*,*,#49265,.T.);
#69476=ORIENTED_EDGE('',*,*,#49261,.T.);
#69477=ORIENTED_EDGE('',*,*,#49266,.F.);
#69478=ORIENTED_EDGE('',*,*,#49267,.F.);
#69479=ORIENTED_EDGE('',*,*,#49268,.T.);
#69480=ORIENTED_EDGE('',*,*,#49264,.T.);
#69481=ORIENTED_EDGE('',*,*,#49269,.F.);
#69482=ORIENTED_EDGE('',*,*,#49270,.F.);
#69483=ORIENTED_EDGE('',*,*,#49271,.T.);
#69484=ORIENTED_EDGE('',*,*,#49267,.T.);
#69485=ORIENTED_EDGE('',*,*,#49272,.F.);
#69486=ORIENTED_EDGE('',*,*,#49273,.F.);
#69487=ORIENTED_EDGE('',*,*,#49274,.T.);
#69488=ORIENTED_EDGE('',*,*,#49270,.T.);
#69489=ORIENTED_EDGE('',*,*,#49275,.F.);
#69490=ORIENTED_EDGE('',*,*,#49276,.F.);
#69491=ORIENTED_EDGE('',*,*,#49277,.T.);
#69492=ORIENTED_EDGE('',*,*,#49273,.T.);
#69493=ORIENTED_EDGE('',*,*,#49278,.F.);
#69494=ORIENTED_EDGE('',*,*,#49279,.F.);
#69495=ORIENTED_EDGE('',*,*,#49280,.T.);
#69496=ORIENTED_EDGE('',*,*,#49276,.T.);
#69497=ORIENTED_EDGE('',*,*,#49281,.F.);
#69498=ORIENTED_EDGE('',*,*,#49282,.F.);
#69499=ORIENTED_EDGE('',*,*,#49283,.T.);
#69500=ORIENTED_EDGE('',*,*,#49279,.T.);
#69501=ORIENTED_EDGE('',*,*,#49284,.F.);
#69502=ORIENTED_EDGE('',*,*,#49285,.F.);
#69503=ORIENTED_EDGE('',*,*,#49286,.T.);
#69504=ORIENTED_EDGE('',*,*,#49282,.T.);
#69505=ORIENTED_EDGE('',*,*,#49287,.F.);
#69506=ORIENTED_EDGE('',*,*,#49288,.F.);
#69507=ORIENTED_EDGE('',*,*,#49289,.T.);
#69508=ORIENTED_EDGE('',*,*,#49290,.F.);
#69509=ORIENTED_EDGE('',*,*,#49291,.F.);
#69510=ORIENTED_EDGE('',*,*,#49292,.F.);
#69511=ORIENTED_EDGE('',*,*,#49293,.T.);
#69512=ORIENTED_EDGE('',*,*,#49294,.T.);
#69513=ORIENTED_EDGE('',*,*,#49293,.F.);
#69514=ORIENTED_EDGE('',*,*,#49198,.T.);
#69515=ORIENTED_EDGE('',*,*,#49195,.T.);
#69516=ORIENTED_EDGE('',*,*,#49295,.T.);
#69517=ORIENTED_EDGE('',*,*,#49296,.F.);
#69518=ORIENTED_EDGE('',*,*,#49297,.T.);
#69519=ORIENTED_EDGE('',*,*,#49298,.T.);
#69520=ORIENTED_EDGE('',*,*,#49299,.F.);
#69521=ORIENTED_EDGE('',*,*,#49298,.F.);
#69522=ORIENTED_EDGE('',*,*,#49300,.T.);
#69523=ORIENTED_EDGE('',*,*,#49285,.T.);
#69524=ORIENTED_EDGE('',*,*,#49301,.F.);
#69525=ORIENTED_EDGE('',*,*,#49296,.T.);
#69526=ORIENTED_EDGE('',*,*,#49302,.T.);
#69527=ORIENTED_EDGE('',*,*,#49299,.T.);
#69528=ORIENTED_EDGE('',*,*,#49292,.T.);
#69529=ORIENTED_EDGE('',*,*,#49244,.F.);
#69530=ORIENTED_EDGE('',*,*,#49303,.F.);
#69531=ORIENTED_EDGE('',*,*,#49304,.F.);
#69532=ORIENTED_EDGE('',*,*,#49305,.F.);
#69533=ORIENTED_EDGE('',*,*,#49294,.F.);
#69534=ORIENTED_EDGE('',*,*,#49290,.T.);
#69535=ORIENTED_EDGE('',*,*,#49291,.T.);
#69536=ORIENTED_EDGE('',*,*,#49306,.F.);
#69537=ORIENTED_EDGE('',*,*,#49307,.F.);
#69538=ORIENTED_EDGE('',*,*,#49308,.F.);
#69539=ORIENTED_EDGE('',*,*,#49289,.F.);
#69540=ORIENTED_EDGE('',*,*,#49309,.F.);
#69541=ORIENTED_EDGE('',*,*,#49310,.F.);
#69542=ORIENTED_EDGE('',*,*,#49308,.T.);
#69543=ORIENTED_EDGE('',*,*,#49311,.F.);
#69544=ORIENTED_EDGE('',*,*,#49307,.T.);
#69545=ORIENTED_EDGE('',*,*,#49312,.F.);
#69546=ORIENTED_EDGE('',*,*,#49306,.T.);
#69547=ORIENTED_EDGE('',*,*,#49313,.F.);
#69548=ORIENTED_EDGE('',*,*,#49310,.T.);
#69549=ORIENTED_EDGE('',*,*,#49314,.F.);
#69550=ORIENTED_EDGE('',*,*,#49309,.T.);
#69551=ORIENTED_EDGE('',*,*,#49315,.F.);
#69552=ORIENTED_EDGE('',*,*,#49316,.T.);
#69553=ORIENTED_EDGE('',*,*,#49317,.T.);
#69554=ORIENTED_EDGE('',*,*,#49318,.T.);
#69555=ORIENTED_EDGE('',*,*,#49319,.T.);
#69556=ORIENTED_EDGE('',*,*,#49320,.T.);
#69557=ORIENTED_EDGE('',*,*,#49321,.T.);
#69558=ORIENTED_EDGE('',*,*,#49322,.T.);
#69559=ORIENTED_EDGE('',*,*,#49288,.T.);
#69560=ORIENTED_EDGE('',*,*,#49323,.F.);
#69561=ORIENTED_EDGE('',*,*,#49317,.F.);
#69562=ORIENTED_EDGE('',*,*,#49323,.T.);
#69563=ORIENTED_EDGE('',*,*,#49311,.T.);
#69564=ORIENTED_EDGE('',*,*,#49324,.F.);
#69565=ORIENTED_EDGE('',*,*,#49318,.F.);
#69566=ORIENTED_EDGE('',*,*,#49324,.T.);
#69567=ORIENTED_EDGE('',*,*,#49312,.T.);
#69568=ORIENTED_EDGE('',*,*,#49325,.F.);
#69569=ORIENTED_EDGE('',*,*,#49319,.F.);
#69570=ORIENTED_EDGE('',*,*,#49325,.T.);
#69571=ORIENTED_EDGE('',*,*,#49313,.T.);
#69572=ORIENTED_EDGE('',*,*,#49326,.F.);
#69573=ORIENTED_EDGE('',*,*,#49320,.F.);
#69574=ORIENTED_EDGE('',*,*,#49326,.T.);
#69575=ORIENTED_EDGE('',*,*,#49314,.T.);
#69576=ORIENTED_EDGE('',*,*,#49327,.F.);
#69577=ORIENTED_EDGE('',*,*,#49321,.F.);
#69578=ORIENTED_EDGE('',*,*,#49327,.T.);
#69579=ORIENTED_EDGE('',*,*,#49315,.T.);
#69580=ORIENTED_EDGE('',*,*,#49322,.F.);
#69581=ORIENTED_EDGE('',*,*,#49316,.F.);
#69582=ORIENTED_EDGE('',*,*,#49305,.T.);
#69583=ORIENTED_EDGE('',*,*,#49328,.F.);
#69584=ORIENTED_EDGE('',*,*,#49241,.F.);
#69585=ORIENTED_EDGE('',*,*,#49238,.F.);
#69586=ORIENTED_EDGE('',*,*,#49235,.F.);
#69587=ORIENTED_EDGE('',*,*,#49232,.F.);
#69588=ORIENTED_EDGE('',*,*,#49229,.F.);
#69589=ORIENTED_EDGE('',*,*,#49226,.F.);
#69590=ORIENTED_EDGE('',*,*,#49223,.F.);
#69591=ORIENTED_EDGE('',*,*,#49220,.F.);
#69592=ORIENTED_EDGE('',*,*,#49217,.F.);
#69593=ORIENTED_EDGE('',*,*,#49214,.F.);
#69594=ORIENTED_EDGE('',*,*,#49211,.F.);
#69595=ORIENTED_EDGE('',*,*,#49208,.F.);
#69596=ORIENTED_EDGE('',*,*,#49205,.F.);
#69597=ORIENTED_EDGE('',*,*,#49202,.F.);
#69598=ORIENTED_EDGE('',*,*,#49199,.F.);
#69599=ORIENTED_EDGE('',*,*,#49300,.F.);
#69600=ORIENTED_EDGE('',*,*,#49297,.F.);
#69601=ORIENTED_EDGE('',*,*,#49301,.T.);
#69602=ORIENTED_EDGE('',*,*,#49287,.T.);
#69603=ORIENTED_EDGE('',*,*,#49284,.T.);
#69604=ORIENTED_EDGE('',*,*,#49281,.T.);
#69605=ORIENTED_EDGE('',*,*,#49278,.T.);
#69606=ORIENTED_EDGE('',*,*,#49275,.T.);
#69607=ORIENTED_EDGE('',*,*,#49272,.T.);
#69608=ORIENTED_EDGE('',*,*,#49269,.T.);
#69609=ORIENTED_EDGE('',*,*,#49266,.T.);
#69610=ORIENTED_EDGE('',*,*,#49263,.T.);
#69611=ORIENTED_EDGE('',*,*,#49260,.T.);
#69612=ORIENTED_EDGE('',*,*,#49257,.T.);
#69613=ORIENTED_EDGE('',*,*,#49254,.T.);
#69614=ORIENTED_EDGE('',*,*,#49251,.T.);
#69615=ORIENTED_EDGE('',*,*,#49248,.T.);
#69616=ORIENTED_EDGE('',*,*,#49245,.T.);
#69617=ORIENTED_EDGE('',*,*,#49239,.T.);
#69618=ORIENTED_EDGE('',*,*,#49328,.T.);
#69619=ORIENTED_EDGE('',*,*,#49304,.T.);
#69620=ORIENTED_EDGE('',*,*,#49329,.F.);
#69621=ORIENTED_EDGE('',*,*,#49303,.T.);
#69622=ORIENTED_EDGE('',*,*,#49243,.F.);
#69623=ORIENTED_EDGE('',*,*,#49247,.F.);
#69624=ORIENTED_EDGE('',*,*,#49250,.F.);
#69625=ORIENTED_EDGE('',*,*,#49253,.F.);
#69626=ORIENTED_EDGE('',*,*,#49256,.F.);
#69627=ORIENTED_EDGE('',*,*,#49259,.F.);
#69628=ORIENTED_EDGE('',*,*,#49262,.F.);
#69629=ORIENTED_EDGE('',*,*,#49265,.F.);
#69630=ORIENTED_EDGE('',*,*,#49268,.F.);
#69631=ORIENTED_EDGE('',*,*,#49271,.F.);
#69632=ORIENTED_EDGE('',*,*,#49274,.F.);
#69633=ORIENTED_EDGE('',*,*,#49277,.F.);
#69634=ORIENTED_EDGE('',*,*,#49280,.F.);
#69635=ORIENTED_EDGE('',*,*,#49283,.F.);
#69636=ORIENTED_EDGE('',*,*,#49286,.F.);
#69637=ORIENTED_EDGE('',*,*,#49302,.F.);
#69638=ORIENTED_EDGE('',*,*,#49295,.F.);
#69639=ORIENTED_EDGE('',*,*,#49194,.T.);
#69640=ORIENTED_EDGE('',*,*,#49197,.T.);
#69641=ORIENTED_EDGE('',*,*,#49201,.T.);
#69642=ORIENTED_EDGE('',*,*,#49204,.T.);
#69643=ORIENTED_EDGE('',*,*,#49207,.T.);
#69644=ORIENTED_EDGE('',*,*,#49210,.T.);
#69645=ORIENTED_EDGE('',*,*,#49213,.T.);
#69646=ORIENTED_EDGE('',*,*,#49216,.T.);
#69647=ORIENTED_EDGE('',*,*,#49219,.T.);
#69648=ORIENTED_EDGE('',*,*,#49222,.T.);
#69649=ORIENTED_EDGE('',*,*,#49225,.T.);
#69650=ORIENTED_EDGE('',*,*,#49228,.T.);
#69651=ORIENTED_EDGE('',*,*,#49231,.T.);
#69652=ORIENTED_EDGE('',*,*,#49234,.T.);
#69653=ORIENTED_EDGE('',*,*,#49237,.T.);
#69654=ORIENTED_EDGE('',*,*,#49240,.T.);
#69655=ORIENTED_EDGE('',*,*,#49329,.T.);
#87931=CYLINDRICAL_SURFACE('',#99249,1.17524047358091);
#87932=CYLINDRICAL_SURFACE('',#99251,1.17524047358091);
#87933=CYLINDRICAL_SURFACE('',#99253,1.17524047358091);
#87934=CYLINDRICAL_SURFACE('',#99254,1.17524047358091);
#87935=CYLINDRICAL_SURFACE('',#99255,1.17524047358091);
#87936=CYLINDRICAL_SURFACE('',#99256,1.17524047358091);
#87937=CYLINDRICAL_SURFACE('',#99257,1.17524047358091);
#87938=CYLINDRICAL_SURFACE('',#99258,1.17524047358091);
#87939=CYLINDRICAL_SURFACE('',#99259,1.17524047358091);
#87940=CYLINDRICAL_SURFACE('',#99260,1.17524047358091);
#87941=CYLINDRICAL_SURFACE('',#99261,1.17524047358091);
#87942=CYLINDRICAL_SURFACE('',#99262,1.17524047358091);
#87943=CYLINDRICAL_SURFACE('',#99263,1.17524047358091);
#87944=CYLINDRICAL_SURFACE('',#99264,1.17524047358091);
#87945=CYLINDRICAL_SURFACE('',#99265,1.17524047358091);
#87946=CYLINDRICAL_SURFACE('',#99266,1.17524047358091);
#87947=CYLINDRICAL_SURFACE('',#99267,1.5);
#87948=CYLINDRICAL_SURFACE('',#99269,1.5);
#87949=CYLINDRICAL_SURFACE('',#99270,1.5);
#87950=CYLINDRICAL_SURFACE('',#99271,1.5);
#87951=CYLINDRICAL_SURFACE('',#99272,1.5);
#87952=CYLINDRICAL_SURFACE('',#99273,1.5);
#87953=CYLINDRICAL_SURFACE('',#99274,1.5);
#87954=CYLINDRICAL_SURFACE('',#99275,1.5);
#87955=CYLINDRICAL_SURFACE('',#99276,1.5);
#87956=CYLINDRICAL_SURFACE('',#99277,1.5);
#87957=CYLINDRICAL_SURFACE('',#99278,1.5);
#87958=CYLINDRICAL_SURFACE('',#99279,1.5);
#87959=CYLINDRICAL_SURFACE('',#99280,1.5);
#87960=CYLINDRICAL_SURFACE('',#99281,1.5);
#87961=CYLINDRICAL_SURFACE('',#99282,1.5);
#87962=CYLINDRICAL_SURFACE('',#99288,3.5);
#87963=CYLINDRICAL_SURFACE('',#99294,1.5);
#87964=CYLINDRICAL_SURFACE('',#99317,1.17524047358091);
#90908=ADVANCED_FACE('',(#8444),#87931,.T.);
#90909=ADVANCED_FACE('',(#8445),#87932,.T.);
#90910=ADVANCED_FACE('',(#8446),#87933,.T.);
#90911=ADVANCED_FACE('',(#8447),#87934,.T.);
#90912=ADVANCED_FACE('',(#8448),#87935,.T.);
#90913=ADVANCED_FACE('',(#8449),#87936,.T.);
#90914=ADVANCED_FACE('',(#8450),#87937,.T.);
#90915=ADVANCED_FACE('',(#8451),#87938,.T.);
#90916=ADVANCED_FACE('',(#8452),#87939,.T.);
#90917=ADVANCED_FACE('',(#8453),#87940,.T.);
#90918=ADVANCED_FACE('',(#8454),#87941,.T.);
#90919=ADVANCED_FACE('',(#8455),#87942,.T.);
#90920=ADVANCED_FACE('',(#8456),#87943,.T.);
#90921=ADVANCED_FACE('',(#8457),#87944,.T.);
#90922=ADVANCED_FACE('',(#8458),#87945,.T.);
#90923=ADVANCED_FACE('',(#8459),#87946,.T.);
#90924=ADVANCED_FACE('',(#8460),#87947,.T.);
#90925=ADVANCED_FACE('',(#8461),#87948,.T.);
#90926=ADVANCED_FACE('',(#8462),#87949,.T.);
#90927=ADVANCED_FACE('',(#8463),#87950,.T.);
#90928=ADVANCED_FACE('',(#8464),#87951,.T.);
#90929=ADVANCED_FACE('',(#8465),#87952,.T.);
#90930=ADVANCED_FACE('',(#8466),#87953,.T.);
#90931=ADVANCED_FACE('',(#8467),#87954,.T.);
#90932=ADVANCED_FACE('',(#8468),#87955,.T.);
#90933=ADVANCED_FACE('',(#8469),#87956,.T.);
#90934=ADVANCED_FACE('',(#8470),#87957,.T.);
#90935=ADVANCED_FACE('',(#8471),#87958,.T.);
#90936=ADVANCED_FACE('',(#8472),#87959,.T.);
#90937=ADVANCED_FACE('',(#8473),#87960,.T.);
#90938=ADVANCED_FACE('',(#8474),#87961,.T.);
#90939=ADVANCED_FACE('',(#8475),#4888,.F.);
#90940=ADVANCED_FACE('',(#8476,#5221),#155,.T.);
#90941=ADVANCED_FACE('',(#8477),#87962,.T.);
#90942=ADVANCED_FACE('',(#8478),#4889,.T.);
#90943=ADVANCED_FACE('',(#8479),#87963,.T.);
#90944=ADVANCED_FACE('',(#8480),#5705,.T.);
#90945=ADVANCED_FACE('',(#8481,#5222),#5706,.F.);
#90946=ADVANCED_FACE('',(#8482,#5223),#5707,.F.);
#90947=ADVANCED_FACE('',(#8483,#5224),#5708,.F.);
#90948=ADVANCED_FACE('',(#8484),#4890,.F.);
#90949=ADVANCED_FACE('',(#8485),#4891,.F.);
#90950=ADVANCED_FACE('',(#8486),#4892,.F.);
#90951=ADVANCED_FACE('',(#8487),#4893,.F.);
#90952=ADVANCED_FACE('',(#8488),#4894,.F.);
#90953=ADVANCED_FACE('',(#8489),#5709,.T.);
#90954=ADVANCED_FACE('',(#8490),#5710,.F.);
#90955=ADVANCED_FACE('',(#8491),#5711,.F.);
#90956=ADVANCED_FACE('',(#8492),#5712,.F.);
#90957=ADVANCED_FACE('',(#8493),#5713,.F.);
#90958=ADVANCED_FACE('',(#8494),#5714,.F.);
#90959=ADVANCED_FACE('',(#8495),#5715,.F.);
#90960=ADVANCED_FACE('',(#8496),#2315,.T.);
#90961=ADVANCED_FACE('',(#8497),#87964,.T.);
#90962=ADVANCED_FACE('',(#8498),#2316,.T.);
#94663=CLOSED_SHELL('',(#90908,#90909,#90910,#90911,#90912,#90913,#90914,
#90915,#90916,#90917,#90918,#90919,#90920,#90921,#90922,#90923,#90924,#90925,
#90926,#90927,#90928,#90929,#90930,#90931,#90932,#90933,#90934,#90935,#90936,
#90937,#90938,#90939,#90940,#90941,#90942,#90943,#90944,#90945,#90946,#90947,
#90948,#90949,#90950,#90951,#90952,#90953,#90954,#90955,#90956,#90957,#90958,
#90959,#90960,#90961,#90962));
#99248=AXIS2_PLACEMENT_3D('',#366325,#116205,#116206);
#99249=AXIS2_PLACEMENT_3D('',#366326,#116207,#116208);
#99250=AXIS2_PLACEMENT_3D('',#366334,#116210,#116211);
#99251=AXIS2_PLACEMENT_3D('',#366335,#116212,#116213);
#99252=AXIS2_PLACEMENT_3D('',#366353,#116215,#116216);
#99253=AXIS2_PLACEMENT_3D('',#366367,#116217,#116218);
#99254=AXIS2_PLACEMENT_3D('',#366397,#116220,#116221);
#99255=AXIS2_PLACEMENT_3D('',#366427,#116223,#116224);
#99256=AXIS2_PLACEMENT_3D('',#366457,#116226,#116227);
#99257=AXIS2_PLACEMENT_3D('',#366487,#116229,#116230);
#99258=AXIS2_PLACEMENT_3D('',#366517,#116232,#116233);
#99259=AXIS2_PLACEMENT_3D('',#366547,#116235,#116236);
#99260=AXIS2_PLACEMENT_3D('',#366577,#116238,#116239);
#99261=AXIS2_PLACEMENT_3D('',#366607,#116241,#116242);
#99262=AXIS2_PLACEMENT_3D('',#366637,#116244,#116245);
#99263=AXIS2_PLACEMENT_3D('',#366667,#116247,#116248);
#99264=AXIS2_PLACEMENT_3D('',#366697,#116250,#116251);
#99265=AXIS2_PLACEMENT_3D('',#366727,#116253,#116254);
#99266=AXIS2_PLACEMENT_3D('',#366757,#116256,#116257);
#99267=AXIS2_PLACEMENT_3D('',#366787,#116259,#116260);
#99268=AXIS2_PLACEMENT_3D('',#366813,#116262,#116263);
#99269=AXIS2_PLACEMENT_3D('',#366830,#116264,#116265);
#99270=AXIS2_PLACEMENT_3D('',#366906,#116267,#116268);
#99271=AXIS2_PLACEMENT_3D('',#366984,#116270,#116271);
#99272=AXIS2_PLACEMENT_3D('',#367060,#116273,#116274);
#99273=AXIS2_PLACEMENT_3D('',#367136,#116276,#116277);
#99274=AXIS2_PLACEMENT_3D('',#367212,#116279,#116280);
#99275=AXIS2_PLACEMENT_3D('',#367288,#116282,#116283);
#99276=AXIS2_PLACEMENT_3D('',#367366,#116285,#116286);
#99277=AXIS2_PLACEMENT_3D('',#367444,#116288,#116289);
#99278=AXIS2_PLACEMENT_3D('',#367520,#116291,#116292);
#99279=AXIS2_PLACEMENT_3D('',#367596,#116294,#116295);
#99280=AXIS2_PLACEMENT_3D('',#367672,#116297,#116298);
#99281=AXIS2_PLACEMENT_3D('',#367748,#116300,#116301);
#99282=AXIS2_PLACEMENT_3D('',#367826,#116303,#116304);
#99283=AXIS2_PLACEMENT_3D('',#367902,#116306,#116307);
#99284=AXIS2_PLACEMENT_3D('',#367908,#116308,#116309);
#99285=AXIS2_PLACEMENT_3D('',#367909,#116310,#116311);
#99286=AXIS2_PLACEMENT_3D('',#367911,#116312,#116313);
#99287=AXIS2_PLACEMENT_3D('',#367913,#116314,#116315);
#99288=AXIS2_PLACEMENT_3D('',#367914,#116316,#116317);
#99289=AXIS2_PLACEMENT_3D('',#367916,#116318,#116319);
#99290=AXIS2_PLACEMENT_3D('',#367919,#116321,#116322);
#99291=AXIS2_PLACEMENT_3D('',#367920,#116323,#116324);
#99292=AXIS2_PLACEMENT_3D('',#367935,#116325,#116326);
#99293=AXIS2_PLACEMENT_3D('',#367965,#116328,#116329);
#99294=AXIS2_PLACEMENT_3D('',#367982,#116330,#116331);
#99295=AXIS2_PLACEMENT_3D('',#368045,#116332,#116333);
#99296=AXIS2_PLACEMENT_3D('',#368046,#116334,#116335);
#99297=AXIS2_PLACEMENT_3D('',#368067,#116336,#116337);
#99298=AXIS2_PLACEMENT_3D('',#368084,#116338,#116339);
#99299=AXIS2_PLACEMENT_3D('',#368085,#116340,#116341);
#99300=AXIS2_PLACEMENT_3D('',#368088,#116342,#116343);
#99301=AXIS2_PLACEMENT_3D('',#368090,#116344,#116345);
#99302=AXIS2_PLACEMENT_3D('',#368091,#116346,#116347);
#99303=AXIS2_PLACEMENT_3D('',#368093,#116348,#116349);
#99304=AXIS2_PLACEMENT_3D('',#368094,#116350,#116351);
#99305=AXIS2_PLACEMENT_3D('',#368095,#116352,#116353);
#99306=AXIS2_PLACEMENT_3D('',#368099,#116354,#116355);
#99307=AXIS2_PLACEMENT_3D('',#368103,#116356,#116357);
#99308=AXIS2_PLACEMENT_3D('',#368107,#116358,#116359);
#99309=AXIS2_PLACEMENT_3D('',#368111,#116360,#116361);
#99310=AXIS2_PLACEMENT_3D('',#368115,#116362,#116363);
#99311=AXIS2_PLACEMENT_3D('',#368128,#116370,#116371);
#99312=AXIS2_PLACEMENT_3D('',#368131,#116374,#116375);
#99313=AXIS2_PLACEMENT_3D('',#368133,#116377,#116378);
#99314=AXIS2_PLACEMENT_3D('',#368135,#116380,#116381);
#99315=AXIS2_PLACEMENT_3D('',#368137,#116383,#116384);
#99316=AXIS2_PLACEMENT_3D('',#368139,#116386,#116387);
#99317=AXIS2_PLACEMENT_3D('',#368563,#116388,#116389);
#116205=DIRECTION('axis',(0.,0.,1.));
#116206=DIRECTION('refdir',(1.,0.,0.));
#116207=DIRECTION('center_axis',(0.,0.,1.));
#116208=DIRECTION('ref_axis',(0.,1.,0.));
#116209=DIRECTION('',(0.,0.,-1.));
#116210=DIRECTION('center_axis',(-1.94626492602832E-14,6.50402624464167E-14,
-1.));
#116211=DIRECTION('ref_axis',(1.5941429827944E-14,-1.,-6.51827352964822E-14));
#116212=DIRECTION('center_axis',(0.,0.,1.));
#116213=DIRECTION('ref_axis',(0.,1.,0.));
#116214=DIRECTION('',(0.,0.,-1.));
#116215=DIRECTION('center_axis',(-1.94626492602832E-14,6.50402624464167E-14,
-1.));
#116216=DIRECTION('ref_axis',(1.5941429827944E-14,-1.,-6.51827352964822E-14));
#116217=DIRECTION('center_axis',(0.,0.,1.));
#116218=DIRECTION('ref_axis',(0.,1.,0.));
#116219=DIRECTION('',(0.,0.,-1.));
#116220=DIRECTION('center_axis',(0.,0.,1.));
#116221=DIRECTION('ref_axis',(0.,1.,0.));
#116222=DIRECTION('',(0.,0.,-1.));
#116223=DIRECTION('center_axis',(0.,0.,1.));
#116224=DIRECTION('ref_axis',(0.,1.,0.));
#116225=DIRECTION('',(0.,0.,-1.));
#116226=DIRECTION('center_axis',(0.,0.,1.));
#116227=DIRECTION('ref_axis',(0.,1.,0.));
#116228=DIRECTION('',(0.,0.,-1.));
#116229=DIRECTION('center_axis',(0.,0.,1.));
#116230=DIRECTION('ref_axis',(0.,1.,0.));
#116231=DIRECTION('',(0.,0.,-1.));
#116232=DIRECTION('center_axis',(0.,0.,1.));
#116233=DIRECTION('ref_axis',(0.,1.,0.));
#116234=DIRECTION('',(0.,0.,-1.));
#116235=DIRECTION('center_axis',(0.,0.,1.));
#116236=DIRECTION('ref_axis',(0.,1.,0.));
#116237=DIRECTION('',(0.,0.,-1.));
#116238=DIRECTION('center_axis',(0.,0.,1.));
#116239=DIRECTION('ref_axis',(0.,1.,0.));
#116240=DIRECTION('',(0.,0.,-1.));
#116241=DIRECTION('center_axis',(0.,0.,1.));
#116242=DIRECTION('ref_axis',(0.,1.,0.));
#116243=DIRECTION('',(0.,0.,-1.));
#116244=DIRECTION('center_axis',(0.,0.,1.));
#116245=DIRECTION('ref_axis',(0.,1.,0.));
#116246=DIRECTION('',(0.,0.,-1.));
#116247=DIRECTION('center_axis',(0.,0.,1.));
#116248=DIRECTION('ref_axis',(0.,1.,0.));
#116249=DIRECTION('',(0.,0.,-1.));
#116250=DIRECTION('center_axis',(0.,0.,1.));
#116251=DIRECTION('ref_axis',(0.,1.,0.));
#116252=DIRECTION('',(0.,0.,-1.));
#116253=DIRECTION('center_axis',(0.,0.,1.));
#116254=DIRECTION('ref_axis',(0.,1.,0.));
#116255=DIRECTION('',(0.,0.,-1.));
#116256=DIRECTION('center_axis',(0.,0.,1.));
#116257=DIRECTION('ref_axis',(0.,1.,0.));
#116258=DIRECTION('',(0.,0.,-1.));
#116259=DIRECTION('center_axis',(0.,2.71050543121376E-17,-1.));
#116260=DIRECTION('ref_axis',(0.,1.,2.71050543121376E-17));
#116261=DIRECTION('',(0.,-2.71050543121376E-17,1.));
#116262=DIRECTION('center_axis',(0.,0.,-1.));
#116263=DIRECTION('ref_axis',(1.,-3.5527136788005E-15,0.));
#116264=DIRECTION('center_axis',(0.,2.71050543121376E-17,-1.));
#116265=DIRECTION('ref_axis',(0.,1.,2.71050543121376E-17));
#116266=DIRECTION('',(0.,-2.71050543121376E-17,1.));
#116267=DIRECTION('center_axis',(0.,2.71050543121376E-17,-1.));
#116268=DIRECTION('ref_axis',(0.,1.,2.71050543121376E-17));
#116269=DIRECTION('',(0.,-2.71050543121376E-17,1.));
#116270=DIRECTION('center_axis',(0.,2.71050543121376E-17,-1.));
#116271=DIRECTION('ref_axis',(0.,1.,2.71050543121376E-17));
#116272=DIRECTION('',(0.,-2.71050543121376E-17,1.));
#116273=DIRECTION('center_axis',(0.,2.71050543121376E-17,-1.));
#116274=DIRECTION('ref_axis',(0.,1.,2.71050543121376E-17));
#116275=DIRECTION('',(0.,-2.71050543121376E-17,1.));
#116276=DIRECTION('center_axis',(0.,2.71050543121376E-17,-1.));
#116277=DIRECTION('ref_axis',(0.,1.,2.71050543121376E-17));
#116278=DIRECTION('',(0.,-2.71050543121376E-17,1.));
#116279=DIRECTION('center_axis',(0.,2.71050543121376E-17,-1.));
#116280=DIRECTION('ref_axis',(0.,1.,2.71050543121376E-17));
#116281=DIRECTION('',(0.,-2.71050543121376E-17,1.));
#116282=DIRECTION('center_axis',(0.,2.71050543121376E-17,-1.));
#116283=DIRECTION('ref_axis',(0.,1.,2.71050543121376E-17));
#116284=DIRECTION('',(0.,-2.71050543121376E-17,1.));
#116285=DIRECTION('center_axis',(0.,2.71050543121376E-17,-1.));
#116286=DIRECTION('ref_axis',(0.,1.,2.71050543121376E-17));
#116287=DIRECTION('',(0.,-2.71050543121376E-17,1.));
#116288=DIRECTION('center_axis',(0.,2.71050543121376E-17,-1.));
#116289=DIRECTION('ref_axis',(0.,1.,2.71050543121376E-17));
#116290=DIRECTION('',(0.,-2.71050543121376E-17,1.));
#116291=DIRECTION('center_axis',(0.,2.71050543121376E-17,-1.));
#116292=DIRECTION('ref_axis',(0.,1.,2.71050543121376E-17));
#116293=DIRECTION('',(0.,-2.71050543121376E-17,1.));
#116294=DIRECTION('center_axis',(0.,2.71050543121376E-17,-1.));
#116295=DIRECTION('ref_axis',(0.,1.,2.71050543121376E-17));
#116296=DIRECTION('',(0.,-2.71050543121376E-17,1.));
#116297=DIRECTION('center_axis',(0.,2.71050543121376E-17,-1.));
#116298=DIRECTION('ref_axis',(0.,1.,2.71050543121376E-17));
#116299=DIRECTION('',(0.,-2.71050543121376E-17,1.));
#116300=DIRECTION('center_axis',(0.,2.71050543121376E-17,-1.));
#116301=DIRECTION('ref_axis',(0.,1.,2.71050543121376E-17));
#116302=DIRECTION('',(0.,-2.71050543121376E-17,1.));
#116303=DIRECTION('center_axis',(0.,2.71050543121376E-17,-1.));
#116304=DIRECTION('ref_axis',(0.,1.,2.71050543121376E-17));
#116305=DIRECTION('',(0.,-2.71050543121376E-17,1.));
#116306=DIRECTION('center_axis',(0.,0.,1.));
#116307=DIRECTION('ref_axis',(1.,0.,0.));
#116308=DIRECTION('center_axis',(0.,0.,1.));
#116309=DIRECTION('ref_axis',(1.,0.,0.));
#116310=DIRECTION('center_axis',(1.,6.9217303377289E-15,0.));
#116311=DIRECTION('ref_axis',(6.98296267768627E-15,-1.,0.));
#116312=DIRECTION('center_axis',(0.,0.,-1.));
#116313=DIRECTION('ref_axis',(-1.,0.,0.));
#116314=DIRECTION('center_axis',(0.,0.,1.));
#116315=DIRECTION('ref_axis',(1.,0.,0.));
#116316=DIRECTION('center_axis',(0.,0.,-1.));
#116317=DIRECTION('ref_axis',(-1.,0.,0.));
#116318=DIRECTION('center_axis',(0.,0.,-1.));
#116319=DIRECTION('ref_axis',(-1.,0.,0.));
#116320=DIRECTION('',(0.,0.,1.));
#116321=DIRECTION('center_axis',(0.,0.,-1.));
#116322=DIRECTION('ref_axis',(-1.,0.,0.));
#116323=DIRECTION('center_axis',(0.,-2.71050543121376E-17,1.));
#116324=DIRECTION('ref_axis',(0.,-1.,-2.71050543121376E-17));
#116325=DIRECTION('center_axis',(0.,-2.71050543121376E-17,1.));
#116326=DIRECTION('ref_axis',(1.77635683940025E-15,1.,2.71050543121376E-17));
#116327=DIRECTION('',(8.65956056235491E-17,-0.707106781186546,-0.707106781186549));
#116328=DIRECTION('center_axis',(0.,2.71050543121376E-17,-1.));
#116329=DIRECTION('ref_axis',(0.,1.,2.71050543121376E-17));
#116330=DIRECTION('center_axis',(0.,2.71050543121376E-17,-1.));
#116331=DIRECTION('ref_axis',(0.,1.,2.71050543121376E-17));
#116332=DIRECTION('center_axis',(0.,2.71050543121376E-17,-1.));
#116333=DIRECTION('ref_axis',(0.,1.,2.71050543121376E-17));
#116334=DIRECTION('center_axis',(0.,0.,1.));
#116335=DIRECTION('ref_axis',(1.,0.,0.));
#116336=DIRECTION('center_axis',(1.77885347431222E-15,2.70173479802082E-15,
-1.));
#116337=DIRECTION('ref_axis',(-0.700629269222034,-0.713525491562424,-3.07020130019678E-15));
#116338=DIRECTION('center_axis',(0.,0.,-1.));
#116339=DIRECTION('ref_axis',(-1.,0.,0.));
#116340=DIRECTION('center_axis',(0.,0.,-1.));
#116341=DIRECTION('ref_axis',(-1.,0.,0.));
#116342=DIRECTION('center_axis',(0.,0.,1.));
#116343=DIRECTION('ref_axis',(1.,0.,0.));
#116344=DIRECTION('center_axis',(0.,0.,1.));
#116345=DIRECTION('ref_axis',(1.,0.,0.));
#116346=DIRECTION('center_axis',(0.,0.,1.));
#116347=DIRECTION('ref_axis',(1.,0.,0.));
#116348=DIRECTION('center_axis',(0.,0.,1.));
#116349=DIRECTION('ref_axis',(1.,0.,0.));
#116350=DIRECTION('center_axis',(0.,0.,1.));
#116351=DIRECTION('ref_axis',(1.,0.,0.));
#116352=DIRECTION('center_axis',(0.,0.,1.));
#116353=DIRECTION('ref_axis',(1.,0.,0.));
#116354=DIRECTION('center_axis',(0.,0.,1.));
#116355=DIRECTION('ref_axis',(1.,0.,0.));
#116356=DIRECTION('center_axis',(0.,0.,1.));
#116357=DIRECTION('ref_axis',(-1.,-3.21624529935327E-16,0.));
#116358=DIRECTION('center_axis',(0.,0.,1.));
#116359=DIRECTION('ref_axis',(1.,0.,0.));
#116360=DIRECTION('center_axis',(0.,0.,1.));
#116361=DIRECTION('ref_axis',(1.,0.,0.));
#116362=DIRECTION('center_axis',(0.,0.,1.));
#116363=DIRECTION('ref_axis',(1.,0.,0.));
#116364=DIRECTION('',(0.866025403784438,0.5,0.));
#116365=DIRECTION('',(0.,1.,0.));
#116366=DIRECTION('',(-0.866025403784439,0.5,0.));
#116367=DIRECTION('',(-0.866025403784438,-0.5,0.));
#116368=DIRECTION('',(1.87789324842145E-16,-1.,0.));
#116369=DIRECTION('',(0.866025403784438,-0.5,0.));
#116370=DIRECTION('center_axis',(1.,0.,0.));
#116371=DIRECTION('ref_axis',(0.,0.,-1.));
#116372=DIRECTION('',(0.,0.,1.));
#116373=DIRECTION('',(0.,0.,1.));
#116374=DIRECTION('center_axis',(0.5,0.866025403784439,0.));
#116375=DIRECTION('ref_axis',(-0.866025403784439,0.5,0.));
#116376=DIRECTION('',(0.,0.,1.));
#116377=DIRECTION('center_axis',(-0.5,0.866025403784439,0.));
#116378=DIRECTION('ref_axis',(-0.866025403784439,-0.5,0.));
#116379=DIRECTION('',(0.,0.,1.));
#116380=DIRECTION('center_axis',(-1.,-1.87789324842145E-16,0.));
#116381=DIRECTION('ref_axis',(1.87789324842145E-16,-1.,0.));
#116382=DIRECTION('',(0.,0.,1.));
#116383=DIRECTION('center_axis',(-0.5,-0.866025403784439,0.));
#116384=DIRECTION('ref_axis',(0.866025403784439,-0.5,0.));
#116385=DIRECTION('',(0.,0.,1.));
#116386=DIRECTION('center_axis',(0.5,-0.866025403784438,0.));
#116387=DIRECTION('ref_axis',(0.866025403784438,0.5,0.));
#116388=DIRECTION('center_axis',(0.,0.,1.));
#116389=DIRECTION('ref_axis',(0.,1.,0.));
#366325=CARTESIAN_POINT('',(0.,0.,0.));
#366326=CARTESIAN_POINT('Origin',(0.,-7.56339435525888E-14,-9.91875));
#366327=CARTESIAN_POINT('',(-4.89956577852113E-30,-1.17524047358082,-9.6375));
#366328=CARTESIAN_POINT('',(1.43925448419928E-16,-1.17524047358099,-9.64975952641922));
#366329=CARTESIAN_POINT('',(1.43925448419928E-16,-1.17524047358099,-9.91875));
#366330=CARTESIAN_POINT('',(-0.190653686693206,-1.15967294634857,-9.64975952641922));
#366331=CARTESIAN_POINT('Ctrl Pts',(-0.190653686693206,-1.15967294634857,
-9.64975952641922));
#366332=CARTESIAN_POINT('Ctrl Pts',(-0.0959624143348448,-1.17524047358082,
-9.64339282863739));
#366333=CARTESIAN_POINT('Ctrl Pts',(-1.43925448419918E-16,-1.17524047358082,
-9.6375));
#366334=CARTESIAN_POINT('Origin',(-1.87350135405495E-14,6.89726054048379E-14,
-9.6497595264191));
#366335=CARTESIAN_POINT('Origin',(0.,-7.56339435525888E-14,-9.91875));
#366336=CARTESIAN_POINT('',(-4.86875089941093E-30,-1.17524047358082,-9.1375));
#366337=CARTESIAN_POINT('',(-4.86875089941093E-30,-1.17524047358082,-9.2));
#366338=CARTESIAN_POINT('',(1.43925448419928E-16,-1.17524047358099,-9.91875));
#366339=CARTESIAN_POINT('Ctrl Pts',(-1.43925448419918E-16,-1.17524047358082,
-9.6375));
#366340=CARTESIAN_POINT('Ctrl Pts',(0.678525403784435,-1.17524047358082,
-9.59583333333333));
#366341=CARTESIAN_POINT('Ctrl Pts',(1.01778810567665,-0.58762023679041,
-9.55416666666667));
#366342=CARTESIAN_POINT('Ctrl Pts',(1.35705080756887,4.56911366618117E-15,
-9.5125));
#366343=CARTESIAN_POINT('Ctrl Pts',(1.01778810567665,0.587620236790419,
-9.47083333333333));
#366344=CARTESIAN_POINT('Ctrl Pts',(0.678525403784436,1.17524047358083,
-9.42916666666667));
#366345=CARTESIAN_POINT('Ctrl Pts',(0.,1.17524047358083,-9.3875));
#366346=CARTESIAN_POINT('Ctrl Pts',(-0.678525403784435,1.17524047358083,
-9.34583333333333));
#366347=CARTESIAN_POINT('Ctrl Pts',(-1.01778810567665,0.58762023679042,
-9.30416666666667));
#366348=CARTESIAN_POINT('Ctrl Pts',(-1.35705080756887,4.79222133198851E-15,
-9.2625));
#366349=CARTESIAN_POINT('Ctrl Pts',(-1.01778810567665,-0.58762023679041,
-9.22083333333333));
#366350=CARTESIAN_POINT('Ctrl Pts',(-0.678525403784435,-1.17524047358082,
-9.17916666666667));
#366351=CARTESIAN_POINT('Ctrl Pts',(-1.43925448419918E-16,-1.17524047358082,
-9.1375));
#366352=CARTESIAN_POINT('',(0.689217670442765,-0.951929185124572,-9.64975952641917));
#366353=CARTESIAN_POINT('Origin',(-1.87350135405495E-14,6.89726054048379E-14,
-9.6497595264191));
#366354=CARTESIAN_POINT('Ctrl Pts',(0.689217670442765,-0.951929185124572,
-9.64975952641917));
#366355=CARTESIAN_POINT('Ctrl Pts',(0.892378271989736,-0.804836440504912,
-9.63206891898562));
#366356=CARTESIAN_POINT('Ctrl Pts',(1.01778810567665,-0.58762023679041,
-9.61666666666667));
#366357=CARTESIAN_POINT('Ctrl Pts',(1.35705080756887,4.59643214611782E-15,
-9.575));
#366358=CARTESIAN_POINT('Ctrl Pts',(1.01778810567665,0.587620236790419,
-9.53333333333333));
#366359=CARTESIAN_POINT('Ctrl Pts',(0.678525403784436,1.17524047358083,
-9.49166666666667));
#366360=CARTESIAN_POINT('Ctrl Pts',(0.,1.17524047358083,-9.45));
#366361=CARTESIAN_POINT('Ctrl Pts',(-0.678525403784435,1.17524047358083,
-9.40833333333333));
#366362=CARTESIAN_POINT('Ctrl Pts',(-1.01778810567665,0.58762023679042,
-9.36666666666667));
#366363=CARTESIAN_POINT('Ctrl Pts',(-1.35705080756887,4.81953981192516E-15,
-9.325));
#366364=CARTESIAN_POINT('Ctrl Pts',(-1.01778810567665,-0.58762023679041,
-9.28333333333333));
#366365=CARTESIAN_POINT('Ctrl Pts',(-0.678525403784435,-1.17524047358082,
-9.24166666666667));
#366366=CARTESIAN_POINT('Ctrl Pts',(-1.43925448419918E-16,-1.17524047358082,
-9.2));
#366367=CARTESIAN_POINT('Origin',(0.,-7.56339435525888E-14,-9.91875));
#366368=CARTESIAN_POINT('',(-4.86875089941093E-30,-1.17524047358082,-8.6375));
#366369=CARTESIAN_POINT('',(-4.86875089941093E-30,-1.17524047358082,-8.7));
#366370=CARTESIAN_POINT('',(1.43925448419928E-16,-1.17524047358099,-9.91875));
#366371=CARTESIAN_POINT('Ctrl Pts',(-1.43925448419918E-16,-1.17524047358082,
-9.1375));
#366372=CARTESIAN_POINT('Ctrl Pts',(0.678525403784435,-1.17524047358083,
-9.09583333333333));
#366373=CARTESIAN_POINT('Ctrl Pts',(1.01778810567665,-0.587620236790411,
-9.05416666666667));
#366374=CARTESIAN_POINT('Ctrl Pts',(1.35705080756887,4.35056582668803E-15,
-9.0125));
#366375=CARTESIAN_POINT('Ctrl Pts',(1.01778810567665,0.587620236790418,
-8.97083333333333));
#366376=CARTESIAN_POINT('Ctrl Pts',(0.678525403784436,1.17524047358083,
-8.92916666666667));
#366377=CARTESIAN_POINT('Ctrl Pts',(0.,1.17524047358083,-8.8875));
#366378=CARTESIAN_POINT('Ctrl Pts',(-0.678525403784435,1.17524047358083,
-8.84583333333333));
#366379=CARTESIAN_POINT('Ctrl Pts',(-1.01778810567665,0.587620236790419,
-8.80416666666667));
#366380=CARTESIAN_POINT('Ctrl Pts',(-1.35705080756887,4.57367349249537E-15,
-8.7625));
#366381=CARTESIAN_POINT('Ctrl Pts',(-1.01778810567665,-0.58762023679041,
-8.72083333333333));
#366382=CARTESIAN_POINT('Ctrl Pts',(-0.678525403784435,-1.17524047358082,
-8.67916666666667));
#366383=CARTESIAN_POINT('Ctrl Pts',(-1.43925448419918E-16,-1.17524047358082,
-8.6375));
#366384=CARTESIAN_POINT('Ctrl Pts',(-1.43925448419918E-16,-1.17524047358082,
-9.2));
#366385=CARTESIAN_POINT('Ctrl Pts',(0.678525403784435,-1.17524047358083,
-9.15833333333333));
#366386=CARTESIAN_POINT('Ctrl Pts',(1.01778810567665,-0.587620236790411,
-9.11666666666667));
#366387=CARTESIAN_POINT('Ctrl Pts',(1.35705080756887,4.37788430662468E-15,
-9.075));
#366388=CARTESIAN_POINT('Ctrl Pts',(1.01778810567665,0.587620236790418,
-9.03333333333333));
#366389=CARTESIAN_POINT('Ctrl Pts',(0.678525403784436,1.17524047358083,
-8.99166666666667));
#366390=CARTESIAN_POINT('Ctrl Pts',(0.,1.17524047358083,-8.95));
#366391=CARTESIAN_POINT('Ctrl Pts',(-0.678525403784435,1.17524047358083,
-8.90833333333333));
#366392=CARTESIAN_POINT('Ctrl Pts',(-1.01778810567665,0.587620236790419,
-8.86666666666667));
#366393=CARTESIAN_POINT('Ctrl Pts',(-1.35705080756887,4.60099197243202E-15,
-8.825));
#366394=CARTESIAN_POINT('Ctrl Pts',(-1.01778810567665,-0.58762023679041,
-8.78333333333333));
#366395=CARTESIAN_POINT('Ctrl Pts',(-0.678525403784435,-1.17524047358082,
-8.74166666666667));
#366396=CARTESIAN_POINT('Ctrl Pts',(-1.43925448419918E-16,-1.17524047358082,
-8.7));
#366397=CARTESIAN_POINT('Origin',(0.,-7.56339435525888E-14,-9.91875));
#366398=CARTESIAN_POINT('',(-4.86875089941093E-30,-1.17524047358083,-8.1375));
#366399=CARTESIAN_POINT('',(-4.86875089941093E-30,-1.17524047358083,-8.2));
#366400=CARTESIAN_POINT('',(1.43925448419928E-16,-1.17524047358099,-9.91875));
#366401=CARTESIAN_POINT('Ctrl Pts',(-1.43925448419918E-16,-1.17524047358082,
-8.6375));
#366402=CARTESIAN_POINT('Ctrl Pts',(0.678525403784435,-1.17524047358083,
-8.59583333333333));
#366403=CARTESIAN_POINT('Ctrl Pts',(1.01778810567665,-0.587620236790411,
-8.55416666666667));
#366404=CARTESIAN_POINT('Ctrl Pts',(1.35705080756887,4.13201798719489E-15,
-8.5125));
#366405=CARTESIAN_POINT('Ctrl Pts',(1.01778810567665,0.587620236790418,
-8.47083333333333));
#366406=CARTESIAN_POINT('Ctrl Pts',(0.678525403784436,1.17524047358083,
-8.42916666666667));
#366407=CARTESIAN_POINT('Ctrl Pts',(0.,1.17524047358083,-8.3875));
#366408=CARTESIAN_POINT('Ctrl Pts',(-0.678525403784435,1.17524047358083,
-8.34583333333333));
#366409=CARTESIAN_POINT('Ctrl Pts',(-1.01778810567665,0.587620236790419,
-8.30416666666667));
#366410=CARTESIAN_POINT('Ctrl Pts',(-1.35705080756887,4.35512565300223E-15,
-8.2625));
#366411=CARTESIAN_POINT('Ctrl Pts',(-1.01778810567665,-0.58762023679041,
-8.22083333333333));
#366412=CARTESIAN_POINT('Ctrl Pts',(-0.678525403784435,-1.17524047358082,
-8.17916666666667));
#366413=CARTESIAN_POINT('Ctrl Pts',(-1.43925448419918E-16,-1.17524047358083,
-8.1375));
#366414=CARTESIAN_POINT('Ctrl Pts',(-1.43925448419918E-16,-1.17524047358082,
-8.7));
#366415=CARTESIAN_POINT('Ctrl Pts',(0.678525403784435,-1.17524047358083,
-8.65833333333333));
#366416=CARTESIAN_POINT('Ctrl Pts',(1.01778810567665,-0.587620236790411,
-8.61666666666667));
#366417=CARTESIAN_POINT('Ctrl Pts',(1.35705080756887,4.15933646713154E-15,
-8.575));
#366418=CARTESIAN_POINT('Ctrl Pts',(1.01778810567665,0.587620236790418,
-8.53333333333333));
#366419=CARTESIAN_POINT('Ctrl Pts',(0.678525403784436,1.17524047358083,
-8.49166666666667));
#366420=CARTESIAN_POINT('Ctrl Pts',(0.,1.17524047358083,-8.45));
#366421=CARTESIAN_POINT('Ctrl Pts',(-0.678525403784435,1.17524047358083,
-8.40833333333333));
#366422=CARTESIAN_POINT('Ctrl Pts',(-1.01778810567665,0.587620236790419,
-8.36666666666667));
#366423=CARTESIAN_POINT('Ctrl Pts',(-1.35705080756887,4.38244413293887E-15,
-8.325));
#366424=CARTESIAN_POINT('Ctrl Pts',(-1.01778810567665,-0.58762023679041,
-8.28333333333333));
#366425=CARTESIAN_POINT('Ctrl Pts',(-0.678525403784435,-1.17524047358082,
-8.24166666666667));
#366426=CARTESIAN_POINT('Ctrl Pts',(-1.43925448419918E-16,-1.17524047358083,
-8.2));
#366427=CARTESIAN_POINT('Origin',(0.,-7.56339435525888E-14,-9.91875));
#366428=CARTESIAN_POINT('',(-4.83793602030074E-30,-1.17524047358083,-7.6375));
#366429=CARTESIAN_POINT('',(-4.83793602030074E-30,-1.17524047358083,-7.7));
#366430=CARTESIAN_POINT('',(1.43925448419928E-16,-1.17524047358099,-9.91875));
#366431=CARTESIAN_POINT('Ctrl Pts',(-1.43925448419918E-16,-1.17524047358083,
-8.1375));
#366432=CARTESIAN_POINT('Ctrl Pts',(0.678525403784435,-1.17524047358083,
-8.09583333333333));
#366433=CARTESIAN_POINT('Ctrl Pts',(1.01778810567665,-0.587620236790411,
-8.05416666666667));
#366434=CARTESIAN_POINT('Ctrl Pts',(1.35705080756887,3.91347014770175E-15,
-8.0125));
#366435=CARTESIAN_POINT('Ctrl Pts',(1.01778810567665,0.587620236790418,
-7.97083333333333));
#366436=CARTESIAN_POINT('Ctrl Pts',(0.678525403784436,1.17524047358083,
-7.92916666666667));
#366437=CARTESIAN_POINT('Ctrl Pts',(0.,1.17524047358083,-7.8875));
#366438=CARTESIAN_POINT('Ctrl Pts',(-0.678525403784435,1.17524047358083,
-7.84583333333333));
#366439=CARTESIAN_POINT('Ctrl Pts',(-1.01778810567665,0.587620236790419,
-7.80416666666667));
#366440=CARTESIAN_POINT('Ctrl Pts',(-1.35705080756887,4.13657781350909E-15,
-7.7625));
#366441=CARTESIAN_POINT('Ctrl Pts',(-1.01778810567665,-0.58762023679041,
-7.72083333333333));
#366442=CARTESIAN_POINT('Ctrl Pts',(-0.678525403784435,-1.17524047358083,
-7.67916666666667));
#366443=CARTESIAN_POINT('Ctrl Pts',(-1.43925448419918E-16,-1.17524047358083,
-7.6375));
#366444=CARTESIAN_POINT('Ctrl Pts',(-1.43925448419918E-16,-1.17524047358083,
-8.2));
#366445=CARTESIAN_POINT('Ctrl Pts',(0.678525403784435,-1.17524047358083,
-8.15833333333333));
#366446=CARTESIAN_POINT('Ctrl Pts',(1.01778810567665,-0.587620236790411,
-8.11666666666667));
#366447=CARTESIAN_POINT('Ctrl Pts',(1.35705080756887,3.94078862763839E-15,
-8.075));
#366448=CARTESIAN_POINT('Ctrl Pts',(1.01778810567665,0.587620236790418,
-8.03333333333333));
#366449=CARTESIAN_POINT('Ctrl Pts',(0.678525403784436,1.17524047358083,
-7.99166666666667));
#366450=CARTESIAN_POINT('Ctrl Pts',(0.,1.17524047358083,-7.95));
#366451=CARTESIAN_POINT('Ctrl Pts',(-0.678525403784435,1.17524047358083,
-7.90833333333333));
#366452=CARTESIAN_POINT('Ctrl Pts',(-1.01778810567665,0.587620236790419,
-7.86666666666667));
#366453=CARTESIAN_POINT('Ctrl Pts',(-1.35705080756887,4.16389629344573E-15,
-7.825));
#366454=CARTESIAN_POINT('Ctrl Pts',(-1.01778810567665,-0.58762023679041,
-7.78333333333333));
#366455=CARTESIAN_POINT('Ctrl Pts',(-0.678525403784435,-1.17524047358083,
-7.74166666666667));
#366456=CARTESIAN_POINT('Ctrl Pts',(-1.43925448419918E-16,-1.17524047358083,
-7.7));
#366457=CARTESIAN_POINT('Origin',(0.,-7.56339435525888E-14,-9.91875));
#366458=CARTESIAN_POINT('',(-4.83793602030074E-30,-1.17524047358083,-7.1375));
#366459=CARTESIAN_POINT('',(-4.83793602030074E-30,-1.17524047358083,-7.2));
#366460=CARTESIAN_POINT('',(1.43925448419928E-16,-1.17524047358099,-9.91875));
#366461=CARTESIAN_POINT('Ctrl Pts',(-1.43925448419918E-16,-1.17524047358083,
-7.6375));
#366462=CARTESIAN_POINT('Ctrl Pts',(0.678525403784435,-1.17524047358083,
-7.59583333333333));
#366463=CARTESIAN_POINT('Ctrl Pts',(1.01778810567665,-0.587620236790411,
-7.55416666666667));
#366464=CARTESIAN_POINT('Ctrl Pts',(1.35705080756887,3.69492230820861E-15,
-7.5125));
#366465=CARTESIAN_POINT('Ctrl Pts',(1.01778810567665,0.587620236790418,
-7.47083333333333));
#366466=CARTESIAN_POINT('Ctrl Pts',(0.678525403784436,1.17524047358083,
-7.42916666666667));
#366467=CARTESIAN_POINT('Ctrl Pts',(0.,1.17524047358083,-7.3875));
#366468=CARTESIAN_POINT('Ctrl Pts',(-0.678525403784435,1.17524047358083,
-7.34583333333333));
#366469=CARTESIAN_POINT('Ctrl Pts',(-1.01778810567665,0.587620236790419,
-7.30416666666667));
#366470=CARTESIAN_POINT('Ctrl Pts',(-1.35705080756887,3.91802997401595E-15,
-7.2625));
#366471=CARTESIAN_POINT('Ctrl Pts',(-1.01778810567665,-0.587620236790411,
-7.22083333333333));
#366472=CARTESIAN_POINT('Ctrl Pts',(-0.678525403784435,-1.17524047358083,
-7.17916666666667));
#366473=CARTESIAN_POINT('Ctrl Pts',(-1.43925448419918E-16,-1.17524047358083,
-7.1375));
#366474=CARTESIAN_POINT('Ctrl Pts',(-1.43925448419918E-16,-1.17524047358083,
-7.7));
#366475=CARTESIAN_POINT('Ctrl Pts',(0.678525403784435,-1.17524047358083,
-7.65833333333333));
#366476=CARTESIAN_POINT('Ctrl Pts',(1.01778810567665,-0.587620236790411,
-7.61666666666667));
#366477=CARTESIAN_POINT('Ctrl Pts',(1.35705080756887,3.72224078814525E-15,
-7.575));
#366478=CARTESIAN_POINT('Ctrl Pts',(1.01778810567665,0.587620236790418,
-7.53333333333333));
#366479=CARTESIAN_POINT('Ctrl Pts',(0.678525403784436,1.17524047358083,
-7.49166666666667));
#366480=CARTESIAN_POINT('Ctrl Pts',(0.,1.17524047358083,-7.45));
#366481=CARTESIAN_POINT('Ctrl Pts',(-0.678525403784435,1.17524047358083,
-7.40833333333333));
#366482=CARTESIAN_POINT('Ctrl Pts',(-1.01778810567665,0.587620236790419,
-7.36666666666667));
#366483=CARTESIAN_POINT('Ctrl Pts',(-1.35705080756887,3.94534845395259E-15,
-7.325));
#366484=CARTESIAN_POINT('Ctrl Pts',(-1.01778810567665,-0.587620236790411,
-7.28333333333333));
#366485=CARTESIAN_POINT('Ctrl Pts',(-0.678525403784435,-1.17524047358083,
-7.24166666666667));
#366486=CARTESIAN_POINT('Ctrl Pts',(-1.43925448419918E-16,-1.17524047358083,
-7.2));
#366487=CARTESIAN_POINT('Origin',(0.,-7.56339435525888E-14,-9.91875));
#366488=CARTESIAN_POINT('',(-4.80712114119054E-30,-1.17524047358083,-6.6375));
#366489=CARTESIAN_POINT('',(-4.80712114119054E-30,-1.17524047358083,-6.7));
#366490=CARTESIAN_POINT('',(1.43925448419928E-16,-1.17524047358099,-9.91875));
#366491=CARTESIAN_POINT('Ctrl Pts',(-1.43925448419918E-16,-1.17524047358083,
-7.1375));
#366492=CARTESIAN_POINT('Ctrl Pts',(0.678525403784435,-1.17524047358083,
-7.09583333333333));
#366493=CARTESIAN_POINT('Ctrl Pts',(1.01778810567665,-0.587620236790411,
-7.05416666666667));
#366494=CARTESIAN_POINT('Ctrl Pts',(1.35705080756887,3.47637446871547E-15,
-7.0125));
#366495=CARTESIAN_POINT('Ctrl Pts',(1.01778810567665,0.587620236790417,
-6.97083333333333));
#366496=CARTESIAN_POINT('Ctrl Pts',(0.678525403784436,1.17524047358083,
-6.92916666666667));
#366497=CARTESIAN_POINT('Ctrl Pts',(0.,1.17524047358083,-6.8875));
#366498=CARTESIAN_POINT('Ctrl Pts',(-0.678525403784435,1.17524047358083,
-6.84583333333333));
#366499=CARTESIAN_POINT('Ctrl Pts',(-1.01778810567665,0.587620236790418,
-6.80416666666667));
#366500=CARTESIAN_POINT('Ctrl Pts',(-1.35705080756887,3.69948213452281E-15,
-6.7625));
#366501=CARTESIAN_POINT('Ctrl Pts',(-1.01778810567665,-0.587620236790411,
-6.72083333333333));
#366502=CARTESIAN_POINT('Ctrl Pts',(-0.678525403784435,-1.17524047358083,
-6.67916666666667));
#366503=CARTESIAN_POINT('Ctrl Pts',(-1.43925448419918E-16,-1.17524047358083,
-6.6375));
#366504=CARTESIAN_POINT('Ctrl Pts',(-1.43925448419918E-16,-1.17524047358083,
-7.2));
#366505=CARTESIAN_POINT('Ctrl Pts',(0.678525403784435,-1.17524047358083,
-7.15833333333333));
#366506=CARTESIAN_POINT('Ctrl Pts',(1.01778810567665,-0.587620236790411,
-7.11666666666667));
#366507=CARTESIAN_POINT('Ctrl Pts',(1.35705080756887,3.50369294865211E-15,
-7.075));
#366508=CARTESIAN_POINT('Ctrl Pts',(1.01778810567665,0.587620236790417,
-7.03333333333333));
#366509=CARTESIAN_POINT('Ctrl Pts',(0.678525403784436,1.17524047358083,
-6.99166666666667));
#366510=CARTESIAN_POINT('Ctrl Pts',(0.,1.17524047358083,-6.95));
#366511=CARTESIAN_POINT('Ctrl Pts',(-0.678525403784435,1.17524047358083,
-6.90833333333333));
#366512=CARTESIAN_POINT('Ctrl Pts',(-1.01778810567665,0.587620236790418,
-6.86666666666667));
#366513=CARTESIAN_POINT('Ctrl Pts',(-1.35705080756887,3.72680061445945E-15,
-6.825));
#366514=CARTESIAN_POINT('Ctrl Pts',(-1.01778810567665,-0.587620236790411,
-6.78333333333333));
#366515=CARTESIAN_POINT('Ctrl Pts',(-0.678525403784435,-1.17524047358083,
-6.74166666666667));
#366516=CARTESIAN_POINT('Ctrl Pts',(-1.43925448419918E-16,-1.17524047358083,
-6.7));
#366517=CARTESIAN_POINT('Origin',(0.,-7.56339435525888E-14,-9.91875));
#366518=CARTESIAN_POINT('',(-4.80712114119054E-30,-1.17524047358083,-6.1375));
#366519=CARTESIAN_POINT('',(-4.80712114119054E-30,-1.17524047358083,-6.2));
#366520=CARTESIAN_POINT('',(1.43925448419928E-16,-1.17524047358099,-9.91875));
#366521=CARTESIAN_POINT('Ctrl Pts',(-1.43925448419918E-16,-1.17524047358083,
-6.6375));
#366522=CARTESIAN_POINT('Ctrl Pts',(0.678525403784435,-1.17524047358083,
-6.59583333333333));
#366523=CARTESIAN_POINT('Ctrl Pts',(1.01778810567665,-0.587620236790412,
-6.55416666666667));
#366524=CARTESIAN_POINT('Ctrl Pts',(1.35705080756887,3.25782662922233E-15,
-6.5125));
#366525=CARTESIAN_POINT('Ctrl Pts',(1.01778810567665,0.587620236790417,
-6.47083333333333));
#366526=CARTESIAN_POINT('Ctrl Pts',(0.678525403784436,1.17524047358083,
-6.42916666666667));
#366527=CARTESIAN_POINT('Ctrl Pts',(0.,1.17524047358083,-6.3875));
#366528=CARTESIAN_POINT('Ctrl Pts',(-0.678525403784435,1.17524047358083,
-6.34583333333333));
#366529=CARTESIAN_POINT('Ctrl Pts',(-1.01778810567665,0.587620236790418,
-6.30416666666667));
#366530=CARTESIAN_POINT('Ctrl Pts',(-1.35705080756887,3.48093429502967E-15,
-6.2625));
#366531=CARTESIAN_POINT('Ctrl Pts',(-1.01778810567665,-0.587620236790411,
-6.22083333333333));
#366532=CARTESIAN_POINT('Ctrl Pts',(-0.678525403784435,-1.17524047358083,
-6.17916666666667));
#366533=CARTESIAN_POINT('Ctrl Pts',(-1.43925448419918E-16,-1.17524047358083,
-6.1375));
#366534=CARTESIAN_POINT('Ctrl Pts',(-1.43925448419918E-16,-1.17524047358083,
-6.7));
#366535=CARTESIAN_POINT('Ctrl Pts',(0.678525403784435,-1.17524047358083,
-6.65833333333333));
#366536=CARTESIAN_POINT('Ctrl Pts',(1.01778810567665,-0.587620236790412,
-6.61666666666667));
#366537=CARTESIAN_POINT('Ctrl Pts',(1.35705080756887,3.28514510915897E-15,
-6.575));
#366538=CARTESIAN_POINT('Ctrl Pts',(1.01778810567665,0.587620236790417,
-6.53333333333333));
#366539=CARTESIAN_POINT('Ctrl Pts',(0.678525403784436,1.17524047358083,
-6.49166666666667));
#366540=CARTESIAN_POINT('Ctrl Pts',(0.,1.17524047358083,-6.45));
#366541=CARTESIAN_POINT('Ctrl Pts',(-0.678525403784435,1.17524047358083,
-6.40833333333334));
#366542=CARTESIAN_POINT('Ctrl Pts',(-1.01778810567665,0.587620236790418,
-6.36666666666667));
#366543=CARTESIAN_POINT('Ctrl Pts',(-1.35705080756887,3.50825277496631E-15,
-6.325));
#366544=CARTESIAN_POINT('Ctrl Pts',(-1.01778810567665,-0.587620236790411,
-6.28333333333333));
#366545=CARTESIAN_POINT('Ctrl Pts',(-0.678525403784435,-1.17524047358083,
-6.24166666666667));
#366546=CARTESIAN_POINT('Ctrl Pts',(-1.43925448419918E-16,-1.17524047358083,
-6.2));
#366547=CARTESIAN_POINT('Origin',(0.,-7.56339435525888E-14,-9.91875));
#366548=CARTESIAN_POINT('',(-4.77630626208034E-30,-1.17524047358083,-5.6375));
#366549=CARTESIAN_POINT('',(-4.77630626208034E-30,-1.17524047358083,-5.7));
#366550=CARTESIAN_POINT('',(1.43925448419928E-16,-1.17524047358099,-9.91875));
#366551=CARTESIAN_POINT('Ctrl Pts',(-1.43925448419918E-16,-1.17524047358083,
-6.1375));
#366552=CARTESIAN_POINT('Ctrl Pts',(0.678525403784435,-1.17524047358083,
-6.09583333333333));
#366553=CARTESIAN_POINT('Ctrl Pts',(1.01778810567665,-0.587620236790412,
-6.05416666666667));
#366554=CARTESIAN_POINT('Ctrl Pts',(1.35705080756887,3.03927878972919E-15,
-6.0125));
#366555=CARTESIAN_POINT('Ctrl Pts',(1.01778810567665,0.587620236790417,
-5.97083333333333));
#366556=CARTESIAN_POINT('Ctrl Pts',(0.678525403784436,1.17524047358083,
-5.92916666666667));
#366557=CARTESIAN_POINT('Ctrl Pts',(0.,1.17524047358083,-5.8875));
#366558=CARTESIAN_POINT('Ctrl Pts',(-0.678525403784435,1.17524047358083,
-5.84583333333333));
#366559=CARTESIAN_POINT('Ctrl Pts',(-1.01778810567665,0.587620236790418,
-5.80416666666667));
#366560=CARTESIAN_POINT('Ctrl Pts',(-1.35705080756887,3.26238645553653E-15,
-5.7625));
#366561=CARTESIAN_POINT('Ctrl Pts',(-1.01778810567665,-0.587620236790411,
-5.72083333333333));
#366562=CARTESIAN_POINT('Ctrl Pts',(-0.678525403784435,-1.17524047358083,
-5.67916666666667));
#366563=CARTESIAN_POINT('Ctrl Pts',(-1.43925448419918E-16,-1.17524047358083,
-5.6375));
#366564=CARTESIAN_POINT('Ctrl Pts',(-1.43925448419918E-16,-1.17524047358083,
-6.2));
#366565=CARTESIAN_POINT('Ctrl Pts',(0.678525403784435,-1.17524047358083,
-6.15833333333333));
#366566=CARTESIAN_POINT('Ctrl Pts',(1.01778810567665,-0.587620236790412,
-6.11666666666667));
#366567=CARTESIAN_POINT('Ctrl Pts',(1.35705080756887,3.06659726966583E-15,
-6.075));
#366568=CARTESIAN_POINT('Ctrl Pts',(1.01778810567665,0.587620236790417,
-6.03333333333333));
#366569=CARTESIAN_POINT('Ctrl Pts',(0.678525403784436,1.17524047358083,
-5.99166666666667));
#366570=CARTESIAN_POINT('Ctrl Pts',(0.,1.17524047358083,-5.95));
#366571=CARTESIAN_POINT('Ctrl Pts',(-0.678525403784435,1.17524047358083,
-5.90833333333333));
#366572=CARTESIAN_POINT('Ctrl Pts',(-1.01778810567665,0.587620236790418,
-5.86666666666667));
#366573=CARTESIAN_POINT('Ctrl Pts',(-1.35705080756887,3.28970493547317E-15,
-5.825));
#366574=CARTESIAN_POINT('Ctrl Pts',(-1.01778810567665,-0.587620236790411,
-5.78333333333333));
#366575=CARTESIAN_POINT('Ctrl Pts',(-0.678525403784435,-1.17524047358083,
-5.74166666666667));
#366576=CARTESIAN_POINT('Ctrl Pts',(-1.43925448419918E-16,-1.17524047358083,
-5.7));
#366577=CARTESIAN_POINT('Origin',(0.,-7.56339435525888E-14,-9.91875));
#366578=CARTESIAN_POINT('',(-4.77630626208034E-30,-1.17524047358083,-5.1375));
#366579=CARTESIAN_POINT('',(-4.77630626208034E-30,-1.17524047358083,-5.2));
#366580=CARTESIAN_POINT('',(1.43925448419928E-16,-1.17524047358099,-9.91875));
#366581=CARTESIAN_POINT('Ctrl Pts',(-1.43925448419918E-16,-1.17524047358083,
-5.6375));
#366582=CARTESIAN_POINT('Ctrl Pts',(0.678525403784435,-1.17524047358083,
-5.59583333333333));
#366583=CARTESIAN_POINT('Ctrl Pts',(1.01778810567665,-0.587620236790412,
-5.55416666666667));
#366584=CARTESIAN_POINT('Ctrl Pts',(1.35705080756887,2.82073095023605E-15,
-5.5125));
#366585=CARTESIAN_POINT('Ctrl Pts',(1.01778810567665,0.587620236790417,
-5.47083333333333));
#366586=CARTESIAN_POINT('Ctrl Pts',(0.678525403784436,1.17524047358083,
-5.42916666666667));
#366587=CARTESIAN_POINT('Ctrl Pts',(0.,1.17524047358083,-5.3875));
#366588=CARTESIAN_POINT('Ctrl Pts',(-0.678525403784435,1.17524047358083,
-5.34583333333333));
#366589=CARTESIAN_POINT('Ctrl Pts',(-1.01778810567665,0.587620236790418,
-5.30416666666667));
#366590=CARTESIAN_POINT('Ctrl Pts',(-1.35705080756887,3.04383861604338E-15,
-5.2625));
#366591=CARTESIAN_POINT('Ctrl Pts',(-1.01778810567665,-0.587620236790411,
-5.22083333333333));
#366592=CARTESIAN_POINT('Ctrl Pts',(-0.678525403784435,-1.17524047358083,
-5.17916666666667));
#366593=CARTESIAN_POINT('Ctrl Pts',(-1.43925448419918E-16,-1.17524047358083,
-5.1375));
#366594=CARTESIAN_POINT('Ctrl Pts',(-1.43925448419918E-16,-1.17524047358083,
-5.7));
#366595=CARTESIAN_POINT('Ctrl Pts',(0.678525403784435,-1.17524047358083,
-5.65833333333333));
#366596=CARTESIAN_POINT('Ctrl Pts',(1.01778810567665,-0.587620236790412,
-5.61666666666667));
#366597=CARTESIAN_POINT('Ctrl Pts',(1.35705080756887,2.84804943017269E-15,
-5.575));
#366598=CARTESIAN_POINT('Ctrl Pts',(1.01778810567665,0.587620236790417,
-5.53333333333333));
#366599=CARTESIAN_POINT('Ctrl Pts',(0.678525403784436,1.17524047358083,
-5.49166666666667));
#366600=CARTESIAN_POINT('Ctrl Pts',(0.,1.17524047358083,-5.45));
#366601=CARTESIAN_POINT('Ctrl Pts',(-0.678525403784435,1.17524047358083,
-5.40833333333333));
#366602=CARTESIAN_POINT('Ctrl Pts',(-1.01778810567665,0.587620236790418,
-5.36666666666667));
#366603=CARTESIAN_POINT('Ctrl Pts',(-1.35705080756887,3.07115709598003E-15,
-5.325));
#366604=CARTESIAN_POINT('Ctrl Pts',(-1.01778810567665,-0.587620236790411,
-5.28333333333333));
#366605=CARTESIAN_POINT('Ctrl Pts',(-0.678525403784435,-1.17524047358083,
-5.24166666666667));
#366606=CARTESIAN_POINT('Ctrl Pts',(-1.43925448419918E-16,-1.17524047358083,
-5.2));
#366607=CARTESIAN_POINT('Origin',(0.,-7.56339435525888E-14,-9.91875));
#366608=CARTESIAN_POINT('',(-4.74549138297015E-30,-1.17524047358083,-4.6375));
#366609=CARTESIAN_POINT('',(-4.74549138297015E-30,-1.17524047358083,-4.7));
#366610=CARTESIAN_POINT('',(1.43925448419928E-16,-1.17524047358099,-9.91875));
#366611=CARTESIAN_POINT('Ctrl Pts',(-1.43925448419918E-16,-1.17524047358083,
-5.1375));
#366612=CARTESIAN_POINT('Ctrl Pts',(0.678525403784435,-1.17524047358083,
-5.09583333333333));
#366613=CARTESIAN_POINT('Ctrl Pts',(1.01778810567665,-0.587620236790412,
-5.05416666666667));
#366614=CARTESIAN_POINT('Ctrl Pts',(1.35705080756887,2.6021831107429E-15,
-5.0125));
#366615=CARTESIAN_POINT('Ctrl Pts',(1.01778810567665,0.587620236790417,
-4.97083333333333));
#366616=CARTESIAN_POINT('Ctrl Pts',(0.678525403784436,1.17524047358083,
-4.92916666666667));
#366617=CARTESIAN_POINT('Ctrl Pts',(0.,1.17524047358083,-4.8875));
#366618=CARTESIAN_POINT('Ctrl Pts',(-0.678525403784435,1.17524047358083,
-4.84583333333333));
#366619=CARTESIAN_POINT('Ctrl Pts',(-1.01778810567665,0.587620236790418,
-4.80416666666667));
#366620=CARTESIAN_POINT('Ctrl Pts',(-1.35705080756887,2.82529077655024E-15,
-4.7625));
#366621=CARTESIAN_POINT('Ctrl Pts',(-1.01778810567665,-0.587620236790412,
-4.72083333333333));
#366622=CARTESIAN_POINT('Ctrl Pts',(-0.678525403784435,-1.17524047358083,
-4.67916666666667));
#366623=CARTESIAN_POINT('Ctrl Pts',(-1.43925448419918E-16,-1.17524047358083,
-4.6375));
#366624=CARTESIAN_POINT('Ctrl Pts',(-1.43925448419918E-16,-1.17524047358083,
-5.2));
#366625=CARTESIAN_POINT('Ctrl Pts',(0.678525403784435,-1.17524047358083,
-5.15833333333333));
#366626=CARTESIAN_POINT('Ctrl Pts',(1.01778810567665,-0.587620236790412,
-5.11666666666667));
#366627=CARTESIAN_POINT('Ctrl Pts',(1.35705080756887,2.62950159067955E-15,
-5.075));
#366628=CARTESIAN_POINT('Ctrl Pts',(1.01778810567665,0.587620236790417,
-5.03333333333333));
#366629=CARTESIAN_POINT('Ctrl Pts',(0.678525403784436,1.17524047358083,
-4.99166666666667));
#366630=CARTESIAN_POINT('Ctrl Pts',(0.,1.17524047358083,-4.95));
#366631=CARTESIAN_POINT('Ctrl Pts',(-0.678525403784435,1.17524047358083,
-4.90833333333333));
#366632=CARTESIAN_POINT('Ctrl Pts',(-1.01778810567665,0.587620236790418,
-4.86666666666667));
#366633=CARTESIAN_POINT('Ctrl Pts',(-1.35705080756887,2.85260925648689E-15,
-4.825));
#366634=CARTESIAN_POINT('Ctrl Pts',(-1.01778810567665,-0.587620236790412,
-4.78333333333333));
#366635=CARTESIAN_POINT('Ctrl Pts',(-0.678525403784435,-1.17524047358083,
-4.74166666666667));
#366636=CARTESIAN_POINT('Ctrl Pts',(-1.43925448419918E-16,-1.17524047358083,
-4.7));
#366637=CARTESIAN_POINT('Origin',(0.,-7.56339435525888E-14,-9.91875));
#366638=CARTESIAN_POINT('',(-4.74549138297015E-30,-1.17524047358083,-4.1375));
#366639=CARTESIAN_POINT('',(-4.74549138297015E-30,-1.17524047358083,-4.2));
#366640=CARTESIAN_POINT('',(1.43925448419928E-16,-1.17524047358099,-9.91875));
#366641=CARTESIAN_POINT('Ctrl Pts',(-1.43925448419918E-16,-1.17524047358083,
-4.6375));
#366642=CARTESIAN_POINT('Ctrl Pts',(0.678525403784435,-1.17524047358083,
-4.59583333333333));
#366643=CARTESIAN_POINT('Ctrl Pts',(1.01778810567665,-0.587620236790413,
-4.55416666666667));
#366644=CARTESIAN_POINT('Ctrl Pts',(1.35705080756887,2.38363527124976E-15,
-4.5125));
#366645=CARTESIAN_POINT('Ctrl Pts',(1.01778810567665,0.587620236790416,
-4.47083333333333));
#366646=CARTESIAN_POINT('Ctrl Pts',(0.678525403784436,1.17524047358083,
-4.42916666666667));
#366647=CARTESIAN_POINT('Ctrl Pts',(0.,1.17524047358083,-4.3875));
#366648=CARTESIAN_POINT('Ctrl Pts',(-0.678525403784435,1.17524047358083,
-4.34583333333333));
#366649=CARTESIAN_POINT('Ctrl Pts',(-1.01778810567665,0.587620236790417,
-4.30416666666667));
#366650=CARTESIAN_POINT('Ctrl Pts',(-1.35705080756887,2.6067429370571E-15,
-4.2625));
#366651=CARTESIAN_POINT('Ctrl Pts',(-1.01778810567665,-0.587620236790412,
-4.22083333333333));
#366652=CARTESIAN_POINT('Ctrl Pts',(-0.678525403784435,-1.17524047358083,
-4.17916666666667));
#366653=CARTESIAN_POINT('Ctrl Pts',(-1.43925448419918E-16,-1.17524047358083,
-4.1375));
#366654=CARTESIAN_POINT('Ctrl Pts',(-1.43925448419918E-16,-1.17524047358083,
-4.7));
#366655=CARTESIAN_POINT('Ctrl Pts',(0.678525403784435,-1.17524047358083,
-4.65833333333333));
#366656=CARTESIAN_POINT('Ctrl Pts',(1.01778810567665,-0.587620236790413,
-4.61666666666667));
#366657=CARTESIAN_POINT('Ctrl Pts',(1.35705080756887,2.41095375118641E-15,
-4.575));
#366658=CARTESIAN_POINT('Ctrl Pts',(1.01778810567665,0.587620236790416,
-4.53333333333333));
#366659=CARTESIAN_POINT('Ctrl Pts',(0.678525403784436,1.17524047358083,
-4.49166666666667));
#366660=CARTESIAN_POINT('Ctrl Pts',(0.,1.17524047358083,-4.45));
#366661=CARTESIAN_POINT('Ctrl Pts',(-0.678525403784435,1.17524047358083,
-4.40833333333333));
#366662=CARTESIAN_POINT('Ctrl Pts',(-1.01778810567665,0.587620236790417,
-4.36666666666667));
#366663=CARTESIAN_POINT('Ctrl Pts',(-1.35705080756887,2.63406141699374E-15,
-4.325));
#366664=CARTESIAN_POINT('Ctrl Pts',(-1.01778810567665,-0.587620236790412,
-4.28333333333333));
#366665=CARTESIAN_POINT('Ctrl Pts',(-0.678525403784435,-1.17524047358083,
-4.24166666666667));
#366666=CARTESIAN_POINT('Ctrl Pts',(-1.43925448419918E-16,-1.17524047358083,
-4.2));
#366667=CARTESIAN_POINT('Origin',(0.,-7.56339435525888E-14,-9.91875));
#366668=CARTESIAN_POINT('',(-4.74549138297015E-30,-1.17524047358083,-3.6375));
#366669=CARTESIAN_POINT('',(-4.74549138297015E-30,-1.17524047358083,-3.7));
#366670=CARTESIAN_POINT('',(1.43925448419928E-16,-1.17524047358099,-9.91875));
#366671=CARTESIAN_POINT('Ctrl Pts',(-1.43925448419918E-16,-1.17524047358083,
-4.1375));
#366672=CARTESIAN_POINT('Ctrl Pts',(0.678525403784435,-1.17524047358083,
-4.09583333333333));
#366673=CARTESIAN_POINT('Ctrl Pts',(1.01778810567665,-0.587620236790413,
-4.05416666666667));
#366674=CARTESIAN_POINT('Ctrl Pts',(1.35705080756887,2.16508743175662E-15,
-4.0125));
#366675=CARTESIAN_POINT('Ctrl Pts',(1.01778810567665,0.587620236790416,
-3.97083333333333));
#366676=CARTESIAN_POINT('Ctrl Pts',(0.678525403784436,1.17524047358083,
-3.92916666666667));
#366677=CARTESIAN_POINT('Ctrl Pts',(0.,1.17524047358083,-3.8875));
#366678=CARTESIAN_POINT('Ctrl Pts',(-0.678525403784435,1.17524047358083,
-3.84583333333333));
#366679=CARTESIAN_POINT('Ctrl Pts',(-1.01778810567665,0.587620236790417,
-3.80416666666667));
#366680=CARTESIAN_POINT('Ctrl Pts',(-1.35705080756887,2.38819509756396E-15,
-3.7625));
#366681=CARTESIAN_POINT('Ctrl Pts',(-1.01778810567665,-0.587620236790412,
-3.72083333333333));
#366682=CARTESIAN_POINT('Ctrl Pts',(-0.678525403784435,-1.17524047358083,
-3.67916666666667));
#366683=CARTESIAN_POINT('Ctrl Pts',(-1.43925448419918E-16,-1.17524047358083,
-3.6375));
#366684=CARTESIAN_POINT('Ctrl Pts',(-1.43925448419918E-16,-1.17524047358083,
-4.2));
#366685=CARTESIAN_POINT('Ctrl Pts',(0.678525403784435,-1.17524047358083,
-4.15833333333333));
#366686=CARTESIAN_POINT('Ctrl Pts',(1.01778810567665,-0.587620236790413,
-4.11666666666667));
#366687=CARTESIAN_POINT('Ctrl Pts',(1.35705080756887,2.19240591169326E-15,
-4.075));
#366688=CARTESIAN_POINT('Ctrl Pts',(1.01778810567665,0.587620236790416,
-4.03333333333333));
#366689=CARTESIAN_POINT('Ctrl Pts',(0.678525403784436,1.17524047358083,
-3.99166666666667));
#366690=CARTESIAN_POINT('Ctrl Pts',(0.,1.17524047358083,-3.95));
#366691=CARTESIAN_POINT('Ctrl Pts',(-0.678525403784435,1.17524047358083,
-3.90833333333333));
#366692=CARTESIAN_POINT('Ctrl Pts',(-1.01778810567665,0.587620236790417,
-3.86666666666667));
#366693=CARTESIAN_POINT('Ctrl Pts',(-1.35705080756887,2.4155135775006E-15,
-3.825));
#366694=CARTESIAN_POINT('Ctrl Pts',(-1.01778810567665,-0.587620236790412,
-3.78333333333333));
#366695=CARTESIAN_POINT('Ctrl Pts',(-0.678525403784435,-1.17524047358083,
-3.74166666666667));
#366696=CARTESIAN_POINT('Ctrl Pts',(-1.43925448419918E-16,-1.17524047358083,
-3.7));
#366697=CARTESIAN_POINT('Origin',(0.,-7.56339435525888E-14,-9.91875));
#366698=CARTESIAN_POINT('',(-4.71467650385995E-30,-1.17524047358083,-3.1375));
#366699=CARTESIAN_POINT('',(-4.71467650385995E-30,-1.17524047358083,-3.2));
#366700=CARTESIAN_POINT('',(1.43925448419928E-16,-1.17524047358099,-9.91875));
#366701=CARTESIAN_POINT('Ctrl Pts',(-1.43925448419918E-16,-1.17524047358083,
-3.6375));
#366702=CARTESIAN_POINT('Ctrl Pts',(0.678525403784435,-1.17524047358083,
-3.59583333333333));
#366703=CARTESIAN_POINT('Ctrl Pts',(1.01778810567665,-0.587620236790413,
-3.55416666666667));
#366704=CARTESIAN_POINT('Ctrl Pts',(1.35705080756887,1.94653959226348E-15,
-3.5125));
#366705=CARTESIAN_POINT('Ctrl Pts',(1.01778810567665,0.587620236790416,
-3.47083333333333));
#366706=CARTESIAN_POINT('Ctrl Pts',(0.678525403784436,1.17524047358083,
-3.42916666666667));
#366707=CARTESIAN_POINT('Ctrl Pts',(0.,1.17524047358083,-3.3875));
#366708=CARTESIAN_POINT('Ctrl Pts',(-0.678525403784435,1.17524047358083,
-3.34583333333333));
#366709=CARTESIAN_POINT('Ctrl Pts',(-1.01778810567665,0.587620236790417,
-3.30416666666667));
#366710=CARTESIAN_POINT('Ctrl Pts',(-1.35705080756887,2.16964725807082E-15,
-3.2625));
#366711=CARTESIAN_POINT('Ctrl Pts',(-1.01778810567665,-0.587620236790412,
-3.22083333333333));
#366712=CARTESIAN_POINT('Ctrl Pts',(-0.678525403784435,-1.17524047358083,
-3.17916666666667));
#366713=CARTESIAN_POINT('Ctrl Pts',(-1.43925448419918E-16,-1.17524047358083,
-3.1375));
#366714=CARTESIAN_POINT('Ctrl Pts',(-1.43925448419918E-16,-1.17524047358083,
-3.7));
#366715=CARTESIAN_POINT('Ctrl Pts',(0.678525403784435,-1.17524047358083,
-3.65833333333333));
#366716=CARTESIAN_POINT('Ctrl Pts',(1.01778810567665,-0.587620236790413,
-3.61666666666667));
#366717=CARTESIAN_POINT('Ctrl Pts',(1.35705080756887,1.97385807220012E-15,
-3.575));
#366718=CARTESIAN_POINT('Ctrl Pts',(1.01778810567665,0.587620236790416,
-3.53333333333333));
#366719=CARTESIAN_POINT('Ctrl Pts',(0.678525403784436,1.17524047358083,
-3.49166666666667));
#366720=CARTESIAN_POINT('Ctrl Pts',(0.,1.17524047358083,-3.45));
#366721=CARTESIAN_POINT('Ctrl Pts',(-0.678525403784435,1.17524047358083,
-3.40833333333333));
#366722=CARTESIAN_POINT('Ctrl Pts',(-1.01778810567665,0.587620236790417,
-3.36666666666667));
#366723=CARTESIAN_POINT('Ctrl Pts',(-1.35705080756887,2.19696573800746E-15,
-3.325));
#366724=CARTESIAN_POINT('Ctrl Pts',(-1.01778810567665,-0.587620236790412,
-3.28333333333333));
#366725=CARTESIAN_POINT('Ctrl Pts',(-0.678525403784435,-1.17524047358083,
-3.24166666666667));
#366726=CARTESIAN_POINT('Ctrl Pts',(-1.43925448419918E-16,-1.17524047358083,
-3.2));
#366727=CARTESIAN_POINT('Origin',(0.,-7.56339435525888E-14,-9.91875));
#366728=CARTESIAN_POINT('',(-4.71467650385995E-30,-1.17524047358083,-2.6375));
#366729=CARTESIAN_POINT('',(-4.71467650385995E-30,-1.17524047358083,-2.7));
#366730=CARTESIAN_POINT('',(1.43925448419928E-16,-1.17524047358099,-9.91875));
#366731=CARTESIAN_POINT('Ctrl Pts',(-1.43925448419918E-16,-1.17524047358083,
-3.1375));
#366732=CARTESIAN_POINT('Ctrl Pts',(0.678525403784435,-1.17524047358083,
-3.09583333333333));
#366733=CARTESIAN_POINT('Ctrl Pts',(1.01778810567665,-0.587620236790413,
-3.05416666666667));
#366734=CARTESIAN_POINT('Ctrl Pts',(1.35705080756887,1.72799175277034E-15,
-3.0125));
#366735=CARTESIAN_POINT('Ctrl Pts',(1.01778810567665,0.587620236790416,
-2.97083333333333));
#366736=CARTESIAN_POINT('Ctrl Pts',(0.678525403784436,1.17524047358083,
-2.92916666666667));
#366737=CARTESIAN_POINT('Ctrl Pts',(0.,1.17524047358083,-2.8875));
#366738=CARTESIAN_POINT('Ctrl Pts',(-0.678525403784435,1.17524047358083,
-2.84583333333333));
#366739=CARTESIAN_POINT('Ctrl Pts',(-1.01778810567665,0.587620236790417,
-2.80416666666667));
#366740=CARTESIAN_POINT('Ctrl Pts',(-1.35705080756887,1.95109941857768E-15,
-2.7625));
#366741=CARTESIAN_POINT('Ctrl Pts',(-1.01778810567665,-0.587620236790413,
-2.72083333333333));
#366742=CARTESIAN_POINT('Ctrl Pts',(-0.678525403784435,-1.17524047358083,
-2.67916666666667));
#366743=CARTESIAN_POINT('Ctrl Pts',(-1.43925448419918E-16,-1.17524047358083,
-2.6375));
#366744=CARTESIAN_POINT('Ctrl Pts',(-1.43925448419918E-16,-1.17524047358083,
-3.2));
#366745=CARTESIAN_POINT('Ctrl Pts',(0.678525403784435,-1.17524047358083,
-3.15833333333333));
#366746=CARTESIAN_POINT('Ctrl Pts',(1.01778810567665,-0.587620236790413,
-3.11666666666667));
#366747=CARTESIAN_POINT('Ctrl Pts',(1.35705080756887,1.75531023270698E-15,
-3.075));
#366748=CARTESIAN_POINT('Ctrl Pts',(1.01778810567665,0.587620236790416,
-3.03333333333333));
#366749=CARTESIAN_POINT('Ctrl Pts',(0.678525403784436,1.17524047358083,
-2.99166666666667));
#366750=CARTESIAN_POINT('Ctrl Pts',(0.,1.17524047358083,-2.95));
#366751=CARTESIAN_POINT('Ctrl Pts',(-0.678525403784435,1.17524047358083,
-2.90833333333333));
#366752=CARTESIAN_POINT('Ctrl Pts',(-1.01778810567665,0.587620236790417,
-2.86666666666667));
#366753=CARTESIAN_POINT('Ctrl Pts',(-1.35705080756887,1.97841789851432E-15,
-2.825));
#366754=CARTESIAN_POINT('Ctrl Pts',(-1.01778810567665,-0.587620236790413,
-2.78333333333333));
#366755=CARTESIAN_POINT('Ctrl Pts',(-0.678525403784435,-1.17524047358083,
-2.74166666666667));
#366756=CARTESIAN_POINT('Ctrl Pts',(-1.43925448419918E-16,-1.17524047358083,
-2.7));
#366757=CARTESIAN_POINT('Origin',(0.,-7.56339435525888E-14,-9.91875));
#366758=CARTESIAN_POINT('',(-4.68386162474976E-30,-1.17524047358083,-2.1375));
#366759=CARTESIAN_POINT('',(-4.68386162474976E-30,-1.17524047358083,-2.2));
#366760=CARTESIAN_POINT('',(1.43925448419928E-16,-1.17524047358099,-9.91875));
#366761=CARTESIAN_POINT('Ctrl Pts',(-1.43925448419918E-16,-1.17524047358083,
-2.6375));
#366762=CARTESIAN_POINT('Ctrl Pts',(0.678525403784435,-1.17524047358083,
-2.59583333333333));
#366763=CARTESIAN_POINT('Ctrl Pts',(1.01778810567665,-0.587620236790414,
-2.55416666666667));
#366764=CARTESIAN_POINT('Ctrl Pts',(1.35705080756887,1.5094439132772E-15,
-2.5125));
#366765=CARTESIAN_POINT('Ctrl Pts',(1.01778810567665,0.587620236790415,
-2.47083333333333));
#366766=CARTESIAN_POINT('Ctrl Pts',(0.678525403784436,1.17524047358083,
-2.42916666666667));
#366767=CARTESIAN_POINT('Ctrl Pts',(0.,1.17524047358083,-2.3875));
#366768=CARTESIAN_POINT('Ctrl Pts',(-0.678525403784435,1.17524047358083,
-2.34583333333333));
#366769=CARTESIAN_POINT('Ctrl Pts',(-1.01778810567665,0.587620236790416,
-2.30416666666667));
#366770=CARTESIAN_POINT('Ctrl Pts',(-1.35705080756887,1.73255157908454E-15,
-2.2625));
#366771=CARTESIAN_POINT('Ctrl Pts',(-1.01778810567665,-0.587620236790413,
-2.22083333333333));
#366772=CARTESIAN_POINT('Ctrl Pts',(-0.678525403784435,-1.17524047358083,
-2.17916666666667));
#366773=CARTESIAN_POINT('Ctrl Pts',(-1.43925448419918E-16,-1.17524047358083,
-2.1375));
#366774=CARTESIAN_POINT('Ctrl Pts',(-1.43925448419918E-16,-1.17524047358083,
-2.7));
#366775=CARTESIAN_POINT('Ctrl Pts',(0.678525403784435,-1.17524047358083,
-2.65833333333333));
#366776=CARTESIAN_POINT('Ctrl Pts',(1.01778810567665,-0.587620236790414,
-2.61666666666667));
#366777=CARTESIAN_POINT('Ctrl Pts',(1.35705080756887,1.53676239321384E-15,
-2.575));
#366778=CARTESIAN_POINT('Ctrl Pts',(1.01778810567665,0.587620236790415,
-2.53333333333333));
#366779=CARTESIAN_POINT('Ctrl Pts',(0.678525403784436,1.17524047358083,
-2.49166666666667));
#366780=CARTESIAN_POINT('Ctrl Pts',(0.,1.17524047358083,-2.45));
#366781=CARTESIAN_POINT('Ctrl Pts',(-0.678525403784435,1.17524047358083,
-2.40833333333333));
#366782=CARTESIAN_POINT('Ctrl Pts',(-1.01778810567665,0.587620236790416,
-2.36666666666667));
#366783=CARTESIAN_POINT('Ctrl Pts',(-1.35705080756887,1.75987005902118E-15,
-2.325));
#366784=CARTESIAN_POINT('Ctrl Pts',(-1.01778810567665,-0.587620236790413,
-2.28333333333333));
#366785=CARTESIAN_POINT('Ctrl Pts',(-0.678525403784435,-1.17524047358083,
-2.24166666666667));
#366786=CARTESIAN_POINT('Ctrl Pts',(-1.43925448419918E-16,-1.17524047358083,
-2.2));
#366787=CARTESIAN_POINT('Origin',(0.,2.16840434497101E-16,-9.7));
#366788=CARTESIAN_POINT('',(8.37355900338938E-15,-1.5,-1.95));
#366789=CARTESIAN_POINT('',(-1.10524344990624E-13,-1.5,-1.88750000000001));
#366790=CARTESIAN_POINT('',(-1.83697019872103E-16,-1.5,-9.7));
#366791=CARTESIAN_POINT('',(3.31235039396818E-12,1.5,-1.70000000000016));
#366792=CARTESIAN_POINT('Ctrl Pts',(1.69308150266509E-14,-1.5,-1.95));
#366793=CARTESIAN_POINT('Ctrl Pts',(0.01548927559932,-1.5,-1.94925477188026));
#366794=CARTESIAN_POINT('Ctrl Pts',(0.0309872899763081,-1.49976008338734,
-1.94850245896548));
#366795=CARTESIAN_POINT('Ctrl Pts',(0.245230706998799,-1.49311698268964,
-1.93801013718304));
#366796=CARTESIAN_POINT('Ctrl Pts',(0.440744097796248,-1.44749995108539,
-1.92733635501567));
#366797=CARTESIAN_POINT('Ctrl Pts',(0.799081574720929,-1.28432119946332,
-1.90556309201812));
#366798=CARTESIAN_POINT('Ctrl Pts',(0.959083807576905,-1.16969177102424,
-1.89468083021062));
#366799=CARTESIAN_POINT('Ctrl Pts',(1.22335267335872,-0.888702989669011,
-1.87416094455096));
#366800=CARTESIAN_POINT('Ctrl Pts',(1.32631553511077,-0.726132398087802,
-1.8653406887826));
#366801=CARTESIAN_POINT('Ctrl Pts',(1.46936522121737,-0.362105715195533,
-1.84511698417747));
#366802=CARTESIAN_POINT('Ctrl Pts',(1.50453671316576,-0.16281355519964,
-1.83404519751103));
#366803=CARTESIAN_POINT('Ctrl Pts',(1.49471805803775,0.230113327460341,
-1.81221592625215));
#366804=CARTESIAN_POINT('Ctrl Pts',(1.45282581838479,0.420057916318203,
-1.80166344909338));
#366805=CARTESIAN_POINT('Ctrl Pts',(1.29846283502885,0.775942345695251,
-1.78189209190576));
#366806=CARTESIAN_POINT('Ctrl Pts',(1.18661123088408,0.938112544720388,
-1.77269884433335));
#366807=CARTESIAN_POINT('Ctrl Pts',(0.906165332737575,1.21137288812808,
-1.75161531967302));
#366808=CARTESIAN_POINT('Ctrl Pts',(0.739976898836962,1.31946560344659,
-1.74061699949345));
#366809=CARTESIAN_POINT('Ctrl Pts',(0.38027303752142,1.4635305198243,-1.71930893616415));
#366810=CARTESIAN_POINT('Ctrl Pts',(0.190972331354127,1.49999999999957,
-1.70918816057627));
#366811=CARTESIAN_POINT('Ctrl Pts',(3.42524619778573E-12,1.5,-1.70000000000016));
#366812=CARTESIAN_POINT('',(1.05094390383305,1.07028823734364,-1.7));
#366813=CARTESIAN_POINT('Origin',(0.,0.,-1.7));
#366814=CARTESIAN_POINT('Ctrl Pts',(1.05094390383305,1.07028823734364,-1.7));
#366815=CARTESIAN_POINT('Ctrl Pts',(1.13868622596693,0.984131765341644,
-1.70661473977534));
#366816=CARTESIAN_POINT('Ctrl Pts',(1.21551289992726,0.887500782972839,
-1.71299525880436));
#366817=CARTESIAN_POINT('Ctrl Pts',(1.34320212457071,0.678698115085337,
-1.72493878359739));
#366818=CARTESIAN_POINT('Ctrl Pts',(1.39385259493898,0.567464160994353,
-1.7309742132781));
#366819=CARTESIAN_POINT('Ctrl Pts',(1.48909100396381,0.265573903134679,
-1.74774589427031));
#366820=CARTESIAN_POINT('Ctrl Pts',(1.51095330790636,0.0702300270822034,
-1.75859833182878));
#366821=CARTESIAN_POINT('Ctrl Pts',(1.47847203925917,-0.321929757940045,
-1.78038498655224));
#366822=CARTESIAN_POINT('Ctrl Pts',(1.42283948268589,-0.514849569711096,
-1.79110275387285));
#366823=CARTESIAN_POINT('Ctrl Pts',(1.24364892170843,-0.859893643390216,
-1.81027186907725));
#366824=CARTESIAN_POINT('Ctrl Pts',(1.12486783254292,-1.01033797780081,
-1.81977804833436));
#366825=CARTESIAN_POINT('Ctrl Pts',(0.832106228736892,-1.26349166477242,
-1.84089559442517));
#366826=CARTESIAN_POINT('Ctrl Pts',(0.659148099511349,-1.36174019513924,
-1.85194617214093));
#366827=CARTESIAN_POINT('Ctrl Pts',(0.319613523634357,-1.47433868038769,
-1.87140977274076));
#366828=CARTESIAN_POINT('Ctrl Pts',(0.160210430373053,-1.50000000000003,
-1.87979187207477));
#366829=CARTESIAN_POINT('Ctrl Pts',(-2.2062213167473E-13,-1.5,-1.88750000000001));
#366830=CARTESIAN_POINT('Origin',(0.,2.16840434497101E-16,-9.7));
#366831=CARTESIAN_POINT('',(1.10235999999511E-13,-1.5,-2.44999999999999));
#366832=CARTESIAN_POINT('',(-1.78584683734892E-16,-1.5,-2.3875));
#366833=CARTESIAN_POINT('',(-1.83697019872103E-16,-1.5,-9.7));
#366834=CARTESIAN_POINT('Ctrl Pts',(2.20655697018894E-13,-1.5,-2.44999999999999));
#366835=CARTESIAN_POINT('Ctrl Pts',(0.0446866432717563,-1.5,-2.44785001287315));
#366836=CARTESIAN_POINT('Ctrl Pts',(0.0894198514888752,-1.498003204062,
-2.44564231883545));
#366837=CARTESIAN_POINT('Ctrl Pts',(0.3321653732503,-1.47621975128952,-2.43335812356398));
#366838=CARTESIAN_POINT('Ctrl Pts',(0.524735235130775,-1.41922200076027,
-2.4225098309164));
#366839=CARTESIAN_POINT('Ctrl Pts',(0.871983263480545,-1.23581136686393,
-2.40070811253234));
#366840=CARTESIAN_POINT('Ctrl Pts',(1.02425456323397,-1.11287912297099,
-2.38996717165455));
#366841=CARTESIAN_POINT('Ctrl Pts',(1.27260752980148,-0.816998279750627,
-2.36979937166772));
#366842=CARTESIAN_POINT('Ctrl Pts',(1.3667848766936,-0.647237619333921,
-2.3609576455185));
#366843=CARTESIAN_POINT('Ctrl Pts',(1.48799058251274,-0.274881222866593,
-2.34027117904809));
#366844=CARTESIAN_POINT('Ctrl Pts',(1.51129959338589,-0.0750919538647505,
-2.32917177521466));
#366845=CARTESIAN_POINT('Ctrl Pts',(1.47915085768955,0.314388053469471,
-2.30753399702943));
#366846=CARTESIAN_POINT('Ctrl Pts',(1.42692591478426,0.500630191029841,
-2.29718721160941));
#366847=CARTESIAN_POINT('Ctrl Pts',(1.25204566055684,0.849614101653204,
-2.27779921657477));
#366848=CARTESIAN_POINT('Ctrl Pts',(1.1286436947597,1.00779587912277,-2.26797423177337));
#366849=CARTESIAN_POINT('Ctrl Pts',(0.828833174688191,1.2655911178986,-2.24638861254606));
#366850=CARTESIAN_POINT('Ctrl Pts',(0.655921667069359,1.36325085762577,
-2.23535663320894));
#366851=CARTESIAN_POINT('Ctrl Pts',(0.288677744379025,1.48416505168848,
-2.21432887412746));
#366852=CARTESIAN_POINT('Ctrl Pts',(0.0986552973958269,1.50874919684857,
-2.20498958845478));
#366853=CARTESIAN_POINT('Ctrl Pts',(-0.289385654160681,1.48519512435956,
-2.18566567967694));
#366854=CARTESIAN_POINT('Ctrl Pts',(-0.483493906473983,1.43379201778904,
-2.17489877796179));
#366855=CARTESIAN_POINT('Ctrl Pts',(-0.836359921965577,1.26027651369972,
-2.1531016287622));
#366856=CARTESIAN_POINT('Ctrl Pts',(-0.992499988597624,1.14138038910413,
-2.1422866661761));
#366857=CARTESIAN_POINT('Ctrl Pts',(-1.2487389672651,0.852825405147202,
-2.12194294634587));
#366858=CARTESIAN_POINT('Ctrl Pts',(-1.34727470246183,0.686665969635683,
-2.11314810942415));
#366859=CARTESIAN_POINT('Ctrl Pts',(-1.47937082574391,0.318393327600033,
-2.09268851819995));
#366860=CARTESIAN_POINT('Ctrl Pts',(-1.50857345947938,0.118766243301032,
-2.08159812462778));
#366861=CARTESIAN_POINT('Ctrl Pts',(-1.48749023769102,-0.272583545355803,
-2.0598564697024));
#366862=CARTESIAN_POINT('Ctrl Pts',(-1.44037126809873,-0.460737270908912,
-2.04940348494945));
#366863=CARTESIAN_POINT('Ctrl Pts',(-1.27571175718277,-0.813199170429424,
-2.02982226830943));
#366864=CARTESIAN_POINT('Ctrl Pts',(-1.15813565951456,-0.973381389779296,
-2.02034912262653));
#366865=CARTESIAN_POINT('Ctrl Pts',(-0.86744354656846,-1.23954180631063,
-1.99896984691782));
#366866=CARTESIAN_POINT('Ctrl Pts',(-0.697073007651896,-1.34276191574104,
-1.98790566528041));
#366867=CARTESIAN_POINT('Ctrl Pts',(-0.347459626841339,-1.46961511417048,
-1.9675611836971));
#366868=CARTESIAN_POINT('Ctrl Pts',(-0.174323197795173,-1.5,-1.95838712876442));
#366869=CARTESIAN_POINT('Ctrl Pts',(1.5855372570428E-14,-1.5,-1.95));
#366870=CARTESIAN_POINT('Ctrl Pts',(-2.20864992961377E-13,-1.5,-1.88750000000001));
#366871=CARTESIAN_POINT('Ctrl Pts',(-0.0368623918547273,-1.5,-1.88927354265503));
#366872=CARTESIAN_POINT('Ctrl Pts',(-0.0737639135159791,-1.49864120837783,
-1.89108671215548));
#366873=CARTESIAN_POINT('Ctrl Pts',(-0.302085379330646,-1.48175565959102,
-1.90254087682316));
#366874=CARTESIAN_POINT('Ctrl Pts',(-0.489025568623064,-1.43097495551993,
-1.91294561598711));
#366875=CARTESIAN_POINT('Ctrl Pts',(-0.840337210031122,-1.25842118658735,
-1.93464126546327));
#366876=CARTESIAN_POINT('Ctrl Pts',(-1.00006721705373,-1.13563545664226,
-1.94573699372998));
#366877=CARTESIAN_POINT('Ctrl Pts',(-1.25712218842694,-0.840510858843861,
-1.96630246230095));
#366878=CARTESIAN_POINT('Ctrl Pts',(-1.35420304308014,-0.673014628741669,
-1.97511029840325));
#366879=CARTESIAN_POINT('Ctrl Pts',(-1.48076488748363,-0.308291742248993,
-1.99537268098618));
#366880=CARTESIAN_POINT('Ctrl Pts',(-1.50819421076492,-0.114223606293866,
-2.0061542440948));
#366881=CARTESIAN_POINT('Ctrl Pts',(-1.48732444675329,0.278204630505327,
-2.02795581280586));
#366882=CARTESIAN_POINT('Ctrl Pts',(-1.43739269292505,0.472711044720166,
-2.03876172470669));
#366883=CARTESIAN_POINT('Ctrl Pts',(-1.26845143123851,0.822853866465687,
-2.05821410369255));
#366884=CARTESIAN_POINT('Ctrl Pts',(-1.15421015875391,0.976665383468958,
-2.06743096516376));
#366885=CARTESIAN_POINT('Ctrl Pts',(-0.869565726160317,1.23791656925302,
-2.08838290419509));
#366886=CARTESIAN_POINT('Ctrl Pts',(-0.700167326634511,1.34102411927311,
-2.09939718710397));
#366887=CARTESIAN_POINT('Ctrl Pts',(-0.328270138095944,1.47718926068047,
-2.12107246396919));
#366888=CARTESIAN_POINT('Ctrl Pts',(-0.129042021872983,1.50770184074051,
-2.13107752280734));
#366889=CARTESIAN_POINT('Ctrl Pts',(0.261537194048148,1.48938177747693,
-2.15037816474122));
#366890=CARTESIAN_POINT('Ctrl Pts',(0.449289004131965,1.44387580850969,
-2.16067543260915));
#366891=CARTESIAN_POINT('Ctrl Pts',(0.804299308327845,1.28166496038003,
-2.18226173072602));
#366892=CARTESIAN_POINT('Ctrl Pts',(0.966986956683662,1.16383327810383,
-2.19336214614247));
#366893=CARTESIAN_POINT('Ctrl Pts',(1.2328126962066,0.875999571507584,-2.21414707373718));
#366894=CARTESIAN_POINT('Ctrl Pts',(1.33510265331455,0.710423042788745,
-2.22303205317841));
#366895=CARTESIAN_POINT('Ctrl Pts',(1.47167733932044,0.348815694246995,
-2.24312135031962));
#366896=CARTESIAN_POINT('Ctrl Pts',(1.50436781701598,0.156109912924603,
-2.25382722705976));
#366897=CARTESIAN_POINT('Ctrl Pts',(1.49456606947089,-0.236252467601609,
-2.27562513708899));
#366898=CARTESIAN_POINT('Ctrl Pts',(1.45011794280952,-0.432111481359206,
-2.28650619340886));
#366899=CARTESIAN_POINT('Ctrl Pts',(1.29101128548853,-0.787023085734208,
-2.30622350476302));
#366900=CARTESIAN_POINT('Ctrl Pts',(1.18103363775905,-0.944079505943259,
-2.31523525666381));
#366901=CARTESIAN_POINT('Ctrl Pts',(0.9040655830077,-1.21286160675192,-2.33602705787802));
#366902=CARTESIAN_POINT('Ctrl Pts',(0.738133667625035,-1.32042497463635,
-2.34699833220925));
#366903=CARTESIAN_POINT('Ctrl Pts',(0.379175592598109,-1.46375304244289,
-2.36825004586315));
#366904=CARTESIAN_POINT('Ctrl Pts',(0.190390033540378,-1.5,-2.37833985524037));
#366905=CARTESIAN_POINT('Ctrl Pts',(9.36750677027476E-16,-1.5,-2.3875));
#366906=CARTESIAN_POINT('Origin',(0.,2.16840434497101E-16,-9.7));
#366907=CARTESIAN_POINT('',(2.53043732100507E-14,-1.5,-2.94999999999999));
#366908=CARTESIAN_POINT('',(2.5321850413124E-14,-1.5,-2.8875));
#366909=CARTESIAN_POINT('',(-1.83697019872103E-16,-1.5,-9.7));
#366910=CARTESIAN_POINT('Ctrl Pts',(5.07924434399736E-14,-1.5,-2.94999999999999));
#366911=CARTESIAN_POINT('Ctrl Pts',(0.0744213382181849,-1.5,-2.94641940169552));
#366912=CARTESIAN_POINT('Ctrl Pts',(0.148892353057916,-1.4944622271461,
-2.94268258629972));
#366913=CARTESIAN_POINT('Ctrl Pts',(0.420969831647567,-1.45359546756537,
-2.92845706474157));
#366914=CARTESIAN_POINT('Ctrl Pts',(0.611154960021442,-1.3844238016528,
-2.91738534332213));
#366915=CARTESIAN_POINT('Ctrl Pts',(0.946549473523585,-1.17948246468226,
-2.89555585235168));
#366916=CARTESIAN_POINT('Ctrl Pts',(1.09011167306719,-1.04824072625686,
-2.88500310896054));
#366917=CARTESIAN_POINT('Ctrl Pts',(1.3211576247791,-0.736636363828259,
-2.86523122869174));
#366918=CARTESIAN_POINT('Ctrl Pts',(1.40568797429451,-0.55869580933379,
-2.85603865607406));
#366919=CARTESIAN_POINT('Ctrl Pts',(1.50252275599202,-0.177726380825034,
-2.83487368782357));
#366920=CARTESIAN_POINT('Ctrl Pts',(1.51283851044406,0.0218258598492461,
-2.82378745223056));
#366921=CARTESIAN_POINT('Ctrl Pts',(1.4564811902691,0.406185454812701,-2.80243414139925));
#366922=CARTESIAN_POINT('Ctrl Pts',(1.39315447369828,0.587696925737235,
-2.79236992793051));
#366923=CARTESIAN_POINT('Ctrl Pts',(1.19789975854395,0.924423411128237,
-2.77362221758452));
#366924=CARTESIAN_POINT('Ctrl Pts',(1.06499159643924,1.0748433825963,-2.76304933811302));
#366925=CARTESIAN_POINT('Ctrl Pts',(0.750911055879611,1.31314905744491,
-2.74131852898062));
#366926=CARTESIAN_POINT('Ctrl Pts',(0.573530775952319,1.39974863451254,
-2.73037877247611));
#366927=CARTESIAN_POINT('Ctrl Pts',(0.200625988877396,1.49864904366988,
-2.70969014895509));
#366928=CARTESIAN_POINT('Ctrl Pts',(0.00915798051034495,1.51198819321672,
-2.70077361890983));
#366929=CARTESIAN_POINT('Ctrl Pts',(-0.377196203055984,1.46536349575517,
-2.68089001410107));
#366930=CARTESIAN_POINT('Ctrl Pts',(-0.567955146829013,1.40248926947439,
-2.66996561385402));
#366931=CARTESIAN_POINT('Ctrl Pts',(-0.908947172797603,1.20879214084764,
-2.64817915156013));
#366932=CARTESIAN_POINT('Ctrl Pts',(-1.05700900098552,1.08171642547661,
-2.63752564254751));
#366933=CARTESIAN_POINT('Ctrl Pts',(-1.29692998600533,0.778114569031601,
-2.61754905387248));
#366934=CARTESIAN_POINT('Ctrl Pts',(-1.38642500099297,0.604416767699619,
-2.6085787093166));
#366935=CARTESIAN_POINT('Ctrl Pts',(-1.49583808741873,0.227799377384436,
-2.58765552096576));
#366936=CARTESIAN_POINT('Ctrl Pts',(-1.51282229632946,0.0280229106174455,
-2.57655682836759));
#366937=CARTESIAN_POINT('Ctrl Pts',(-1.46886197321051,-0.359103764703532,
-2.55504979084976));
#366938=CARTESIAN_POINT('Ctrl Pts',(-1.41121851423137,-0.543135540070848,
-2.54482580332935));
#366939=CARTESIAN_POINT('Ctrl Pts',(-1.2262879171076,-0.886416245393696,
-2.52575465303364));
#366940=CARTESIAN_POINT('Ctrl Pts',(-1.0981320239873,-1.0409918706452,-2.51558412745327));
#366941=CARTESIAN_POINT('Ctrl Pts',(-0.791055940191536,-1.28945370009369,
-2.49390820499849));
#366942=CARTESIAN_POINT('Ctrl Pts',(-0.615872233743788,-1.38172540247317,
-2.48291657214834));
#366943=CARTESIAN_POINT('Ctrl Pts',(-0.288782841940459,-1.47907824222109,
-2.46447523089923));
#366944=CARTESIAN_POINT('Ctrl Pts',(-0.144663401257926,-1.5,-2.45696012113819));
#366945=CARTESIAN_POINT('Ctrl Pts',(2.20655697018894E-13,-1.5,-2.44999999999999));
#366946=CARTESIAN_POINT('Ctrl Pts',(-1.73472347597681E-16,-1.5,-2.3875));
#366947=CARTESIAN_POINT('Ctrl Pts',(-0.00820824151007254,-1.5,-2.38789491920379));
#366948=CARTESIAN_POINT('Ctrl Pts',(-0.0164192878007734,-1.49993262484668,
-2.38829184488469));
#366949=CARTESIAN_POINT('Ctrl Pts',(-0.215498919763185,-1.49666298850653,
-2.397960891375));
#366950=CARTESIAN_POINT('Ctrl Pts',(-0.403990759766078,-1.4571230805755,
-2.40812804003134));
#366951=CARTESIAN_POINT('Ctrl Pts',(-0.762822106339094,-1.30667918707593,
-2.42957131828446));
#366952=CARTESIAN_POINT('Ctrl Pts',(-0.928672474770597,-1.19452158185493,
-2.44066628688997));
#366953=CARTESIAN_POINT('Ctrl Pts',(-1.20432184412241,-0.915064031477631,
-2.46169118308911));
#366954=CARTESIAN_POINT('Ctrl Pts',(-1.31255322090007,-0.751619157500383,
-2.47074338013888));
#366955=CARTESIAN_POINT('Ctrl Pts',(-1.46026970433536,-0.393568310786017,
-2.49063509384523));
#366956=CARTESIAN_POINT('Ctrl Pts',(-1.49874761594601,-0.202541870011464,
-2.50124767388826));
#366957=CARTESIAN_POINT('Ctrl Pts',(-1.5012409378723,0.191236548850281,
-2.52312425271391));
#366958=CARTESIAN_POINT('Ctrl Pts',(-1.46220428198257,0.390220278258254,
-2.53417890434769));
#366959=CARTESIAN_POINT('Ctrl Pts',(-1.31209345675809,0.751436486119095,
-2.55424647145107));
#366960=CARTESIAN_POINT('Ctrl Pts',(-1.20624636216264,0.911713663222863,
-2.56312315770868));
#366961=CARTESIAN_POINT('Ctrl Pts',(-0.936749160411386,1.18771357230621,
-2.58375601201463));
#366962=CARTESIAN_POINT('Ctrl Pts',(-0.774277755585629,1.29948057143874,
-2.59467755998873));
#366963=CARTESIAN_POINT('Ctrl Pts',(-0.412519795634319,1.45579132507715,
-2.61642461333086));
#366964=CARTESIAN_POINT('Ctrl Pts',(-0.216181858431131,1.49759565573891,
-2.62703215814616));
#366965=CARTESIAN_POINT('Ctrl Pts',(0.172891068474,1.50210410915275,-2.6458766728868));
#366966=CARTESIAN_POINT('Ctrl Pts',(0.361923021625222,1.46808371059299,
-2.65579959309142));
#366967=CARTESIAN_POINT('Ctrl Pts',(0.724037963046113,1.32847515826504,
-2.67709987167611));
#366968=CARTESIAN_POINT('Ctrl Pts',(0.892625190355791,1.22159778381432,
-2.68817984438883));
#366969=CARTESIAN_POINT('Ctrl Pts',(1.17722185853026,0.949977003646278,
-2.70941752964192));
#366970=CARTESIAN_POINT('Ctrl Pts',(1.29097321174977,0.788469814882173,
-2.71869612139544));
#366971=CARTESIAN_POINT('Ctrl Pts',(1.44878182832975,0.433721693734626,
-2.73840435034808));
#366972=CARTESIAN_POINT('Ctrl Pts',(1.49243191904509,0.244361021410866,
-2.7489243876994));
#366973=CARTESIAN_POINT('Ctrl Pts',(1.50603213313662,-0.148072780988375,
-2.77072626561047));
#366974=CARTESIAN_POINT('Ctrl Pts',(1.47286098589617,-0.347496303598292,
-2.78180535019991));
#366975=CARTESIAN_POINT('Ctrl Pts',(1.33347477910016,-0.712958631639371,
-2.80210881286886));
#366976=CARTESIAN_POINT('Ctrl Pts',(1.23199853818993,-0.876725265436446,
-2.81091225562337));
#366977=CARTESIAN_POINT('Ctrl Pts',(0.970426193171564,-1.16026762329887,
-2.83137333754807));
#366978=CARTESIAN_POINT('Ctrl Pts',(0.81171179415968,-1.27634746178067,
-2.84223392758871));
#366979=CARTESIAN_POINT('Ctrl Pts',(0.455182813765921,-1.4430263855456,
-2.86401740626031));
#366980=CARTESIAN_POINT('Ctrl Pts',(0.260122768660399,-1.49059615477631,
-2.87472361953476));
#366981=CARTESIAN_POINT('Ctrl Pts',(0.0409548134732333,-1.49958097346455,
-2.88551792099208));
#366982=CARTESIAN_POINT('Ctrl Pts',(0.0204702234117732,-1.5,-2.88651512591691));
#366983=CARTESIAN_POINT('Ctrl Pts',(5.08273978461202E-14,-1.5,-2.8875));
#366984=CARTESIAN_POINT('Origin',(0.,2.16840434497101E-16,-9.7));
#366985=CARTESIAN_POINT('',(-2.58985031534265E-15,-1.5,-3.45));
#366986=CARTESIAN_POINT('',(1.01771113999419E-13,-1.5,-3.38749999999999));
#366987=CARTESIAN_POINT('',(-1.83697019872103E-16,-1.5,-9.7));
#366988=CARTESIAN_POINT('Ctrl Pts',(-1.12757025938492E-15,-1.5,-3.45));
#366989=CARTESIAN_POINT('Ctrl Pts',(0.104274349025483,-1.5,-3.44498309804338));
#366990=CARTESIAN_POINT('Ctrl Pts',(0.20848744942163,-1.48912928790673,
-3.43966717868797));
#366991=CARTESIAN_POINT('Ctrl Pts',(0.505825920466392,-1.42611936646804,
-3.42361119923427));
#366992=CARTESIAN_POINT('Ctrl Pts',(0.69051093996075,-1.34642509850937,
-3.41251180742539));
#366993=CARTESIAN_POINT('Ctrl Pts',(1.01175618937721,-1.12386701912129,
-3.39087371928463));
#366994=CARTESIAN_POINT('Ctrl Pts',(1.14694586773164,-0.985527209922369,
-3.38052663037441));
#366995=CARTESIAN_POINT('Ctrl Pts',(1.36175721992224,-0.659604114449861,
-3.36113809505471));
#366996=CARTESIAN_POINT('Ctrl Pts',(1.43705865734217,-0.473655318003814,
-3.35131418433351));
#366997=CARTESIAN_POINT('Ctrl Pts',(1.51044358412492,-0.0851242809337696,
-3.32972912671851));
#366998=CARTESIAN_POINT('Ctrl Pts',(1.50858050856705,0.113453209714267,
-3.31869704390473));
#366999=CARTESIAN_POINT('Ctrl Pts',(1.42970448816059,0.491961281274415,
-3.29766881770694));
#367000=CARTESIAN_POINT('Ctrl Pts',(1.35599837329553,0.668823945725757,
-3.28832872588338));
#367001=CARTESIAN_POINT('Ctrl Pts',(1.1416063557085,0.993118075303684,-3.26900561486183));
#367002=CARTESIAN_POINT('Ctrl Pts',(1.00004772648413,1.13553089559032,-3.25823896046313));
#367003=CARTESIAN_POINT('Ctrl Pts',(0.673362868540264,1.35439206440055,
-3.23644185099557));
#367004=CARTESIAN_POINT('Ctrl Pts',(0.492330483354827,1.43018065835238,
-3.22562668758144));
#367005=CARTESIAN_POINT('Ctrl Pts',(0.114322046291612,1.50784274836868,
-3.20528246789535));
#367006=CARTESIAN_POINT('Ctrl Pts',(-0.0788414997936811,1.51011337096137,
-3.19648766354368));
#367007=CARTESIAN_POINT('Ctrl Pts',(-0.463828289110963,1.44040839658907,
-3.17602872871833));
#367008=CARTESIAN_POINT('Ctrl Pts',(-0.651319540490476,1.36590000784234,
-3.16493837421526));
#367009=CARTESIAN_POINT('Ctrl Pts',(-0.97971687249228,1.15199150335434,
-3.14319644731011));
#367010=CARTESIAN_POINT('Ctrl Pts',(-1.11911517725929,1.01711848626125,
-3.13274317054793));
#367011=CARTESIAN_POINT('Ctrl Pts',(-1.34204941391269,0.698308531425868,
-3.11316141000722));
#367012=CARTESIAN_POINT('Ctrl Pts',(-1.42199632483557,0.516404899013764,
-3.10368916105629));
#367013=CARTESIAN_POINT('Ctrl Pts',(-1.50718522169627,0.131588669849777,
-3.08231048165829));
#367014=CARTESIAN_POINT('Ctrl Pts',(-1.51140847386047,-0.0675679828713596,
-3.07124622317378));
#367015=CARTESIAN_POINT('Ctrl Pts',(-1.44378208131313,-0.449055345529514,
-3.05005248080388));
#367016=CARTESIAN_POINT('Ctrl Pts',(-1.3753031265635,-0.628220357727625,
-3.04038540370243));
#367017=CARTESIAN_POINT('Ctrl Pts',(-1.17054174751803,-0.958837005905384,
-3.02135002147708));
#367018=CARTESIAN_POINT('Ctrl Pts',(-1.03329182319454,-1.10535941348711,
-3.01067651453694));
#367019=CARTESIAN_POINT('Ctrl Pts',(-0.712824034722463,-1.33412698629862,
-2.98890334607488));
#367020=CARTESIAN_POINT('Ctrl Pts',(-0.533556107643747,-1.41539361172663,
-2.97802090764999));
#367021=CARTESIAN_POINT('Ctrl Pts',(-0.230841399415094,-1.48666354507819,
-2.96147681908883));
#367022=CARTESIAN_POINT('Ctrl Pts',(-0.115498535002616,-1.5,-2.95555692585623));
#367023=CARTESIAN_POINT('Ctrl Pts',(5.20763987488237E-14,-1.5,-2.94999999999999));
#367024=CARTESIAN_POINT('Ctrl Pts',(5.19029264012261E-14,-1.5,-2.8875));
#367025=CARTESIAN_POINT('Ctrl Pts',(-0.169191228008341,-1.5,-2.89564021675293));
#367026=CARTESIAN_POINT('Ctrl Pts',(-0.337325653434019,-1.47137896582402,
-2.90452461679501));
#367027=CARTESIAN_POINT('Ctrl Pts',(-0.683215605809903,-1.34983600112939,
-2.9245424483516));
#367028=CARTESIAN_POINT('Ctrl Pts',(-0.854465761761834,-1.24849108906284,
-2.93559686176769));
#367029=CARTESIAN_POINT('Ctrl Pts',(-1.14825257380326,-0.985142589364441,
-2.95704692245513));
#367030=CARTESIAN_POINT('Ctrl Pts',(-1.26779153793086,-0.825636253928343,
-2.96663131922621));
#367031=CARTESIAN_POINT('Ctrl Pts',(-1.43592311619488,-0.474346778137693,
-2.98614740121458));
#367032=CARTESIAN_POINT('Ctrl Pts',(-1.48478620139945,-0.286827721696611,
-2.99656512657242));
#367033=CARTESIAN_POINT('Ctrl Pts',(-1.5096423051372,0.103920533796697,
-3.01827336298871));
#367034=CARTESIAN_POINT('Ctrl Pts',(-1.48244575409252,0.303621637952862,
-3.02936786877517));
#367035=CARTESIAN_POINT('Ctrl Pts',(-1.35404742260803,0.673295757271683,
-3.04990531984843));
#367036=CARTESIAN_POINT('Ctrl Pts',(-1.25699504700908,0.84067543846082,
-3.05870822644941));
#367037=CARTESIAN_POINT('Ctrl Pts',(-1.00344486967301,1.13173871654929,
-3.07899225610226));
#367038=CARTESIAN_POINT('Ctrl Pts',(-0.848615659840483,1.25202804359538,
-3.08978285012926));
#367039=CARTESIAN_POINT('Ctrl Pts',(-0.497638394565766,1.42894587829609,
-3.11158363597532));
#367040=CARTESIAN_POINT('Ctrl Pts',(-0.304037264242564,1.4822663644638,
-3.12237939931671));
#367041=CARTESIAN_POINT('Ctrl Pts',(0.0837578803978027,1.5096490567957,
-3.14179783225498));
#367042=CARTESIAN_POINT('Ctrl Pts',(0.274001552302664,1.48694279115938,
-3.15104560607727));
#367043=CARTESIAN_POINT('Ctrl Pts',(0.642224686814734,1.36972878103256,
-3.17201769462238));
#367044=CARTESIAN_POINT('Ctrl Pts',(0.815935095358566,1.27391432361466,
-3.18303685325625));
#367045=CARTESIAN_POINT('Ctrl Pts',(1.11873386344195,1.01891457967269,-3.2046885919988));
#367046=CARTESIAN_POINT('Ctrl Pts',(1.24407365753746,0.861395430350653,
-3.21464469831386));
#367047=CARTESIAN_POINT('Ctrl Pts',(1.4222980773209,0.513567189131623,-3.23396848949269));
#367048=CARTESIAN_POINT('Ctrl Pts',(1.47617461089027,0.327978621958125,
-3.24427896544678));
#367049=CARTESIAN_POINT('Ctrl Pts',(1.51191594848997,-0.0608250166043019,
-3.26587916758913));
#367050=CARTESIAN_POINT('Ctrl Pts',(1.49052695146521,-0.260630887484796,
-3.27697949374916));
#367051=CARTESIAN_POINT('Ctrl Pts',(1.37288845797995,-0.634294366679431,
-3.29773857592664));
#367052=CARTESIAN_POINT('Ctrl Pts',(1.28013121590112,-0.805241597497524,
-3.3066108136445));
#367053=CARTESIAN_POINT('Ctrl Pts',(1.03434044541333,-1.10348098533582,
-3.32672085504324));
#367054=CARTESIAN_POINT('Ctrl Pts',(0.883340843740472,-1.22769128682558,
-3.33743611291852));
#367055=CARTESIAN_POINT('Ctrl Pts',(0.537967582982333,-1.41426044671337,
-3.35923536833787));
#367056=CARTESIAN_POINT('Ctrl Pts',(0.345930252409157,-1.47305589754972,
-3.37010797568062));
#367057=CARTESIAN_POINT('Ctrl Pts',(0.0987335442719462,-1.49756561069993,
-3.38268205821138));
#367058=CARTESIAN_POINT('Ctrl Pts',(0.0493410623683693,-1.5,-3.38512607702997));
#367059=CARTESIAN_POINT('Ctrl Pts',(2.0372592501871E-13,-1.5,-3.38749999999999));
#367060=CARTESIAN_POINT('Origin',(0.,2.16840434497101E-16,-9.7));
#367061=CARTESIAN_POINT('',(-9.36276598708176E-14,-1.5,-3.95000000000001));
#367062=CARTESIAN_POINT('',(1.68390526155976E-14,-1.5,-3.8875));
#367063=CARTESIAN_POINT('',(-1.83697019872103E-16,-1.5,-9.7));
#367064=CARTESIAN_POINT('Ctrl Pts',(-1.88182802673964E-13,-1.5,-3.95000000000001));
#367065=CARTESIAN_POINT('Ctrl Pts',(0.135231780044054,-1.50000000000002,
-3.94349365794904));
#367066=CARTESIAN_POINT('Ctrl Pts',(0.270091652890841,-1.48171749714704,
-3.93649736198997));
#367067=CARTESIAN_POINT('Ctrl Pts',(0.591701203054428,-1.39250952169454,
-3.91854591597511));
#367068=CARTESIAN_POINT('Ctrl Pts',(0.770114601928998,-1.30234851268668,
-3.90745752484706));
#367069=CARTESIAN_POINT('Ctrl Pts',(1.07578737076159,-1.06254064857899,
-3.88608950734106));
#367070=CARTESIAN_POINT('Ctrl Pts',(1.20195921834089,-0.917403757532496,
-3.87598748118721));
#367071=CARTESIAN_POINT('Ctrl Pts',(1.39726514048798,-0.580627582297759,
-3.85723592687019));
#367072=CARTESIAN_POINT('Ctrl Pts',(1.46184639615906,-0.39057002758959,
-3.84669833486606));
#367073=CARTESIAN_POINT('Ctrl Pts',(1.51269818200308,0.000576252643117829,
-3.82496798596425));
#367074=CARTESIAN_POINT('Ctrl Pts',(1.49973660386404,0.197615433066233,
-3.81402136482963));
#367075=CARTESIAN_POINT('Ctrl Pts',(1.40029435044894,0.570401185793709,
-3.79331104523366));
#367076=CARTESIAN_POINT('Ctrl Pts',(1.31677448459466,0.743154425879645,
-3.78437683009855));
#367077=CARTESIAN_POINT('Ctrl Pts',(1.0844223927983,1.05526976744912,-3.76452791427061));
#367078=CARTESIAN_POINT('Ctrl Pts',(0.935098847945181,1.18959576866844,
-3.75361230405752));
#367079=CARTESIAN_POINT('Ctrl Pts',(0.597548595218118,1.38936178618908,
-3.73182285390887));
#367080=CARTESIAN_POINT('Ctrl Pts',(0.413639769565851,1.45475338707051,
-3.72115810305133));
#367081=CARTESIAN_POINT('Ctrl Pts',(0.0310519172398163,1.51210510409059,
-3.70115773317334));
#367082=CARTESIAN_POINT('Ctrl Pts',(-0.163986821645253,1.50350863135109,
-3.69220764234691));
#367083=CARTESIAN_POINT('Ctrl Pts',(-0.545135657673647,1.41148227548547,
-3.67131332276045));
#367084=CARTESIAN_POINT('Ctrl Pts',(-0.727040565581374,1.32697370289724,
-3.66021395844849));
#367085=CARTESIAN_POINT('Ctrl Pts',(-1.04131881414212,1.09644554015147,
-3.63868967908831));
#367086=CARTESIAN_POINT('Ctrl Pts',(-1.17245071122195,0.954944868213632,
-3.62845001852794));
#367087=CARTESIAN_POINT('Ctrl Pts',(-1.37948364167474,0.622305661029978,
-3.60924916403995));
#367088=CARTESIAN_POINT('Ctrl Pts',(-1.45027427968896,0.432417245938569,
-3.59902318032989));
#367089=CARTESIAN_POINT('Ctrl Pts',(-1.5122245890554,0.0404690730220717,
-3.57724828183453));
#367090=CARTESIAN_POINT('Ctrl Pts',(-1.50455808839533,-0.157382516188904,
-3.56625652687837));
#367091=CARTESIAN_POINT('Ctrl Pts',(-1.41494260791851,-0.532945936441863,
-3.54539189241987));
#367092=CARTESIAN_POINT('Ctrl Pts',(-1.33615682591316,-0.70764727509372,
-3.53629567317408));
#367093=CARTESIAN_POINT('Ctrl Pts',(-1.11244224847975,-1.02568553090108,
-3.51669780455419));
#367094=CARTESIAN_POINT('Ctrl Pts',(-0.96680680985833,-1.16396852008114,
-3.50584972210266));
#367095=CARTESIAN_POINT('Ctrl Pts',(-0.634359896426993,-1.37301589271101,
-3.48404799106065));
#367096=CARTESIAN_POINT('Ctrl Pts',(-0.451765861327982,-1.44343532132478,
-3.47330683621165));
#367097=CARTESIAN_POINT('Ctrl Pts',(-0.174510362890852,-1.49238980262838,
-3.45860752812069));
#367098=CARTESIAN_POINT('Ctrl Pts',(-0.0872440292034471,-1.5,-3.45419753031215));
#367099=CARTESIAN_POINT('Ctrl Pts',(8.19989359106401E-22,-1.5,-3.45));
#367100=CARTESIAN_POINT('Ctrl Pts',(2.05807593189888E-13,-1.5,-3.3875));
#367101=CARTESIAN_POINT('Ctrl Pts',(-0.140029260838789,-1.5,-3.3942371609533));
#367102=CARTESIAN_POINT('Ctrl Pts',(-0.279591813351883,-1.48039732319827,
-3.40149638619188));
#367103=CARTESIAN_POINT('Ctrl Pts',(-0.602949332181216,-1.38738786328683,
-3.41963752817892));
#367104=CARTESIAN_POINT('Ctrl Pts',(-0.778825446680177,-1.29684993574237,
-3.43061431411487));
#367105=CARTESIAN_POINT('Ctrl Pts',(-1.08810807736369,-1.05146177325118,
-3.45231101946858));
#367106=CARTESIAN_POINT('Ctrl Pts',(-1.21772387864441,-0.898137641636366,
-3.46260346435354));
#367107=CARTESIAN_POINT('Ctrl Pts',(-1.40584314148586,-0.556838944498058,
-3.48156450308345));
#367108=CARTESIAN_POINT('Ctrl Pts',(-1.46522861883794,-0.373558785243038,
-3.49174673415317));
#367109=CARTESIAN_POINT('Ctrl Pts',(-1.51300181436644,0.0127280448211617,
-3.51320711360118));
#367110=CARTESIAN_POINT('Ctrl Pts',(-1.49806689799126,0.212458701953946,
-3.52430326121967));
#367111=CARTESIAN_POINT('Ctrl Pts',(-1.39250216908306,0.590429007327594,
-3.5453016115182));
#367112=CARTESIAN_POINT('Ctrl Pts',(-1.30452860073399,0.7654203759335,-3.55433084887599));
#367113=CARTESIAN_POINT('Ctrl Pts',(-1.06733578123864,1.07149557017,-3.57424488245357));
#367114=CARTESIAN_POINT('Ctrl Pts',(-0.920650162759634,1.19987330666118,
-3.58486834579903));
#367115=CARTESIAN_POINT('Ctrl Pts',(-0.580061762350196,1.39780315213869,
-3.60675296411723));
#367116=CARTESIAN_POINT('Ctrl Pts',(-0.387913345294798,1.46282819114682,
-3.61780396022673));
#367117=CARTESIAN_POINT('Ctrl Pts',(0.000164181943814248,1.51202666694766,
-3.63784197328934));
#367118=CARTESIAN_POINT('Ctrl Pts',(0.191793026215588,1.49981555817854,
-3.64673276966012));
#367119=CARTESIAN_POINT('Ctrl Pts',(0.565239014991216,1.40310163880413,
-3.6673866959328));
#367120=CARTESIAN_POINT('Ctrl Pts',(0.743025460494158,1.31760999323215,
-3.67831521821281));
#367121=CARTESIAN_POINT('Ctrl Pts',(1.05846051210802,1.08127713162049,-3.700056395921));
#367122=CARTESIAN_POINT('Ctrl Pts',(1.19228276290732,0.931658386013542,
-3.71065099823141));
#367123=CARTESIAN_POINT('Ctrl Pts',(1.38952397062882,0.596198198774931,
-3.72945910879692));
#367124=CARTESIAN_POINT('Ctrl Pts',(1.45392729091196,0.415183262171618,
-3.73943426321269));
#367125=CARTESIAN_POINT('Ctrl Pts',(1.51265330275542,0.0314178396428978,
-3.76075456446429));
#367126=CARTESIAN_POINT('Ctrl Pts',(1.50361722287959,-0.168066484823331,
-3.77183702693463));
#367127=CARTESIAN_POINT('Ctrl Pts',(1.40921555701814,-0.549854287798661,
-3.79304746043326));
#367128=CARTESIAN_POINT('Ctrl Pts',(1.32564340431154,-0.728620246368115,
-3.80229273659395));
#367129=CARTESIAN_POINT('Ctrl Pts',(1.0963004264774,-1.04174588564233,-3.82202494018401));
#367130=CARTESIAN_POINT('Ctrl Pts',(0.953608685826855,-1.17376398194826,
-3.83255736909882));
#367131=CARTESIAN_POINT('Ctrl Pts',(0.619670176697447,-1.38061497341427,
-3.85436985398443));
#367132=CARTESIAN_POINT('Ctrl Pts',(0.430041132846712,-1.45091992434412,
-3.86544630091415));
#367133=CARTESIAN_POINT('Ctrl Pts',(0.155211736207756,-1.4939816801484,
-3.87986519630849));
#367134=CARTESIAN_POINT('Ctrl Pts',(0.0775835479173541,-1.5,-3.88376725981044));
#367135=CARTESIAN_POINT('Ctrl Pts',(3.38618022510672E-14,-1.5,-3.8875));
#367136=CARTESIAN_POINT('Origin',(0.,2.16840434497101E-16,-9.7));
#367137=CARTESIAN_POINT('',(-8.50234748894081E-14,-1.5,-4.45000000000001));
#367138=CARTESIAN_POINT('',(-8.67872971602131E-15,-1.5,-4.38750000000001));
#367139=CARTESIAN_POINT('',(-1.83697019872103E-16,-1.5,-9.7));
#367140=CARTESIAN_POINT('Ctrl Pts',(-1.71841707530263E-13,-1.5,-4.45));
#367141=CARTESIAN_POINT('Ctrl Pts',(0.166531914299599,-1.50000000000002,
-4.44198772953754));
#367142=CARTESIAN_POINT('Ctrl Pts',(0.332117043998036,-1.47227294080272,
-4.43325081518161));
#367143=CARTESIAN_POINT('Ctrl Pts',(0.675932825307817,-1.35345201347111,
-4.41340838937594));
#367144=CARTESIAN_POINT('Ctrl Pts',(0.847457115836254,-1.25320965332295,
-4.40237141309606));
#367145=CARTESIAN_POINT('Ctrl Pts',(1.13691812902165,-0.996746171624119,
-4.38132072800311));
#367146=CARTESIAN_POINT('Ctrl Pts',(1.25384871279216,-0.844940101725643,
-4.37194111676252));
#367147=CARTESIAN_POINT('Ctrl Pts',(1.42888981888619,-0.497816171315387,
-4.35265645396195));
#367148=CARTESIAN_POINT('Ctrl Pts',(1.48221684129832,-0.304232262081196,
-4.34190179233783));
#367149=CARTESIAN_POINT('Ctrl Pts',(1.5099890379016,0.088078041336461,-4.32010677548129));
#367150=CARTESIAN_POINT('Ctrl Pts',(1.48586312548998,0.28292349174859,-4.30928202823617));
#367151=CARTESIAN_POINT('Ctrl Pts',(1.36554003428657,0.649551699860725,
-4.28891379445217));
#367152=CARTESIAN_POINT('Ctrl Pts',(1.27164877018827,0.818245178988515,
-4.28011986389887));
#367153=CARTESIAN_POINT('Ctrl Pts',(1.02002676734894,1.117806391016,-4.25969254986422));
#367154=CARTESIAN_POINT('Ctrl Pts',(0.862190388629051,1.24360767462841,
-4.24860416345206));
#367155=CARTESIAN_POINT('Ctrl Pts',(0.513302369906706,1.42249008150699,
-4.22684932507823));
#367156=CARTESIAN_POINT('Ctrl Pts',(0.326934852408628,1.47651275693882,
-4.21638208383882));
#367157=CARTESIAN_POINT('Ctrl Pts',(-0.0603370709084466,1.51162109260476,
-4.19677422319448));
#367158=CARTESIAN_POINT('Ctrl Pts',(-0.257685646017792,1.4907219683773,
-4.1873443704748));
#367159=CARTESIAN_POINT('Ctrl Pts',(-0.633891516278368,1.37373098968563,
-4.16599440769455));
#367160=CARTESIAN_POINT('Ctrl Pts',(-0.808949118249591,1.27849692188573,
-4.15492655412052));
#367161=CARTESIAN_POINT('Ctrl Pts',(-1.10662584179872,1.03031748334567,
-4.13371070278836));
#367162=CARTESIAN_POINT('Ctrl Pts',(-1.22817582784007,0.881883674541403,
-4.1239935374745));
#367163=CARTESIAN_POINT('Ctrl Pts',(-1.41350113107434,0.539952906895013,
-4.10499738371637));
#367164=CARTESIAN_POINT('Ctrl Pts',(-1.4725343002586,0.3480690531609,-4.09433716962003));
#367165=CARTESIAN_POINT('Ctrl Pts',(-1.51199443291843,-0.0437630945133086,
-4.07256871697146));
#367166=CARTESIAN_POINT('Ctrl Pts',(-1.49350167119399,-0.239798016752632,
-4.06167788795817));
#367167=CARTESIAN_POINT('Ctrl Pts',(-1.3837481189278,-0.609585871565706,
-4.04113411824633));
#367168=CARTESIAN_POINT('Ctrl Pts',(-1.29516287259196,-0.780322278400673,
-4.03230460058346));
#367169=CARTESIAN_POINT('Ctrl Pts',(-1.05268606270819,-1.08721665840631,
-4.01211358573953));
#367170=CARTESIAN_POINT('Ctrl Pts',(-0.89813822328151,-1.21799821368605,
-4.00104507836823));
#367171=CARTESIAN_POINT('Ctrl Pts',(-0.553550220567405,-1.40738923330208,
-3.97920521870169));
#367172=CARTESIAN_POINT('Ctrl Pts',(-0.368264244678165,-1.46681995203088,
-3.96863978973227));
#367173=CARTESIAN_POINT('Ctrl Pts',(-0.117999612449124,-1.49652294866404,
-3.95577384376029));
#367174=CARTESIAN_POINT('Ctrl Pts',(-0.0589691261687392,-1.49999999999999,
-3.95283715340561));
#367175=CARTESIAN_POINT('Ctrl Pts',(-1.87071622721763E-13,-1.5,-3.95));
#367176=CARTESIAN_POINT('Ctrl Pts',(3.4104663537704E-14,-1.5,-3.8875));
#367177=CARTESIAN_POINT('Ctrl Pts',(-0.112457791852702,-1.5,-3.89291062803322));
#367178=CARTESIAN_POINT('Ctrl Pts',(-0.224787631218977,-1.48735641864598,
-3.89866631054274));
#367179=CARTESIAN_POINT('Ctrl Pts',(-0.524844452862437,-1.41863092322023,
-3.91501184264468));
#367180=CARTESIAN_POINT('Ctrl Pts',(-0.704500440241314,-1.33852372035449,
-3.92588074544717));
#367181=CARTESIAN_POINT('Ctrl Pts',(-1.02631289747861,-1.11184373287966,
-3.9476606208338));
#367182=CARTESIAN_POINT('Ctrl Pts',(-1.164487448864,-0.96618224120435,-3.95835469958346));
#367183=CARTESIAN_POINT('Ctrl Pts',(-1.37129796079268,-0.63689936401491,
-3.97745162156649));
#367184=CARTESIAN_POINT('Ctrl Pts',(-1.44088801771752,-0.45823039515529,
-3.98704275582471));
#367185=CARTESIAN_POINT('Ctrl Pts',(-1.51092172795299,-0.0773713183246262,
-4.00820159342641));
#367186=CARTESIAN_POINT('Ctrl Pts',(-1.50800092734712,0.121676946614712,
-4.01925983036749));
#367187=CARTESIAN_POINT('Ctrl Pts',(-1.42532298188988,0.507299084571875,
-4.04068328247622));
#367188=CARTESIAN_POINT('Ctrl Pts',(-1.34636387258557,0.690061032852196,
-4.05022473333497));
#367189=CARTESIAN_POINT('Ctrl Pts',(-1.12516572374012,1.01039983755458,
-4.06976543436394));
#367190=CARTESIAN_POINT('Ctrl Pts',(-0.986663972320751,1.14602806404199,
-4.0801965537218));
#367191=CARTESIAN_POINT('Ctrl Pts',(-0.65978368952105,1.36181310646325,
-4.10191761761688));
#367192=CARTESIAN_POINT('Ctrl Pts',(-0.472883402989013,1.43744329523372,
-4.11301070042224));
#367193=CARTESIAN_POINT('Ctrl Pts',(-0.088295867177473,1.50961319637537,
-4.13351889634238));
#367194=CARTESIAN_POINT('Ctrl Pts',(0.105065807819668,1.50853894991074,
-4.14231778798253));
#367195=CARTESIAN_POINT('Ctrl Pts',(0.483598568783563,1.43314108124307,
-4.1626243391766));
#367196=CARTESIAN_POINT('Ctrl Pts',(0.664981538209517,1.35850999407786,
-4.17342421711657));
#367197=CARTESIAN_POINT('Ctrl Pts',(0.992936135736941,1.14175588414345,
-4.19522388754512));
#367198=CARTESIAN_POINT('Ctrl Pts',(1.13538582934671,1.00022493250985,-4.20600891694757));
#367199=CARTESIAN_POINT('Ctrl Pts',(1.35179690425842,0.677274072965561,
-4.22539185685346));
#367200=CARTESIAN_POINT('Ctrl Pts',(1.4266010967402,0.500884954451108,-4.23467305808605));
#367201=CARTESIAN_POINT('Ctrl Pts',(1.50781525845693,0.123009737984317,
-4.25566612566754));
#367202=CARTESIAN_POINT('Ctrl Pts',(1.51094277891903,-0.0754241163179732,
-4.26669022868434));
#367203=CARTESIAN_POINT('Ctrl Pts',(1.4400335667351,-0.464710305168755,
-4.28831723917605));
#367204=CARTESIAN_POINT('Ctrl Pts',(1.36570752133438,-0.651510534190223,
-4.29822321441556));
#367205=CARTESIAN_POINT('Ctrl Pts',(1.15258764832469,-0.978902033192879,
-4.31757115739218));
#367206=CARTESIAN_POINT('Ctrl Pts',(1.01827836840078,-1.11794241172047,
-4.32789534837228));
#367207=CARTESIAN_POINT('Ctrl Pts',(0.698538920278946,-1.34225976346303,
-4.34950985729099));
#367208=CARTESIAN_POINT('Ctrl Pts',(0.51445103527626,-1.42301366315333,
-4.36060995358802));
#367209=CARTESIAN_POINT('Ctrl Pts',(0.214614486740088,-1.48847859698552,
-4.37685431663842));
#367210=CARTESIAN_POINT('Ctrl Pts',(0.107350430474416,-1.5,-4.38233510000567));
#367211=CARTESIAN_POINT('Ctrl Pts',(-1.85615411929518E-14,-1.5,-4.38750000000001));
#367212=CARTESIAN_POINT('Origin',(0.,2.16840434497101E-16,-9.7));
#367213=CARTESIAN_POINT('',(2.85080663018025E-8,-1.5,-4.94999999725681));
#367214=CARTESIAN_POINT('',(-9.36107910998493E-14,-1.5,-4.88750000000001));
#367215=CARTESIAN_POINT('',(-1.83697019872103E-16,-1.5,-9.7));
#367216=CARTESIAN_POINT('Ctrl Pts',(2.85743037217734E-8,-1.5,-4.94999999862521));
#367217=CARTESIAN_POINT('Ctrl Pts',(0.195910416521886,-1.499999996268,-4.94057425558667));
#367218=CARTESIAN_POINT('Ctrl Pts',(0.390036215857167,-1.46161847367431,
-4.93016822030604));
#367219=CARTESIAN_POINT('Ctrl Pts',(0.752265960510316,-1.31239413191948,
-4.9085953129864));
#367220=CARTESIAN_POINT('Ctrl Pts',(0.916863851397284,-1.20318262903278,
-4.8976424404108));
#367221=CARTESIAN_POINT('Ctrl Pts',(1.19093071414502,-0.931584875463727,
-4.87691201028527));
#367222=CARTESIAN_POINT('Ctrl Pts',(1.29930258487063,-0.773285365167594,
-4.86796029806485));
#367223=CARTESIAN_POINT('Ctrl Pts',(1.4546550758443,-0.416586025147008,
-4.84814366806371));
#367224=CARTESIAN_POINT('Ctrl Pts',(1.49700859427159,-0.220254463497417,
-4.83723635908318));
#367225=CARTESIAN_POINT('Ctrl Pts',(1.5026082262154,0.172000542307146,-4.81544441431626));
#367226=CARTESIAN_POINT('Ctrl Pts',(1.46793179708167,0.36415166339195,-4.80476935203377));
#367227=CARTESIAN_POINT('Ctrl Pts',(1.32755011756857,0.724554399049284,
-4.78474697783058));
#367228=CARTESIAN_POINT('Ctrl Pts',(1.22324763612743,0.889402637915464,
-4.77581456716931));
#367229=CARTESIAN_POINT('Ctrl Pts',(0.954072389203067,1.17440610602936,
-4.75494710406024));
#367230=CARTESIAN_POINT('Ctrl Pts',(0.790288222939562,1.29031783605482,
-4.74384726440832));
#367231=CARTESIAN_POINT('Ctrl Pts',(0.433936319256726,1.44853778172871,
-4.72230727695758));
#367232=CARTESIAN_POINT('Ctrl Pts',(0.245911886995276,1.49201616816243,
-4.71205321428606));
#367233=CARTESIAN_POINT('Ctrl Pts',(-0.145430304789549,1.50631428890775,
-4.69282758428434));
#367234=CARTESIAN_POINT('Ctrl Pts',(-0.34512098777978,1.47345268809556,
-4.68265793340284));
#367235=CARTESIAN_POINT('Ctrl Pts',(-0.71590585867546,1.33265493519117,
-4.66090748929246));
#367236=CARTESIAN_POINT('Ctrl Pts',(-0.883887722705555,1.22769535459211,
-4.64990991418554));
#367237=CARTESIAN_POINT('Ctrl Pts',(-1.165370081398,0.963327528173154,-4.62902353715474));
#367238=CARTESIAN_POINT('Ctrl Pts',(-1.27785210651291,0.808186899595166,
-4.61989927219972));
#367239=CARTESIAN_POINT('Ctrl Pts',(-1.44275937897357,0.456073158691434,
-4.60033739770507));
#367240=CARTESIAN_POINT('Ctrl Pts',(-1.49044284487975,0.260991823984585,
-4.58949954577691));
#367241=CARTESIAN_POINT('Ctrl Pts',(-1.50676289141006,-0.131447377579266,
-4.56769736791225));
#367242=CARTESIAN_POINT('Ctrl Pts',(-1.47716553931379,-0.324972780132217,
-4.55694595665931));
#367243=CARTESIAN_POINT('Ctrl Pts',(-1.3464895819,-0.688424820958513,-4.5367541766134));
#367244=CARTESIAN_POINT('Ctrl Pts',(-1.2472828805662,-0.855131192483876,
-4.52792294800186));
#367245=CARTESIAN_POINT('Ctrl Pts',(-0.986631235378525,-1.14728655357929,
-4.50726691317862));
#367246=CARTESIAN_POINT('Ctrl Pts',(-0.825673461623653,-1.26805370866375,
-4.49616818548137));
#367247=CARTESIAN_POINT('Ctrl Pts',(-0.472812948553632,-1.43638517702935,
-4.47451530200948));
#367248=CARTESIAN_POINT('Ctrl Pts',(-0.285522965064557,-1.48500905798133,
-4.46415364511771));
#367249=CARTESIAN_POINT('Ctrl Pts',(-0.0627541717646307,-1.4990164725753,
-4.45304658170298));
#367250=CARTESIAN_POINT('Ctrl Pts',(-0.0313615984996725,-1.5,-4.45150888561133));
#367251=CARTESIAN_POINT('Ctrl Pts',(-1.69863252758944E-13,-1.5,-4.45000000000001));
#367252=CARTESIAN_POINT('Ctrl Pts',(-1.71737624121705E-14,-1.5,-4.38750000000001));
#367253=CARTESIAN_POINT('Ctrl Pts',(-0.0829221129230426,-1.5,-4.39148959201816));
#367254=CARTESIAN_POINT('Ctrl Pts',(-0.165877183164973,-1.49312504344208,
-4.39567174071156));
#367255=CARTESIAN_POINT('Ctrl Pts',(-0.445313583363476,-1.44627570677349,
-4.41041750124758));
#367256=CARTESIAN_POINT('Ctrl Pts',(-0.633989368825423,-1.37406727321907,
-4.42150095902903));
#367257=CARTESIAN_POINT('Ctrl Pts',(-0.965446337687612,-1.16401532744184,
-4.4432829661504));
#367258=CARTESIAN_POINT('Ctrl Pts',(-1.10665945088798,-1.03069955306717,
-4.45378030118187));
#367259=CARTESIAN_POINT('Ctrl Pts',(-1.33311870096298,-0.715008228143621,
-4.47344503040124));
#367260=CARTESIAN_POINT('Ctrl Pts',(-1.41506355227756,-0.534836499656983,
-4.48278686113017));
#367261=CARTESIAN_POINT('Ctrl Pts',(-1.50533076614708,-0.151675795448859,
-4.50407356691951));
#367262=CARTESIAN_POINT('Ctrl Pts',(-1.51220048320158,0.0476751903314799,
-4.51514862168509));
#367263=CARTESIAN_POINT('Ctrl Pts',(-1.44946690860152,0.430423689729183,
-4.53641242720718));
#367264=CARTESIAN_POINT('Ctrl Pts',(-1.38323455609893,0.610602562238479,
-4.54624361200806));
#367265=CARTESIAN_POINT('Ctrl Pts',(-1.18261816761641,0.943898733305205,
-4.56515399947332));
#367266=CARTESIAN_POINT('Ctrl Pts',(-1.04725098352344,1.09214011438375,
-4.57578467229569));
#367267=CARTESIAN_POINT('Ctrl Pts',(-0.729538359551367,1.32509637034778,
-4.59754163515374));
#367268=CARTESIAN_POINT('Ctrl Pts',(-0.551075941165947,1.40869768735186,
-4.60845017106733));
#367269=CARTESIAN_POINT('Ctrl Pts',(-0.176716557605994,1.5016872279536,
-4.62904458810115));
#367270=CARTESIAN_POINT('Ctrl Pts',(0.0151935172421368,1.51197132588372,
-4.63789846160904));
#367271=CARTESIAN_POINT('Ctrl Pts',(0.402703160445184,1.45879716567031,
-4.65801958801637));
#367272=CARTESIAN_POINT('Ctrl Pts',(0.593985367226513,1.39191361876467,
-4.66908053378401));
#367273=CARTESIAN_POINT('Ctrl Pts',(0.932271564999293,1.19083659572109,
-4.69094180892527));
#367274=CARTESIAN_POINT('Ctrl Pts',(1.07756911177044,1.06117073233087,-4.70153426994229));
#367275=CARTESIAN_POINT('Ctrl Pts',(1.31202288914959,0.752624332817159,
-4.72138516588565));
#367276=CARTESIAN_POINT('Ctrl Pts',(1.39846495836364,0.576324684903343,
-4.73048196194982));
#367277=CARTESIAN_POINT('Ctrl Pts',(1.5001497547969,0.197009390524566,-4.75155503385975));
#367278=CARTESIAN_POINT('Ctrl Pts',(1.51302651117266,-0.0026546548410443,
-4.76264748082451));
#367279=CARTESIAN_POINT('Ctrl Pts',(1.46143097252156,-0.388059744347202,
-4.78405887468596));
#367280=CARTESIAN_POINT('Ctrl Pts',(1.40030268792451,-0.570567507184692,
-4.7941981948436));
#367281=CARTESIAN_POINT('Ctrl Pts',(1.20899755076974,-0.909843039816958,
-4.81304683554539));
#367282=CARTESIAN_POINT('Ctrl Pts',(1.07792543005673,-1.06189520343739,
-4.82346871088358));
#367283=CARTESIAN_POINT('Ctrl Pts',(0.766452670177431,-1.30417307550099,
-4.84518439192103));
#367284=CARTESIAN_POINT('Ctrl Pts',(0.589896936198974,-1.39296218739351,
-4.85614529785189));
#367285=CARTESIAN_POINT('Ctrl Pts',(0.270346234866123,-1.48167998739823,
-4.87398407147154));
#367286=CARTESIAN_POINT('Ctrl Pts',(0.135370689680846,-1.50000000000002,
-4.88098697465604));
#367287=CARTESIAN_POINT('Ctrl Pts',(-1.88703219716757E-13,-1.5,-4.88750000000001));
#367288=CARTESIAN_POINT('Origin',(0.,2.16840434497101E-16,-9.7));
#367289=CARTESIAN_POINT('',(5.08393723981206E-14,-1.5,-5.44999999999999));
#367290=CARTESIAN_POINT('',(-5.10233297646163E-14,-1.5,-5.38750000000001));
#367291=CARTESIAN_POINT('',(-1.83697019872103E-16,-1.5,-9.7));
#367292=CARTESIAN_POINT('Ctrl Pts',(1.01862441816113E-13,-1.5,-5.44999999999999));
#367293=CARTESIAN_POINT('Ctrl Pts',(0.0263651739551401,-1.5,-5.44873150497664));
#367294=CARTESIAN_POINT('Ctrl Pts',(0.0527523821946788,-1.49930488812725,
-5.44744264116515));
#367295=CARTESIAN_POINT('Ctrl Pts',(0.277718326846129,-1.4874199513975,
-5.43628882497519));
#367296=CARTESIAN_POINT('Ctrl Pts',(0.472215788715003,-1.43754461477542,
-5.42554563546068));
#367297=CARTESIAN_POINT('Ctrl Pts',(0.826559672875883,-1.26674832897375,
-5.40375291611291));
#367298=CARTESIAN_POINT('Ctrl Pts',(0.983733117419562,-1.14896970203481,
-5.39291927671044));
#367299=CARTESIAN_POINT('Ctrl Pts',(1.24210426384262,-0.862412663408363,
-5.37252847139263));
#367300=CARTESIAN_POINT('Ctrl Pts',(1.34181572159714,-0.697214195621655,
-5.36373412197897));
#367301=CARTESIAN_POINT('Ctrl Pts',(1.47683335814032,-0.330060296931495,
-5.34333668316285));
#367302=CARTESIAN_POINT('Ctrl Pts',(1.50762432316895,-0.130505577948834,
-5.33225030988604));
#367303=CARTESIAN_POINT('Ctrl Pts',(1.48953296953489,0.261294957627765,
-5.31048361346512));
#367304=CARTESIAN_POINT('Ctrl Pts',(1.44379939786353,0.449939486882149,
-5.30000336183987));
#367305=CARTESIAN_POINT('Ctrl Pts',(1.28188447478999,0.803321599497433,
-5.28037102225013));
#367306=CARTESIAN_POINT('Ctrl Pts',(1.16584828536497,0.964035863125838,
-5.27097979447342));
#367307=CARTESIAN_POINT('Ctrl Pts',(0.877599962231806,1.2323976979204,-5.24965694514959));
#367308=CARTESIAN_POINT('Ctrl Pts',(0.707936356116261,1.33708986900095,
-5.23858588523104));
#367309=CARTESIAN_POINT('Ctrl Pts',(0.344567510283842,1.47223165337793,
-5.21734935502975));
#367310=CARTESIAN_POINT('Ctrl Pts',(0.155317568062389,1.50400359956028,
-5.20758393107645));
#367311=CARTESIAN_POINT('Ctrl Pts',(-0.233539223820948,1.49498906414918,
-5.18862464619252));
#367312=CARTESIAN_POINT('Ctrl Pts',(-0.429393951225143,1.45090598297018,
-5.17797705119403));
#367313=CARTESIAN_POINT('Ctrl Pts',(-0.789125099850543,1.29048502131858,
-5.15621334041248));
#367314=CARTESIAN_POINT('Ctrl Pts',(-0.95012792291364,1.17700237915228,
-5.14531479286043));
#367315=CARTESIAN_POINT('Ctrl Pts',(-1.21650593922147,0.898020105215934,
-5.12474916696596));
#367316=CARTESIAN_POINT('Ctrl Pts',(-1.320631925763,0.736378716832192,-5.11590992871289));
#367317=CARTESIAN_POINT('Ctrl Pts',(-1.46653676135899,0.373481609252619,
-5.0957489782918));
#367318=CARTESIAN_POINT('Ctrl Pts',(-1.50326970020796,0.174305383486191,
-5.08468363241589));
#367319=CARTESIAN_POINT('Ctrl Pts',(-1.49640740843039,-0.218981562746956,
-5.06283435762516));
#367320=CARTESIAN_POINT('Ctrl Pts',(-1.45589167669697,-0.409370563639839,
-5.05225719090889));
#367321=CARTESIAN_POINT('Ctrl Pts',(-1.30421536216214,-0.766134745524016,
-5.03243695858199));
#367322=CARTESIAN_POINT('Ctrl Pts',(-1.19383411420971,-0.928820751969231,
-5.02330446082362));
#367323=CARTESIAN_POINT('Ctrl Pts',(-0.914679147103492,-1.20523228366345,
-5.00219551310397));
#367324=CARTESIAN_POINT('Ctrl Pts',(-0.747739827958748,-1.31533367575935,
-4.9911052693641));
#367325=CARTESIAN_POINT('Ctrl Pts',(-0.387629444244665,-1.46153354298933,
-4.96971834302643));
#367326=CARTESIAN_POINT('Ctrl Pts',(-0.198917662169693,-1.49893060653779,
-4.95960013585729));
#367327=CARTESIAN_POINT('Ctrl Pts',(-0.00548928539186333,-1.49999246786982,
-4.95026431259238));
#367328=CARTESIAN_POINT('Ctrl Pts',(-0.00274446328429652,-1.50000000005228,
-4.95013204305278));
#367329=CARTESIAN_POINT('Ctrl Pts',(2.85743048114312E-8,-1.5,-4.94999999862521));
#367330=CARTESIAN_POINT('Ctrl Pts',(-1.87037885179826E-13,-1.5,-4.88750000000001));
#367331=CARTESIAN_POINT('Ctrl Pts',(-0.0540462695308795,-1.49999999999999,
-4.8901003023552));
#367332=CARTESIAN_POINT('Ctrl Pts',(-0.108147676289032,-1.49707922019035,
-4.89278439027397));
#367333=CARTESIAN_POINT('Ctrl Pts',(-0.359814125721349,-1.46972714332125,
-4.90565247788081));
#367334=CARTESIAN_POINT('Ctrl Pts',(-0.551295619407549,-1.40911968988848,
-4.91654867591433));
#367335=CARTESIAN_POINT('Ctrl Pts',(-0.894744498290115,-1.21937731862514,
-4.93834348922795));
#367336=CARTESIAN_POINT('Ctrl Pts',(-1.04444802750409,-1.09388814473448,
-4.94903191402133));
#367337=CARTESIAN_POINT('Ctrl Pts',(-1.28764107828231,-0.793268603442221,
-4.96908308794599));
#367338=CARTESIAN_POINT('Ctrl Pts',(-1.37895629232874,-0.621109605663026,
-4.9779939107965));
#367339=CARTESIAN_POINT('Ctrl Pts',(-1.4929637296001,-0.246131760036213,
-4.99882601333133));
#367340=CARTESIAN_POINT('Ctrl Pts',(-1.5124042662344,-0.046327287996343,
-5.00992626177799));
#367341=CARTESIAN_POINT('Ctrl Pts',(-1.47302330444493,0.341756093908819,
-5.0314864496616));
#367342=CARTESIAN_POINT('Ctrl Pts',(-1.41747667306572,0.52666588745438,
-5.04175921596969));
#367343=CARTESIAN_POINT('Ctrl Pts',(-1.23585023889997,0.873309400994758,
-5.06101718894416));
#367344=CARTESIAN_POINT('Ctrl Pts',(-1.10852292020812,1.03014952423744,
-5.07111476403007));
#367345=CARTESIAN_POINT('Ctrl Pts',(-0.802682556237449,1.28227517515059,
-5.09283300570551));
#367346=CARTESIAN_POINT('Ctrl Pts',(-0.628176408674604,1.37619980171365,
-5.10383795404925));
#367347=CARTESIAN_POINT('Ctrl Pts',(-0.258965513662954,1.48963680612895,
-5.12475264941824));
#367348=CARTESIAN_POINT('Ctrl Pts',(-0.0684870903143073,1.51042170292824,
-5.13391542158291));
#367349=CARTESIAN_POINT('Ctrl Pts',(0.319042014244513,1.47911051435621,
-5.15343017955735));
#367350=CARTESIAN_POINT('Ctrl Pts',(0.512102500769454,1.42382780144004,
-5.16425443746044));
#367351=CARTESIAN_POINT('Ctrl Pts',(0.861107381613573,1.24344002427904,
-5.1860567142069));
#367352=CARTESIAN_POINT('Ctrl Pts',(1.01457887995497,1.12173564265987,-5.19682129238079));
#367353=CARTESIAN_POINT('Ctrl Pts',(1.2653628380366,0.828102729138014,-5.21704361100975));
#367354=CARTESIAN_POINT('Ctrl Pts',(1.36088590783901,0.65945994173573,-5.22586333657024));
#367355=CARTESIAN_POINT('Ctrl Pts',(1.48546319186562,0.288353241746187,
-5.24648037545855));
#367356=CARTESIAN_POINT('Ctrl Pts',(1.51059193401268,0.0885961576228984,
-5.25757799124318));
#367357=CARTESIAN_POINT('Ctrl Pts',(1.48185374683415,-0.301494364037364,
-5.27924968689097));
#367358=CARTESIAN_POINT('Ctrl Pts',(1.43119950302677,-0.488341944754652,
-5.28963010804193));
#367359=CARTESIAN_POINT('Ctrl Pts',(1.2594817962717,-0.838410696396134,
-5.30907837202201));
#367360=CARTESIAN_POINT('Ctrl Pts',(1.13789799615601,-0.997215134410307,
-5.31878661086771));
#367361=CARTESIAN_POINT('Ctrl Pts',(0.840911554960286,-1.25762727854883,
-5.34030904835239));
#367362=CARTESIAN_POINT('Ctrl Pts',(0.668770495030703,-1.35702049989082,
-5.35135211177486));
#367363=CARTESIAN_POINT('Ctrl Pts',(0.326816869742832,-1.47315072340218,
-5.37103020278437));
#367364=CARTESIAN_POINT('Ctrl Pts',(0.163873689066774,-1.50000000000001,
-5.37961562345869));
#367365=CARTESIAN_POINT('Ctrl Pts',(-1.03146657881581E-13,-1.5,-5.38750000000001));
#367366=CARTESIAN_POINT('Origin',(0.,2.16840434497101E-16,-9.7));
#367367=CARTESIAN_POINT('',(9.74881735715278E-14,-1.5,-5.94999999999999));
#367368=CARTESIAN_POINT('',(-4.32989591281128E-8,-1.5,-5.88750000416645));
#367369=CARTESIAN_POINT('',(-1.83697019872103E-16,-1.5,-9.7));
#367370=CARTESIAN_POINT('Ctrl Pts',(1.95160044162928E-13,-1.5,-5.94999999999999));
#367371=CARTESIAN_POINT('Ctrl Pts',(0.0546724918751179,-1.5,-5.94736956850821));
#367372=CARTESIAN_POINT('Ctrl Pts',(0.109400508428987,-1.49701114857146,
-5.94465344193329));
#367373=CARTESIAN_POINT('Ctrl Pts',(0.361659483794658,-1.46927425572993,
-5.93174615707662));
#367374=CARTESIAN_POINT('Ctrl Pts',(0.553065678554439,-1.40842605692642,
-5.92084689449298));
#367375=CARTESIAN_POINT('Ctrl Pts',(0.896256244038983,-1.21826288033519,
-5.89905282025163));
#367376=CARTESIAN_POINT('Ctrl Pts',(1.04578649131481,-1.09260450286954,
-5.88836803239008));
#367377=CARTESIAN_POINT('Ctrl Pts',(1.28863322740306,-0.791668488711237,
-5.86832472962576));
#367378=CARTESIAN_POINT('Ctrl Pts',(1.37975600578144,-0.619347280917291,
-5.85940818227318));
#367379=CARTESIAN_POINT('Ctrl Pts',(1.49327827165981,-0.244195051917849,
-5.83856639177321));
#367380=CARTESIAN_POINT('Ctrl Pts',(1.51245892969766,-0.0443921573901792,
-5.82746623096612));
#367381=CARTESIAN_POINT('Ctrl Pts',(1.47259300132903,0.343592577334264,
-5.80591152348143));
#367382=CARTESIAN_POINT('Ctrl Pts',(1.41682407311496,0.528410655372149,
-5.79564385247932));
#367383=CARTESIAN_POINT('Ctrl Pts',(1.23474322506663,0.874895225824404,
-5.77639470967642));
#367384=CARTESIAN_POINT('Ctrl Pts',(1.10714918922497,1.03164424545367,-5.7662776222734));
#367385=CARTESIAN_POINT('Ctrl Pts',(0.800902451810381,1.28338366753864,
-5.74455055752509));
#367386=CARTESIAN_POINT('Ctrl Pts',(0.626291330195158,1.37705491791357,
-5.73354759684234));
#367387=CARTESIAN_POINT('Ctrl Pts',(0.256949134406888,1.4899864401885,-5.71264062543236));
#367388=CARTESIAN_POINT('Ctrl Pts',(0.0664386026299455,1.5105138274722,
-5.70348857952253));
#367389=CARTESIAN_POINT('Ctrl Pts',(-0.32105371365814,1.47867531398939,
-5.68396094361041));
#367390=CARTESIAN_POINT('Ctrl Pts',(-0.51404007021658,1.42312963011403,
-5.67313294753812));
#367391=CARTESIAN_POINT('Ctrl Pts',(-0.86277756894227,1.24227774632932,
-5.65133064336918));
#367392=CARTESIAN_POINT('Ctrl Pts',(-1.0160658593181,1.12038455171356,-5.64056963498718));
#367393=CARTESIAN_POINT('Ctrl Pts',(-1.26647789513751,0.826407077074905,
-5.62035563933427));
#367394=CARTESIAN_POINT('Ctrl Pts',(-1.36179517096147,0.657593764873694,
-5.61153298693742));
#367395=CARTESIAN_POINT('Ctrl Pts',(-1.48585744571148,0.286295279048441,
-5.59090529328046));
#367396=CARTESIAN_POINT('Ctrl Pts',(-1.5107079190491,0.086532237250619,
-5.57980734651392));
#367397=CARTESIAN_POINT('Ctrl Pts',(-1.48144784744948,-0.303466848535801,
-5.55814073063689));
#367398=CARTESIAN_POINT('Ctrl Pts',(-1.4305530780986,-0.490222727524862,
-5.54776540402639));
#367399=CARTESIAN_POINT('Ctrl Pts',(-1.25835217976544,-0.84012623627136,
-5.52832632020714));
#367400=CARTESIAN_POINT('Ctrl Pts',(-1.13649149405738,-0.998835774444738,
-5.51860070098978));
#367401=CARTESIAN_POINT('Ctrl Pts',(-0.839073707596556,-1.25884976420935,
-5.49706857024008));
#367402=CARTESIAN_POINT('Ctrl Pts',(-0.666814006000366,-1.35797887345876,
-5.48602713511478));
#367403=CARTESIAN_POINT('Ctrl Pts',(-0.325397739255144,-1.47338552249901,
-5.46639499707107));
#367404=CARTESIAN_POINT('Ctrl Pts',(-0.16315592440875,-1.5,-5.45784984307311));
#367405=CARTESIAN_POINT('Ctrl Pts',(1.01377239936085E-13,-1.5,-5.44999999999999));
#367406=CARTESIAN_POINT('Ctrl Pts',(-1.0186296250936E-13,-1.5,-5.38750000000001));
#367407=CARTESIAN_POINT('Ctrl Pts',(-0.0256619673057862,-1.5,-5.38873466197767));
#367408=CARTESIAN_POINT('Ctrl Pts',(-0.0513450144281305,-1.49934147279655,
-5.3899886305808));
#367409=CARTESIAN_POINT('Ctrl Pts',(-0.275621128406905,-1.48780980469279,
-5.40109944425966));
#367410=CARTESIAN_POINT('Ctrl Pts',(-0.47018718093381,-1.43820917050335,
-5.41183830322061));
#367411=CARTESIAN_POINT('Ctrl Pts',(-0.824794258445663,-1.26790258960189,
-5.43363008255048));
#367412=CARTESIAN_POINT('Ctrl Pts',(-0.982152470284429,-1.15032558928547,
-5.44446701083407));
#367413=CARTESIAN_POINT('Ctrl Pts',(-1.24090605577986,-0.864127755771773,
-5.46486623834053));
#367414=CARTESIAN_POINT('Ctrl Pts',(-1.34082836484502,-0.699101034024753,
-5.4736610536653));
#367415=CARTESIAN_POINT('Ctrl Pts',(-1.47636902037079,-0.332148478379624,
-5.49404730675669));
#367416=CARTESIAN_POINT('Ctrl Pts',(-1.50744463298203,-0.132608012550994,
-5.50513288819162));
#367417=CARTESIAN_POINT('Ctrl Pts',(-1.48988989187833,0.259270920023298,
-5.5269039400013));
#367418=CARTESIAN_POINT('Ctrl Pts',(-1.44440501779414,0.448002314883359,
-5.53738901749352));
#367419=CARTESIAN_POINT('Ctrl Pts',(-1.28298157039537,0.801548601297589,
-5.55703047784987));
#367420=CARTESIAN_POINT('Ctrl Pts',(-1.16722005041924,0.962357952463247,
-5.56640759782012));
#367421=CARTESIAN_POINT('Ctrl Pts',(-0.879409087628147,1.23111202588909,
-5.58772030015221));
#367422=CARTESIAN_POINT('Ctrl Pts',(-0.70987313894258,1.33606683349401,
-5.59879251360881));
#367423=CARTESIAN_POINT('Ctrl Pts',(-0.346653687238665,1.4717442380186,
-5.62003673441918));
#367424=CARTESIAN_POINT('Ctrl Pts',(-0.157430484209326,1.50378596490384,
-5.62982045660516));
#367425=CARTESIAN_POINT('Ctrl Pts',(0.231453196392725,1.4953132249182,-5.64876598530023));
#367426=CARTESIAN_POINT('Ctrl Pts',(0.427367482033715,1.45150391708622,
-5.65940884098053));
#367427=CARTESIAN_POINT('Ctrl Pts',(0.787344881840087,1.29157591836,-5.68117070611296));
#367428=CARTESIAN_POINT('Ctrl Pts',(0.94852526786724,1.17829863658823,-5.69207209221169));
#367429=CARTESIAN_POINT('Ctrl Pts',(1.21527890331185,0.899674554409161,
-5.71264584031927));
#367430=CARTESIAN_POINT('Ctrl Pts',(1.31961207830169,0.73819807357228,-5.72148899591266));
#367431=CARTESIAN_POINT('Ctrl Pts',(1.46602444349983,0.375502732956456,
-5.74163873705798));
#367432=CARTESIAN_POINT('Ctrl Pts',(1.5030351545464,0.176348361746048,-5.75270286879189));
#367433=CARTESIAN_POINT('Ctrl Pts',(1.49669919734387,-0.217000356834536,
-5.7745555753797));
#367434=CARTESIAN_POINT('Ctrl Pts',(1.45642873751693,-0.407467369946189,
-5.78513707610813));
#367435=CARTESIAN_POINT('Ctrl Pts',(1.30523012125535,-0.76438740080986,
-5.80496596671167));
#367436=CARTESIAN_POINT('Ctrl Pts',(1.19510931166096,-0.927165031214452,
-5.8140881939672));
#367437=CARTESIAN_POINT('Ctrl Pts',(0.916377607621684,-1.2039459831623,
-5.83518703910676));
#367438=CARTESIAN_POINT('Ctrl Pts',(0.749568638977346,-1.31429650733405,
-5.84627793169071));
#367439=CARTESIAN_POINT('Ctrl Pts',(0.389610289995854,-1.46101002328375,
-5.86767181127388));
#367440=CARTESIAN_POINT('Ctrl Pts',(0.200923816790519,-1.49866618236168,
-5.8777959978675));
#367441=CARTESIAN_POINT('Ctrl Pts',(0.00681097685229299,-1.49998840442069,
-5.88717198462399));
#367442=CARTESIAN_POINT('Ctrl Pts',(0.00340521405330191,-1.50000000009853,
-5.88733616655974));
#367443=CARTESIAN_POINT('Ctrl Pts',(-4.33996891097767E-8,-1.5,-5.88750000208807));
#367444=CARTESIAN_POINT('Origin',(0.,2.16840434497101E-16,-9.7));
#367445=CARTESIAN_POINT('',(4.06290604931913E-15,-1.5,-6.45));
#367446=CARTESIAN_POINT('',(8.47483643639537E-14,-1.5,-6.3875));
#367447=CARTESIAN_POINT('',(-1.83697019872103E-16,-1.5,-9.7));
#367448=CARTESIAN_POINT('Ctrl Pts',(8.30950911851036E-15,-1.5,-6.45));
#367449=CARTESIAN_POINT('Ctrl Pts',(0.0836220240189683,-1.5,-6.44597673349354));
#367450=CARTESIAN_POINT('Ctrl Pts',(0.167275159716708,-1.4930085099386,
-6.44175776206847));
#367451=CARTESIAN_POINT('Ctrl Pts',(0.447311848965298,-1.44565501504088,
-6.42696911571681));
#367452=CARTESIAN_POINT('Ctrl Pts',(0.635861319637451,-1.37319794769801,
-6.41588482876439));
#367453=CARTESIAN_POINT('Ctrl Pts',(0.966990781533922,-1.16272850281152,
-6.39410698163178));
#367454=CARTESIAN_POINT('Ctrl Pts',(1.10800920467463,-1.02924381484293,
-6.3836143215859));
#367455=CARTESIAN_POINT('Ctrl Pts',(1.334089564726,-0.713216352739631,-6.36395848457741));
#367456=CARTESIAN_POINT('Ctrl Pts',(1.4158201412557,-0.532859175839884,
-6.35460328754666));
#367457=CARTESIAN_POINT('Ctrl Pts',(1.50554279496689,-0.149519314526434,
-6.3333066285848));
#367458=CARTESIAN_POINT('Ctrl Pts',(1.51212795197166,0.0498124374358952,
-6.32223264236467));
#367459=CARTESIAN_POINT('Ctrl Pts',(1.44886815250877,0.432426328348405,
-6.30097631509175));
#367460=CARTESIAN_POINT('Ctrl Pts',(1.38239490638562,0.61249579567037,-6.29116340050872));
#367461=CARTESIAN_POINT('Ctrl Pts',(1.18133400021063,0.945505775759388,
-6.27223957592539));
#367462=CARTESIAN_POINT('Ctrl Pts',(1.0457641280893,1.09356425628846,-6.26160423184153));
#367463=CARTESIAN_POINT('Ctrl Pts',(0.727753807144858,1.32607351058838,
-6.23984536274412));
#367464=CARTESIAN_POINT('Ctrl Pts',(0.549203697674222,1.40942514019646,
-6.22893954355222));
#367465=CARTESIAN_POINT('Ctrl Pts',(0.17472459156813,1.50192328426092,-6.20835301626852));
#367466=CARTESIAN_POINT('Ctrl Pts',(-0.0172232732627098,1.51195258899534,
-6.19950336123977));
#367467=CARTESIAN_POINT('Ctrl Pts',(-0.404656715019742,1.45825267216852,
-6.17937129672584));
#367468=CARTESIAN_POINT('Ctrl Pts',(-0.595823034910048,1.39112403379354,
-6.16830911847248));
#367469=CARTESIAN_POINT('Ctrl Pts',(-0.933802532933181,1.18963253496017,
-6.14645108621343));
#367470=CARTESIAN_POINT('Ctrl Pts',(-1.07891560035492,1.05979734012534,
-6.135862797312));
#367471=CARTESIAN_POINT('Ctrl Pts',(-1.31300625698492,0.75092422433093,
-6.11602029657159));
#367472=CARTESIAN_POINT('Ctrl Pts',(-1.39924496724479,0.574450422168306,
-6.10691391234268));
#367473=CARTESIAN_POINT('Ctrl Pts',(-1.50041417045913,0.194957843525356,
-6.08583099130696));
#367474=CARTESIAN_POINT('Ctrl Pts',(-1.51301804316835,-0.00469581672682119,
-6.07473912129295));
#367475=CARTESIAN_POINT('Ctrl Pts',(-1.46091624463761,-0.389981114792215,
-6.05333438251154));
#367476=CARTESIAN_POINT('Ctrl Pts',(-1.399557396858,-0.572385147039804,
-6.04320082516445));
#367477=CARTESIAN_POINT('Ctrl Pts',(-1.20783109806283,-0.911389995950663,
-6.02436722244718));
#367478=CARTESIAN_POINT('Ctrl Pts',(-1.07656661998166,-1.06327239050781,
-6.0139276581398));
#367479=CARTESIAN_POINT('Ctrl Pts',(-0.764805407702597,-1.30513611986922,
-5.99220960289375));
#367480=CARTESIAN_POINT('Ctrl Pts',(-0.588160753060915,-1.39369278579797,
-5.98125087559781));
#367481=CARTESIAN_POINT('Ctrl Pts',(-0.269119198949494,-1.48184688845222,
-5.96345225659501));
#367482=CARTESIAN_POINT('Ctrl Pts',(-0.134752651461745,-1.5,-5.95648328996629));
#367483=CARTESIAN_POINT('Ctrl Pts',(1.96006405550619E-13,-1.5,-5.94999999999999));
#367484=CARTESIAN_POINT('Ctrl Pts',(-4.33996887733157E-8,-1.5,-5.88750000208807));
#367485=CARTESIAN_POINT('Ctrl Pts',(-0.195242606810165,-1.49999999435102,
-5.89689361445685));
#367486=CARTESIAN_POINT('Ctrl Pts',(-0.388722924848865,-1.46187996269871,
-5.90726133036685));
#367487=CARTESIAN_POINT('Ctrl Pts',(-0.750561595655201,-1.31337333001173,
-5.92879548577426));
#367488=CARTESIAN_POINT('Ctrl Pts',(-0.915321653672233,-1.20436028788468,
-5.93975064782067));
#367489=CARTESIAN_POINT('Ctrl Pts',(-1.18973972539303,-0.93310251861447,
-5.96048853148749));
#367490=CARTESIAN_POINT('Ctrl Pts',(-1.29830585366695,-0.774954000507073,
-5.96944699997184));
#367491=CARTESIAN_POINT('Ctrl Pts',(-1.45411392074071,-0.41847063235772,
-5.98925163153569));
#367492=CARTESIAN_POINT('Ctrl Pts',(-1.49672162993495,-0.22219512861367,
-6.00015582618814));
#367493=CARTESIAN_POINT('Ctrl Pts',(-1.50283046342648,0.17007530608529,
-6.02194862811586));
#367494=CARTESIAN_POINT('Ctrl Pts',(-1.46839435017176,0.362294737240242,
-6.03262748540224));
#367495=CARTESIAN_POINT('Ctrl Pts',(-1.32847421282326,0.722844100909313,
-6.05265800560608));
#367496=CARTESIAN_POINT('Ctrl Pts',(-1.22441668040302,0.887780618452159,
-6.06158413106555));
#367497=CARTESIAN_POINT('Ctrl Pts',(-0.955647919996864,1.17312894984812,
-6.08244161661851));
#367498=CARTESIAN_POINT('Ctrl Pts',(-0.791995833525539,1.28927449625884,
-6.09354159647806));
#367499=CARTESIAN_POINT('Ctrl Pts',(-0.435804622016396,1.44797995007156,
-6.11508733896017));
#367500=CARTESIAN_POINT('Ctrl Pts',(-0.247812161776026,1.49170477213654,
-6.12534670881131));
#367501=CARTESIAN_POINT('Ctrl Pts',(0.143437792981978,1.50649233312871,
-6.14458149661943));
#367502=CARTESIAN_POINT('Ctrl Pts',(0.343071986735211,1.47391757420866,
-6.1547305704853));
#367503=CARTESIAN_POINT('Ctrl Pts',(0.71399393589645,1.33368434453721,-6.17647192857588));
#367504=CARTESIAN_POINT('Ctrl Pts',(0.882149412527287,1.22894938002697,
-6.18747161728716));
#367505=CARTESIAN_POINT('Ctrl Pts',(1.16401738391211,0.964960525296338,
-6.20836602012592));
#367506=CARTESIAN_POINT('Ctrl Pts',(1.27671370824356,0.80998253382708,-6.21750097034295));
#367507=CARTESIAN_POINT('Ctrl Pts',(1.44211419342194,0.458108664485862,
-6.23704951863969));
#367508=CARTESIAN_POINT('Ctrl Pts',(1.49007263878478,0.263096120522399,
-6.24788354885988));
#367509=CARTESIAN_POINT('Ctrl Pts',(1.5069482561287,-0.129344586869214,
-6.26968581038164));
#367510=CARTESIAN_POINT('Ctrl Pts',(1.47761524480886,-0.322937556506277,
-6.28044097536147));
#367511=CARTESIAN_POINT('Ctrl Pts',(1.34744177127719,-0.686545509678991,
-6.3006414172044));
#367512=CARTESIAN_POINT('Ctrl Pts',(1.24849578411744,-0.853348254296545,
-6.30946917008806));
#367513=CARTESIAN_POINT('Ctrl Pts',(0.988283968217334,-1.14586823009435,
-6.33011417180102));
#367514=CARTESIAN_POINT('Ctrl Pts',(0.827475233263472,-1.26688320437232,
-6.3412126127321));
#367515=CARTESIAN_POINT('Ctrl Pts',(0.474801747978033,-1.43573244565706,
-6.36287088040659));
#367516=CARTESIAN_POINT('Ctrl Pts',(0.28755328116884,-1.48462055179668,
-6.37323787941471));
#367517=CARTESIAN_POINT('Ctrl Pts',(0.0641026458976871,-1.49897376207815,
-6.38438735340234));
#367518=CARTESIAN_POINT('Ctrl Pts',(0.0320353314952041,-1.5,-6.38595869939481));
#367519=CARTESIAN_POINT('Ctrl Pts',(1.6968042574778E-13,-1.5,-6.3875));
#367520=CARTESIAN_POINT('Origin',(0.,2.16840434497101E-16,-9.7));
#367521=CARTESIAN_POINT('',(-2.14167123658283E-14,-1.5,-6.95));
#367522=CARTESIAN_POINT('',(9.32415705023364E-14,-1.5,-6.8875));
#367523=CARTESIAN_POINT('',(-1.83697019872103E-16,-1.5,-9.7));
#367524=CARTESIAN_POINT('Ctrl Pts',(-4.29864477347053E-14,-1.5,-6.95));
#367525=CARTESIAN_POINT('Ctrl Pts',(0.11291155950509,-1.5,-6.94456754006042));
#367526=CARTESIAN_POINT('Ctrl Pts',(0.225691172814987,-1.48725419527285,
-6.93878737825382));
#367527=CARTESIAN_POINT('Ctrl Pts',(0.526145953213928,-1.41815114243535,
-6.92241221164644));
#367528=CARTESIAN_POINT('Ctrl Pts',(0.705744487927115,-1.33787078720479,
-6.9115412632487));
#367529=CARTESIAN_POINT('Ctrl Pts',(1.02735711636434,-1.11087871951942,
-6.88976233323497));
#367530=CARTESIAN_POINT('Ctrl Pts',(1.16539401547416,-0.965088350881621,
-6.87907129736788));
#367531=CARTESIAN_POINT('Ctrl Pts',(1.37189888429361,-0.63560614470349,
-6.85998354372944));
#367532=CARTESIAN_POINT('Ctrl Pts',(1.44132318505672,-0.456863402306125,
-6.85038130012812));
#367533=CARTESIAN_POINT('Ctrl Pts',(1.51099830419892,-0.0759104136947216,
-6.82921724520526));
#367534=CARTESIAN_POINT('Ctrl Pts',(1.50788348376108,0.1231545316006,-6.81815808157774));
#367535=CARTESIAN_POINT('Ctrl Pts',(1.42483099268254,0.508656990753634,
-6.79674127829146));
#367536=CARTESIAN_POINT('Ctrl Pts',(1.34572453403093,0.691290828855329,
-6.78721034547439));
#367537=CARTESIAN_POINT('Ctrl Pts',(1.1242677063703,1.01140212949755,-6.76766351831235));
#367538=CARTESIAN_POINT('Ctrl Pts',(0.985632258322067,1.14691832046349,
-6.75722907857026));
#367539=CARTESIAN_POINT('Ctrl Pts',(0.658525520100797,1.3624247149364,-6.73550485955441));
#367540=CARTESIAN_POINT('Ctrl Pts',(0.471536868009192,1.43788821446901,
-6.72441215551569));
#367541=CARTESIAN_POINT('Ctrl Pts',(0.0868895231586778,1.50969127631196,
-6.70391127201234));
#367542=CARTESIAN_POINT('Ctrl Pts',(-0.106442488420188,1.50843893766231,
-6.69511319859553));
#367543=CARTESIAN_POINT('Ctrl Pts',(-0.489874426699714,1.43170848958283,
-6.67453391950496));
#367544=CARTESIAN_POINT('Ctrl Pts',(-0.675645000454847,1.35397879398435,
-6.66343687014768));
#367545=CARTESIAN_POINT('Ctrl Pts',(-0.999641720894044,1.13468977939164,
-6.64175720915104));
#367546=CARTESIAN_POINT('Ctrl Pts',(-1.136445113522,0.997655916834551,-6.63136875667225));
#367547=CARTESIAN_POINT('Ctrl Pts',(-1.35436332559314,0.674441434527717,
-6.61190598174145));
#367548=CARTESIAN_POINT('Ctrl Pts',(-1.43144886866969,0.490048524005243,
-6.60222491800029));
#367549=CARTESIAN_POINT('Ctrl Pts',(-1.50936527731721,0.102921352358107,
-6.58071785290878));
#367550=CARTESIAN_POINT('Ctrl Pts',(-1.50982762747414,-0.0958993071838165,
-6.56967226071201));
#367551=CARTESIAN_POINT('Ctrl Pts',(-1.4352502306905,-0.475558716944506,
-6.54858007128086));
#367552=CARTESIAN_POINT('Ctrl Pts',(-1.36355215107595,-0.653296429370576,
-6.53912347708507));
#367553=CARTESIAN_POINT('Ctrl Pts',(-1.15285655631797,-0.980033616011744,
-6.5199103475936));
#367554=CARTESIAN_POINT('Ctrl Pts',(-1.01294046321328,-1.12404277400895,
-6.50917837703663));
#367555=CARTESIAN_POINT('Ctrl Pts',(-0.688610762681138,-1.34673460120227,
-6.48738817295556));
#367556=CARTESIAN_POINT('Ctrl Pts',(-0.508237694368947,-1.42463435001778,
-6.47654608774863));
#367557=CARTESIAN_POINT('Ctrl Pts',(-0.213285115742221,-1.4886213369331,
-6.46057775888974));
#367558=CARTESIAN_POINT('Ctrl Pts',(-0.106683253673148,-1.5,-6.45513280043552));
#367559=CARTESIAN_POINT('Ctrl Pts',(8.01442245901285E-15,-1.5,-6.45));
#367560=CARTESIAN_POINT('Ctrl Pts',(1.6968042574778E-13,-1.5,-6.3875));
#367561=CARTESIAN_POINT('Ctrl Pts',(-0.165755393035949,-1.5,-6.39547491006574));
#367562=CARTESIAN_POINT('Ctrl Pts',(-0.330581797108966,-1.47253101276845,
-6.40416815155229));
#367563=CARTESIAN_POINT('Ctrl Pts',(-0.673877430137846,-1.3544808574772,
-6.42396414137767));
#367564=CARTESIAN_POINT('Ctrl Pts',(-0.845578985174142,-1.25448224127724,
-6.43500287563493));
#367565=CARTESIAN_POINT('Ctrl Pts',(-1.13544569244925,-0.998424297400548,
-6.45606181475437));
#367566=CARTESIAN_POINT('Ctrl Pts',(-1.25260337840686,-0.846786137732792,
-6.46545632568153));
#367567=CARTESIAN_POINT('Ctrl Pts',(-1.42815583912755,-0.499917375911177,
-6.4847268124494));
#367568=CARTESIAN_POINT('Ctrl Pts',(-1.48176718453481,-0.306413707829004,
-6.49547701623174));
#367569=CARTESIAN_POINT('Ctrl Pts',(-1.51011914362045,0.0858811320265719,
-6.51727117400149));
#367570=CARTESIAN_POINT('Ctrl Pts',(-1.48627148300686,0.28078934314199,
-6.52809940795235));
#367571=CARTESIAN_POINT('Ctrl Pts',(-1.3664724106079,0.647576246047647,
-6.54847645811377));
#367572=CARTESIAN_POINT('Ctrl Pts',(-1.27284707380272,0.81637051742483,
-6.55727040875927));
#367573=CARTESIAN_POINT('Ctrl Pts',(-1.02168025717648,1.11630068461384,
-6.57768607139152));
#367574=CARTESIAN_POINT('Ctrl Pts',(-0.864004598244528,1.24235271466741,
-6.5887736903482));
#367575=CARTESIAN_POINT('Ctrl Pts',(-0.515324127038387,1.42176250249477,
-6.6105331925583));
#367576=CARTESIAN_POINT('Ctrl Pts',(-0.329006976753908,1.47605584177366,
-6.62100552894422));
#367577=CARTESIAN_POINT('Ctrl Pts',(0.0581570840512136,1.51169543180713,
-6.64062295711679));
#367578=CARTESIAN_POINT('Ctrl Pts',(0.255447828508453,1.49109567670693,
-6.65003758169315));
#367579=CARTESIAN_POINT('Ctrl Pts',(0.631781586702912,1.37470695816143,
-6.67137696803598));
#367580=CARTESIAN_POINT('Ctrl Pts',(0.80701146867335,1.27972548506312,-6.68244609391585));
#367581=CARTESIAN_POINT('Ctrl Pts',(1.10509610966416,1.0319613805034,-6.70367003413006));
#367582=CARTESIAN_POINT('Ctrl Pts',(1.22687666158932,0.883693556645477,
-6.71340591351972));
#367583=CARTESIAN_POINT('Ctrl Pts',(1.41270876705042,0.54202201144847,-6.73238766603066));
#367584=CARTESIAN_POINT('Ctrl Pts',(1.4720223737034,0.350226621709424,-6.74304296546061));
#367585=CARTESIAN_POINT('Ctrl Pts',(1.5120598119248,-0.0415728267988367,
-6.76480960148885));
#367586=CARTESIAN_POINT('Ctrl Pts',(1.4938465836399,-0.237662363874076,
-6.77570346465969));
#367587=CARTESIAN_POINT('Ctrl Pts',(1.38461556434909,-0.607604161078553,
-6.79625578672661));
#367588=CARTESIAN_POINT('Ctrl Pts',(1.29628956641475,-0.778442162188688,
-6.80508896588438));
#367589=CARTESIAN_POINT('Ctrl Pts',(1.05426285246871,-1.08569323481702,
-6.82526823360582));
#367590=CARTESIAN_POINT('Ctrl Pts',(0.899880040821621,-1.21671675064297,
-6.83633552220066));
#367591=CARTESIAN_POINT('Ctrl Pts',(0.555510646549586,-1.40662016700689,
-6.85817909730662));
#367592=CARTESIAN_POINT('Ctrl Pts',(0.370281643719095,-1.46631538374509,
-6.8687491323254));
#367593=CARTESIAN_POINT('Ctrl Pts',(0.119354979579826,-1.49644258950569,
-6.88165871390939));
#367594=CARTESIAN_POINT('Ctrl Pts',(0.0596467206442825,-1.5,-6.88463024581499));
#367595=CARTESIAN_POINT('Ctrl Pts',(1.86666838024545E-13,-1.5,-6.8875));
#367596=CARTESIAN_POINT('Origin',(0.,2.16840434497101E-16,-9.7));
#367597=CARTESIAN_POINT('',(-1.0210217068046E-13,-1.5,-7.45000000000001));
#367598=CARTESIAN_POINT('',(-1.83697019872103E-16,-1.5,-7.38750000000001));
#367599=CARTESIAN_POINT('',(-1.83697019872103E-16,-1.5,-9.7));
#367600=CARTESIAN_POINT('Ctrl Pts',(-2.049402314519E-13,-1.5,-7.45000000000001));
#367601=CARTESIAN_POINT('Ctrl Pts',(0.140437042333261,-1.50000000000002,
-7.44324321965039));
#367602=CARTESIAN_POINT('Ctrl Pts',(0.280400822634887,-1.48028297751634,
-7.4359615140619));
#367603=CARTESIAN_POINT('Ctrl Pts',(0.604088942930021,-1.38689428063388,
-7.41779393164412));
#367604=CARTESIAN_POINT('Ctrl Pts',(0.779904782302742,-1.29620355229113,
-7.40681580122991));
#367605=CARTESIAN_POINT('Ctrl Pts',(1.08899436646274,-1.05054410181683,
-7.38512084805408));
#367606=CARTESIAN_POINT('Ctrl Pts',(1.21848215277776,-0.897109286002776,
-7.37483940477793));
#367607=CARTESIAN_POINT('Ctrl Pts',(1.406321603195,-0.555634949767438,-7.35586860832041));
#367608=CARTESIAN_POINT('Ctrl Pts',(1.46555412110688,-0.37228798043576,
-7.34568266557976));
#367609=CARTESIAN_POINT('Ctrl Pts',(1.51299221578371,0.0140742457643191,
-7.32421809745754));
#367610=CARTESIAN_POINT('Ctrl Pts',(1.49787704346723,0.213809752656271,
-7.31312168040798));
#367611=CARTESIAN_POINT('Ctrl Pts',(1.39197323008777,0.591661603187691,
-7.29212991093402));
#367612=CARTESIAN_POINT('Ctrl Pts',(1.3038657083438,0.766538828644638,-7.28310618956815));
#367613=CARTESIAN_POINT('Ctrl Pts',(1.06643296464032,1.07239698873722,-7.26318664135795));
#367614=CARTESIAN_POINT('Ctrl Pts',(0.919626058030341,1.20066098112188,
-7.25256050209308));
#367615=CARTESIAN_POINT('Ctrl Pts',(0.578836958715456,1.39831341033431,
-7.23067393365165));
#367616=CARTESIAN_POINT('Ctrl Pts',(0.386613340744211,1.46317483680862,
-7.21962386422901));
#367617=CARTESIAN_POINT('Ctrl Pts',(-0.00151335003668148,1.51202423354,
-7.19959318242519));
#367618=CARTESIAN_POINT('Ctrl Pts',(-0.193117885335683,1.49964389128048,
-7.1906987195008));
#367619=CARTESIAN_POINT('Ctrl Pts',(-0.566482987975544,1.40260223596492,
-7.17003958108799));
#367620=CARTESIAN_POINT('Ctrl Pts',(-0.74420899135005,1.31694443138796,
-7.15910935130334));
#367621=CARTESIAN_POINT('Ctrl Pts',(-1.05944183060186,1.08031540776268,
-7.13736967581935));
#367622=CARTESIAN_POINT('Ctrl Pts',(-1.1931273993454,0.930576214328794,
-7.12677830385444));
#367623=CARTESIAN_POINT('Ctrl Pts',(-1.39007108458186,0.594926025763823,
-7.10797923003154));
#367624=CARTESIAN_POINT('Ctrl Pts',(-1.45431316870517,0.413836933241608,
-7.09799094073564));
#367625=CARTESIAN_POINT('Ctrl Pts',(-1.5126848900854,0.0299823118952904,
-7.07666568399418));
#367626=CARTESIAN_POINT('Ctrl Pts',(-1.503457366199,-0.169512684862048,
-7.06558262861877));
#367627=CARTESIAN_POINT('Ctrl Pts',(-1.40869127483083,-0.551178404032966,
-7.04437897755372));
#367628=CARTESIAN_POINT('Ctrl Pts',(-1.32497563560172,-0.729820644777665,
-7.03514179096876));
#367629=CARTESIAN_POINT('Ctrl Pts',(-1.09537787108247,-1.04271897136768,
-7.01540364318983));
#367630=CARTESIAN_POINT('Ctrl Pts',(-0.952555765747528,-1.17462138761499,
-7.00486815543617));
#367631=CARTESIAN_POINT('Ctrl Pts',(-0.618398965905427,-1.38118758222441,
-6.98305307905755));
#367632=CARTESIAN_POINT('Ctrl Pts',(-0.428686397280591,-1.4513234117932,
-6.97197731135584));
#367633=CARTESIAN_POINT('Ctrl Pts',(-0.154267259301207,-1.49405477840375,
-6.95758733201806));
#367634=CARTESIAN_POINT('Ctrl Pts',(-0.0771108902263344,-1.5,-6.9537099994358));
#367635=CARTESIAN_POINT('Ctrl Pts',(-4.26497277117844E-14,-1.5,-6.95));
#367636=CARTESIAN_POINT('Ctrl Pts',(1.87055232414579E-13,-1.5,-6.8875));
#367637=CARTESIAN_POINT('Ctrl Pts',(-0.134476935078994,-1.5,-6.89397002455563));
#367638=CARTESIAN_POINT('Ctrl Pts',(-0.268592394842974,-1.48192102679756,
-6.90092485132217));
#367639=CARTESIAN_POINT('Ctrl Pts',(-0.589636184084624,-1.39338934895648,
-6.91883029110723));
#367640=CARTESIAN_POINT('Ctrl Pts',(-0.768209078573734,-1.30347783016702,
-6.92991942568776));
#367641=CARTESIAN_POINT('Ctrl Pts',(-1.07427176036584,-1.06407770958817,
-6.95129487668064));
#367642=CARTESIAN_POINT('Ctrl Pts',(-1.20066717458189,-0.919099539462454,
-6.96140325027485));
#367643=CARTESIAN_POINT('Ctrl Pts',(-1.39645751585126,-0.582568918544948,
-6.9801712902645));
#367644=CARTESIAN_POINT('Ctrl Pts',(-1.46130323893525,-0.392598325701134,
-6.99068898190552));
#367645=CARTESIAN_POINT('Ctrl Pts',(-1.51270095576477,-0.0014949167896889,
-7.01241694906727));
#367646=CARTESIAN_POINT('Ctrl Pts',(-1.50000567634135,0.195588578785192,
-7.02336603215476));
#367647=CARTESIAN_POINT('Ctrl Pts',(-1.40105852305377,0.568516146700469,
-7.04408423037227));
#367648=CARTESIAN_POINT('Ctrl Pts',(-1.31777927839766,0.741366900979518,
-7.05302517326762));
#367649=CARTESIAN_POINT('Ctrl Pts',(-1.08586476580297,1.05378535214069,
-7.07286145576728));
#367650=CARTESIAN_POINT('Ctrl Pts',(-0.936725907773699,1.18831479822963,
-7.08377383147779));
#367651=CARTESIAN_POINT('Ctrl Pts',(-0.599428604164675,1.38855525628651,
-7.10556429051011));
#367652=CARTESIAN_POINT('Ctrl Pts',(-0.415583281557217,1.45420272592114,
-7.11623309354135));
#367653=CARTESIAN_POINT('Ctrl Pts',(-0.0331046029529278,1.51205403693844,
-7.13624208840723));
#367654=CARTESIAN_POINT('Ctrl Pts',(0.161885171787989,1.50372875951478,
-7.14518512730597));
#367655=CARTESIAN_POINT('Ctrl Pts',(0.543135763622651,1.41225702056906,
-7.16606893659539));
#367656=CARTESIAN_POINT('Ctrl Pts',(0.725185762635119,1.32799244163293,
-7.17716850400493));
#367657=CARTESIAN_POINT('Ctrl Pts',(1.0398249511182,1.09786677591472,-7.19869896862224));
#367658=CARTESIAN_POINT('Ctrl Pts',(1.17116611133969,0.956524919258439,
-7.2089442858246));
#367659=CARTESIAN_POINT('Ctrl Pts',(1.3785991781178,0.624228926299006,-7.22815485815207));
#367660=CARTESIAN_POINT('Ctrl Pts',(1.44962349447218,0.434544642446531,
-7.23835863097522));
#367661=CARTESIAN_POINT('Ctrl Pts',(1.51216510990107,0.0427687254564257,
-7.26012395969689));
#367662=CARTESIAN_POINT('Ctrl Pts',(1.50479638433807,-0.15512427430675,
-7.27111801523929));
#367663=CARTESIAN_POINT('Ctrl Pts',(1.41573257018693,-0.530841294492776,
-7.2919911830274));
#367664=CARTESIAN_POINT('Ctrl Pts',(1.33721003007483,-0.705652812938672,
-7.30109825279054));
#367665=CARTESIAN_POINT('Ctrl Pts',(1.11397734882578,-1.02401785086592,
-7.32068201345055));
#367666=CARTESIAN_POINT('Ctrl Pts',(0.968550256288191,-1.16251792797778,
-7.33152610206678));
#367667=CARTESIAN_POINT('Ctrl Pts',(0.636394820737358,-1.372077846342,-7.35332804675424));
#367668=CARTESIAN_POINT('Ctrl Pts',(0.453877912632891,-1.44277632123166,
-7.36407324211443));
#367669=CARTESIAN_POINT('Ctrl Pts',(0.175951754616519,-1.49226334300853,
-7.37881961012036));
#367670=CARTESIAN_POINT('Ctrl Pts',(0.0879659976243163,-1.5,-7.38326773396601));
#367671=CARTESIAN_POINT('Ctrl Pts',(-1.83697019872104E-16,-1.5,-7.38750000000001));
#367672=CARTESIAN_POINT('Origin',(0.,2.16840434497101E-16,-9.7));
#367673=CARTESIAN_POINT('',(-2.56633154350194E-14,-1.5,-7.95));
#367674=CARTESIAN_POINT('',(-2.56633154350194E-14,-1.5,-7.88750000000001));
#367675=CARTESIAN_POINT('',(-1.83697019872103E-16,-1.5,-9.7));
#367676=CARTESIAN_POINT('Ctrl Pts',(-5.15212872365112E-14,-1.5,-7.95));
#367677=CARTESIAN_POINT('Ctrl Pts',(0.169649030212483,-1.50000000000001,
-7.94183775722825));
#367678=CARTESIAN_POINT('Ctrl Pts',(0.338229987551259,-1.47122377203185,
-7.93292756247082));
#367679=CARTESIAN_POINT('Ctrl Pts',(0.684455122501634,-1.34921053430319,
-7.91288054129526));
#367680=CARTESIAN_POINT('Ctrl Pts',(0.855627600158956,-1.24769800639786,
-7.90182520918234));
#367681=CARTESIAN_POINT('Ctrl Pts',(1.1491386146339,-0.984097798600795,
-7.88038142591987));
#367682=CARTESIAN_POINT('Ctrl Pts',(1.26850206005723,-0.82453111852428,
-7.87080728436246));
#367683=CARTESIAN_POINT('Ctrl Pts',(1.43632435921431,-0.473136830219077,
-7.85128537945661));
#367684=CARTESIAN_POINT('Ctrl Pts',(1.48503247678298,-0.28556062007432,
-7.84086447889301));
#367685=CARTESIAN_POINT('Ctrl Pts',(1.50955306563698,0.105242630406832,
-7.81915318719962));
#367686=CARTESIAN_POINT('Ctrl Pts',(1.48217797589332,0.304937933588397,
-7.80805900368953));
#367687=CARTESIAN_POINT('Ctrl Pts',(1.35345017162957,0.674487844230075,
-7.78752845309833));
#367688=CARTESIAN_POINT('Ctrl Pts',(1.25626583476381,0.841758623162788,
-7.77872660084614));
#367689=CARTESIAN_POINT('Ctrl Pts',(1.00247653346502,1.13259933499009,-7.75843724873241));
#367690=CARTESIAN_POINT('Ctrl Pts',(0.847530404712385,1.25276548683173,
-7.74764445097471));
#367691=CARTESIAN_POINT('Ctrl Pts',(0.496384048790409,1.42938196077102,
-7.72584390088335));
#367692=CARTESIAN_POINT('Ctrl Pts',(0.302737087598003,1.48253235258537,
-7.71505065734638));
#367693=CARTESIAN_POINT('Ctrl Pts',(-0.0850804230589879,1.50957501010104,
-7.6956405937342));
#367694=CARTESIAN_POINT('Ctrl Pts',(-0.275304145189383,1.48670218358323,
-7.68638503934947));
#367695=CARTESIAN_POINT('Ctrl Pts',(-0.643440979793326,1.36916031540728,
-7.66540799574259));
#367696=CARTESIAN_POINT('Ctrl Pts',(-0.817081372258155,1.27318210552497,
-7.65438765707932));
#367697=CARTESIAN_POINT('Ctrl Pts',(-1.11961569878932,1.01793386183373,
-7.63274173851608));
#367698=CARTESIAN_POINT('Ctrl Pts',(-1.2447834190928,0.860355903267692,
-7.62279755018153));
#367699=CARTESIAN_POINT('Ctrl Pts',(-1.42271198097539,0.512425064932855,
-7.60346805916293));
#367700=CARTESIAN_POINT('Ctrl Pts',(-1.47644279044892,0.32677812751696,
-7.59315434041761));
#367701=CARTESIAN_POINT('Ctrl Pts',(-1.5118668771993,-0.0620866185101912,
-7.5715507434161));
#367702=CARTESIAN_POINT('Ctrl Pts',(-1.49030819952901,-0.261891740745748,
-7.56045045884746));
#367703=CARTESIAN_POINT('Ctrl Pts',(-1.37235403146986,-0.635440182437178,
-7.53969776764238));
#367704=CARTESIAN_POINT('Ctrl Pts',(-1.27947126280045,-0.806282252778367,
-7.53082852725601));
#367705=CARTESIAN_POINT('Ctrl Pts',(-1.03345416187703,-1.10431373891751,
-7.5107133715763));
#367706=CARTESIAN_POINT('Ctrl Pts',(-0.882341954946408,-1.22841180962396,
-7.4999958134998));
#367707=CARTESIAN_POINT('Ctrl Pts',(-0.536802147266234,-1.41470310596347,
-7.47819626351982));
#367708=CARTESIAN_POINT('Ctrl Pts',(-0.344717144208225,-1.47334017307293,
-7.46732576208155));
#367709=CARTESIAN_POINT('Ctrl Pts',(-0.097911947230068,-1.49760595641594,
-7.45477729196818));
#367710=CARTESIAN_POINT('Ctrl Pts',(-0.0489304567307137,-1.49999999999999,
-7.45235416769708));
#367711=CARTESIAN_POINT('Ctrl Pts',(-2.04020644341047E-13,-1.5,-7.45000000000001));
#367712=CARTESIAN_POINT('Ctrl Pts',(-4.33680868994202E-16,-1.5,-7.38750000000001));
#367713=CARTESIAN_POINT('Ctrl Pts',(-0.103498290049447,-1.5,-7.39247956380173));
#367714=CARTESIAN_POINT('Ctrl Pts',(-0.206940275664367,-1.48929046845617,
-7.39775390564245));
#367715=CARTESIAN_POINT('Ctrl Pts',(-0.503643604568591,-1.42689583247804,
-7.41376223554287));
#367716=CARTESIAN_POINT('Ctrl Pts',(-0.688478575587678,-1.34746996432422,
-7.42486138634771));
#367717=CARTESIAN_POINT('Ctrl Pts',(-1.0101028052577,-1.12535794412252,
-7.44650531765147));
#367718=CARTESIAN_POINT('Ctrl Pts',(-1.14551436471142,-0.987196013291791,
-7.45685814075527));
#367719=CARTESIAN_POINT('Ctrl Pts',(-1.36075238870163,-0.661644015737823,
-7.47625689605598));
#367720=CARTESIAN_POINT('Ctrl Pts',(-1.43629940598586,-0.475909511502501,
-7.48606058269434));
#367721=CARTESIAN_POINT('Ctrl Pts',(-1.51030786796259,-0.0875699896681622,
-7.50763500057403));
#367722=CARTESIAN_POINT('Ctrl Pts',(-1.50876393250556,0.111042482143407,
-7.51866902678578));
#367723=CARTESIAN_POINT('Ctrl Pts',(-1.43047794526851,0.489709522131853,
-7.53970608456291));
#367724=CARTESIAN_POINT('Ctrl Pts',(-1.35704827088219,0.666691954518031,
-7.54906153891744));
#367725=CARTESIAN_POINT('Ctrl Pts',(-1.14316482437444,0.991323444194374,
-7.56836955241538));
#367726=CARTESIAN_POINT('Ctrl Pts',(-1.00183132950032,1.13395729188269,
-7.57913151468264));
#367727=CARTESIAN_POINT('Ctrl Pts',(-0.675468170279157,1.3533475707223,
-7.60092784391401));
#367728=CARTESIAN_POINT('Ctrl Pts',(-0.494525159301831,1.42942724371325,
-7.61174679283841));
#367729=CARTESIAN_POINT('Ctrl Pts',(-0.116649211979274,1.50765892423412,
-7.63210046006734));
#367730=CARTESIAN_POINT('Ctrl Pts',(0.076465011572568,1.51022996233389,
-7.64089475896424));
#367731=CARTESIAN_POINT('Ctrl Pts',(0.461551125383072,1.44114414373383,
-7.66134127377004));
#367732=CARTESIAN_POINT('Ctrl Pts',(0.649189784601783,1.36691817947591,
-7.6724308753114));
#367733=CARTESIAN_POINT('Ctrl Pts',(0.977966479177636,1.15348257980608,
-7.69417791806195));
#367734=CARTESIAN_POINT('Ctrl Pts',(1.11758931678336,1.01880014504509,-7.7046367037117));
#367735=CARTESIAN_POINT('Ctrl Pts',(1.34095887333867,0.700374278604906,
-7.72422873946887));
#367736=CARTESIAN_POINT('Ctrl Pts',(1.42115306908879,0.518685318835995,
-7.7336841489536));
#367737=CARTESIAN_POINT('Ctrl Pts',(1.50697056267944,0.134072157882677,
-7.75505154678434));
#367738=CARTESIAN_POINT('Ctrl Pts',(1.51152051034369,-0.0651103607297328,
-7.76611724226281));
#367739=CARTESIAN_POINT('Ctrl Pts',(1.44449799810243,-0.446754527862136,
-7.78731969599238));
#367740=CARTESIAN_POINT('Ctrl Pts',(1.3762971592515,-0.626044261873528,
-7.79700632377052));
#367741=CARTESIAN_POINT('Ctrl Pts',(1.17204880129264,-0.956993882235811,
-7.81602627248468));
#367742=CARTESIAN_POINT('Ctrl Pts',(1.03503100953311,-1.10373068000132,
-7.82669456622451));
#367743=CARTESIAN_POINT('Ctrl Pts',(0.714901685733098,-1.33301916458055,
-7.84846592006877));
#367744=CARTESIAN_POINT('Ctrl Pts',(0.535731969675832,-1.41457552668073,
-7.85935168155458));
#367745=CARTESIAN_POINT('Ctrl Pts',(0.232355588865252,-1.48648730918881,
-7.87594543399592));
#367746=CARTESIAN_POINT('Ctrl Pts',(0.11625927429028,-1.5,-7.88190647305773));
#367747=CARTESIAN_POINT('Ctrl Pts',(-5.09314812546791E-14,-1.5,-7.88750000000001));
#367748=CARTESIAN_POINT('Origin',(0.,2.16840434497101E-16,-9.7));
#367749=CARTESIAN_POINT('',(6.18620758391476E-15,-1.5,-8.45));
#367750=CARTESIAN_POINT('',(-1.06348773749651E-13,-1.5,-8.38750000000002));
#367751=CARTESIAN_POINT('',(-1.83697019872103E-16,-1.5,-9.7));
#367752=CARTESIAN_POINT('Ctrl Pts',(1.25561121877016E-14,-1.5,-8.45));
#367753=CARTESIAN_POINT('Ctrl Pts',(0.00861429778850655,-1.5,-8.44958554440441));
#367754=CARTESIAN_POINT('Ctrl Pts',(0.0172316723228776,-1.49992579396597,
-8.44916887950008));
#367755=CARTESIAN_POINT('Ctrl Pts',(0.216730498483306,-1.49648709693699,
-8.43947496838927));
#367756=CARTESIAN_POINT('Ctrl Pts',(0.405205023619677,-1.45678790405548,
-8.42930422821288));
#367757=CARTESIAN_POINT('Ctrl Pts',(0.763939328292724,-1.30602890974033,
-8.40785686608991));
#367758=CARTESIAN_POINT('Ctrl Pts',(0.929707761400483,-1.19371884349497,
-8.39676160457105));
#367759=CARTESIAN_POINT('Ctrl Pts',(1.20509608623561,-0.914035700736181,
-8.37574300142704));
#367760=CARTESIAN_POINT('Ctrl Pts',(1.31316801726847,-0.750534306911873,
-8.36669635038398));
#367761=CARTESIAN_POINT('Ctrl Pts',(1.46058931529617,-0.392388022013749,
-8.34679933455631));
#367762=CARTESIAN_POINT('Ctrl Pts',(1.49891489916418,-0.201314907576628,
-8.33618416153202));
#367763=CARTESIAN_POINT('Ctrl Pts',(1.50108200612855,0.19249826939769,-8.31430565170012));
#367764=CARTESIAN_POINT('Ctrl Pts',(1.46187352216226,0.391466615992827,
-8.30325185466706));
#367765=CARTESIAN_POINT('Ctrl Pts',(1.31144926331368,0.752556761797094,
-8.28319129101127));
#367766=CARTESIAN_POINT('Ctrl Pts',(1.20547352871805,0.912732494481734,
-8.27431135845658));
#367767=CARTESIAN_POINT('Ctrl Pts',(0.935743303605986,1.18850887613864,
-8.25367350190414));
#367768=CARTESIAN_POINT('Ctrl Pts',(0.77316273312452,1.30014676725224,-8.24275028802884));
#367769=CARTESIAN_POINT('Ctrl Pts',(0.411255019791086,1.45614895662291,
-8.22100460090341));
#367770=CARTESIAN_POINT('Ctrl Pts',(0.214882025841304,1.49778257196538,
-8.21040011151181));
#367771=CARTESIAN_POINT('Ctrl Pts',(-0.174206396355913,1.50195375454829,
-8.19156421988777));
#367772=CARTESIAN_POINT('Ctrl Pts',(-0.363222433697757,1.467764624521,-8.1816290254141));
#367773=CARTESIAN_POINT('Ctrl Pts',(-0.725242470020206,1.32782064009227,
-8.16032399539473));
#367774=CARTESIAN_POINT('Ctrl Pts',(-0.893747788845163,1.22077963681101,
-8.14924341826052));
#367775=CARTESIAN_POINT('Ctrl Pts',(-1.17806984563516,0.948915230794823,
-8.12801217786916));
#367776=CARTESIAN_POINT('Ctrl Pts',(-1.2916501441798,0.787348491302205,
-8.11874158285011));
#367777=CARTESIAN_POINT('Ctrl Pts',(-1.4491496887938,0.432498074699068,
-8.09902767081661));
#367778=CARTESIAN_POINT('Ctrl Pts',(-1.49264245272113,0.243084388697504,
-8.08850468826097));
#367779=CARTESIAN_POINT('Ctrl Pts',(-1.50590393515616,-0.149395073754563,
-8.0667002736803));
#367780=CARTESIAN_POINT('Ctrl Pts',(-1.47255346733907,-0.348807606776928,
-8.0556217996235));
#367781=CARTESIAN_POINT('Ctrl Pts',(-1.33283856573897,-0.714141759724103,
-8.0353254577931));
#367782=CARTESIAN_POINT('Ctrl Pts',(-1.23122919841274,-0.877800908019311,
-8.02652085053871));
#367783=CARTESIAN_POINT('Ctrl Pts',(-0.969415363518022,-1.16111510898422,
-8.00605448761852));
#367784=CARTESIAN_POINT('Ctrl Pts',(-0.810585245633811,-1.27706577719137,
-7.99519191811422));
#367785=CARTESIAN_POINT('Ctrl Pts',(-0.453893095493189,-1.44343242172073,
-7.97340926335772));
#367786=CARTESIAN_POINT('Ctrl Pts',(-0.25879168041917,-1.49082770289231,
-7.96270590656026));
#367787=CARTESIAN_POINT('Ctrl Pts',(-0.0400632634351528,-1.4995990138221,
-7.95193868316567));
#367788=CARTESIAN_POINT('Ctrl Pts',(-0.0200247189458719,-1.5,-7.95096343973948));
#367789=CARTESIAN_POINT('Ctrl Pts',(-5.11429338501666E-14,-1.5,-7.95));
#367790=CARTESIAN_POINT('Ctrl Pts',(-5.11429338501666E-14,-1.5,-7.88750000000001));
#367791=CARTESIAN_POINT('Ctrl Pts',(-0.0736320868157455,-1.5,-7.89104262542868));
#367792=CARTESIAN_POINT('Ctrl Pts',(-0.147314902069754,-1.49457904917319,
-7.89473827349793));
#367793=CARTESIAN_POINT('Ctrl Pts',(-0.418702927434066,-1.45425447866906,
-7.90891556291462));
#367794=CARTESIAN_POINT('Ctrl Pts',(-0.609025848846148,-1.38536633060707,
-7.91998603840886));
#367795=CARTESIAN_POINT('Ctrl Pts',(-0.944782138143701,-1.18090318746338,
-7.94181965216352));
#367796=CARTESIAN_POINT('Ctrl Pts',(-1.08856096172562,-1.04985610672164,
-7.95237741072569));
#367797=CARTESIAN_POINT('Ctrl Pts',(-1.32003136507659,-0.738631619722692,
-7.97215916033823));
#367798=CARTESIAN_POINT('Ctrl Pts',(-1.40480022985449,-0.560896232853786,
-7.98133909817484));
#367799=CARTESIAN_POINT('Ctrl Pts',(-1.50224046510422,-0.180131641157084,
-8.00249268660243));
#367800=CARTESIAN_POINT('Ctrl Pts',(-1.51287518985252,0.0194362765722913,
-8.01357979314295));
#367801=CARTESIAN_POINT('Ctrl Pts',(-1.45710848051361,0.403943219053963,
-8.03494128994749));
#367802=CARTESIAN_POINT('Ctrl Pts',(-1.3940497063946,0.585578769316464,
-8.04502816248795));
#367803=CARTESIAN_POINT('Ctrl Pts',(-1.19928932849217,0.922619535335456,
-8.06376081903927));
#367804=CARTESIAN_POINT('Ctrl Pts',(-1.06660917766218,1.07323780149619,
-8.07432823649911));
#367805=CARTESIAN_POINT('Ctrl Pts',(-0.752867300763901,1.31203272481169,
-8.0960563419037));
#367806=CARTESIAN_POINT('Ctrl Pts',(-0.575589044828377,1.39890746718006,
-8.10699883325719));
#367807=CARTESIAN_POINT('Ctrl Pts',(-0.202819353943747,1.49835135182648,
-8.12769605350109));
#367808=CARTESIAN_POINT('Ctrl Pts',(-0.0113908336243939,1.51197052822358,
-8.1366194435889));
#367809=CARTESIAN_POINT('Ctrl Pts',(0.375011792040734,1.46592391911218,
-8.15648932105949));
#367810=CARTESIAN_POINT('Ctrl Pts',(0.565863175268461,1.40333444856677,
-8.16741025892034));
#367811=CARTESIAN_POINT('Ctrl Pts',(0.907166874920003,1.21013321233666,
-8.1891979418325));
#367812=CARTESIAN_POINT('Ctrl Pts',(1.05543618606226,1.08325598596651,-8.19985591979005));
#367813=CARTESIAN_POINT('Ctrl Pts',(1.29576961923913,0.780029096600294,
-8.21984193663411));
#367814=CARTESIAN_POINT('Ctrl Pts',(1.38549433300877,0.606526026137088,
-8.2288041096591));
#367815=CARTESIAN_POINT('Ctrl Pts',(1.49548781765011,0.230114298782428,
-8.24971587228992));
#367816=CARTESIAN_POINT('Ctrl Pts',(1.51278175429125,0.030332685950176,
-8.2608148507806));
#367817=CARTESIAN_POINT('Ctrl Pts',(1.46939831026169,-0.356917622094825,
-8.2823287567831));
#367818=CARTESIAN_POINT('Ctrl Pts',(1.41201871989969,-0.541061483730698,
-8.29255897131843));
#367819=CARTESIAN_POINT('Ctrl Pts',(1.22663389120196,-0.886385431748862,
-8.31174363509721));
#367820=CARTESIAN_POINT('Ctrl Pts',(1.09709178138546,-1.04246898246255,
-8.32200695212607));
#367821=CARTESIAN_POINT('Ctrl Pts',(0.78788982081973,-1.29138352291927,
-8.34379773118042));
#367822=CARTESIAN_POINT('Ctrl Pts',(0.612524884090505,-1.38320591296693,
-8.35478560257844));
#367823=CARTESIAN_POINT('Ctrl Pts',(0.286398521866563,-1.47942465534937,
-8.37314910734072));
#367824=CARTESIAN_POINT('Ctrl Pts',(0.14346092522985,-1.50000000000002,
-8.3805977330167));
#367825=CARTESIAN_POINT('Ctrl Pts',(-2.12746487093796E-13,-1.5,-8.38750000000002));
#367826=CARTESIAN_POINT('Origin',(0.,2.16840434497101E-16,-9.7));
#367827=CARTESIAN_POINT('',(1.03858078175315E-13,-1.5,-8.94999999999999));
#367828=CARTESIAN_POINT('',(-1.50468077620414E-14,-1.5,-8.88750000000001));
#367829=CARTESIAN_POINT('',(-1.83697019872103E-16,-1.5,-9.7));
#367830=CARTESIAN_POINT('Ctrl Pts',(2.07899853370503E-13,-1.5,-8.94999999999999));
#367831=CARTESIAN_POINT('Ctrl Pts',(0.0372649113391745,-1.5,-8.94820709111724));
#367832=CARTESIAN_POINT('Ctrl Pts',(0.0745695358632018,-1.49861137275991,
-8.9463736985541));
#367833=CARTESIAN_POINT('Ctrl Pts',(0.30329600300598,-1.48151031632727,
-8.93489406192744));
#367834=CARTESIAN_POINT('Ctrl Pts',(0.490209627590489,-1.43057183543788,
-8.9244862181692));
#367835=CARTESIAN_POINT('Ctrl Pts',(0.841405977044156,-1.25770957002068,
-8.90278754633298));
#367836=CARTESIAN_POINT('Ctrl Pts',(1.00104516758194,-1.13477656415575,
-8.89169209647867));
#367837=CARTESIAN_POINT('Ctrl Pts',(1.25783645012521,-0.839435377793257,
-8.87113329829344));
#367838=CARTESIAN_POINT('Ctrl Pts',(1.35476199033148,-0.671881071606827,
-8.86232672620036));
#367839=CARTESIAN_POINT('Ctrl Pts',(1.48102174625321,-0.307065382477598,
-8.84205918791541));
#367840=CARTESIAN_POINT('Ctrl Pts',(1.50829154998946,-0.112958337924697,
-8.83127546321802));
#367841=CARTESIAN_POINT('Ctrl Pts',(1.48708764335021,0.279467001944457,
-8.80947405544752));
#367842=CARTESIAN_POINT('Ctrl Pts',(1.43699109229512,0.473930153689053,
-8.79867054701726));
#367843=CARTESIAN_POINT('Ctrl Pts',(1.26775400370753,0.823927635892113,
-8.77922624245043));
#367844=CARTESIAN_POINT('Ctrl Pts',(1.15338312850122,0.977641779435656,
-8.77000212221447));
#367845=CARTESIAN_POINT('Ctrl Pts',(0.868506079734434,1.23866287308289,
-8.74904538288054));
#367846=CARTESIAN_POINT('Ctrl Pts',(0.699004118880926,1.34163326918927,
-8.73802992720589));
#367847=CARTESIAN_POINT('Ctrl Pts',(0.327026154934649,1.47745730690498,
-8.71636023913459));
#367848=CARTESIAN_POINT('Ctrl Pts',(0.127832000440199,1.50779735873836,
-8.70636691328704));
#367849=CARTESIAN_POINT('Ctrl Pts',(-0.262690489890152,1.48918065627799,
-8.68706076058674));
#367850=CARTESIAN_POINT('Ctrl Pts',(-0.450421298277766,1.44352492164979,
-8.67676034300615));
#367851=CARTESIAN_POINT('Ctrl Pts',(-0.805330745648177,1.28101962154612,
-8.65517071814405));
#367852=CARTESIAN_POINT('Ctrl Pts',(-0.967936513681968,1.16304646733895,
-8.64407031242057));
#367853=CARTESIAN_POINT('Ctrl Pts',(-1.23351437923819,0.875004344501689,
-8.62329152132761));
#367854=CARTESIAN_POINT('Ctrl Pts',(-1.33565592983522,0.709373834332001,
-8.61440965746288));
#367855=CARTESIAN_POINT('Ctrl Pts',(-1.47194853413449,0.347677667547077,
-8.59431542597483));
#367856=CARTESIAN_POINT('Ctrl Pts',(-1.50449152991188,0.154931586657638,
-8.58360731036986));
#367857=CARTESIAN_POINT('Ctrl Pts',(-1.49437825522114,-0.237436947311771,
-8.56180905848267));
#367858=CARTESIAN_POINT('Ctrl Pts',(-1.4497751209325,-0.433260028587922,
-8.55092999841177));
#367859=CARTESIAN_POINT('Ctrl Pts',(-1.29039062376177,-0.788038602079775,
-8.53122007766222));
#367860=CARTESIAN_POINT('Ctrl Pts',(-1.18029367557154,-0.945003126011328,
-8.52220348577584));
#367861=CARTESIAN_POINT('Ctrl Pts',(-0.903110269139051,-1.21357556860263,
-8.50140714728842));
#367862=CARTESIAN_POINT('Ctrl Pts',(-0.737079841084386,-1.321015807329,
-8.49043455351843));
#367863=CARTESIAN_POINT('Ctrl Pts',(-0.378368345440081,-1.46390916922604,
-8.46920677858477));
#367864=CARTESIAN_POINT('Ctrl Pts',(-0.189979927018365,-1.5,-8.45914041350039));
#367865=CARTESIAN_POINT('Ctrl Pts',(1.30798150088651E-14,-1.5,-8.45));
#367866=CARTESIAN_POINT('Ctrl Pts',(-2.12513850479429E-13,-1.5,-8.38750000000002));
#367867=CARTESIAN_POINT('Ctrl Pts',(-0.0458918994678753,-1.49999999999999,
-8.38970797504262));
#367868=CARTESIAN_POINT('Ctrl Pts',(-0.0918317158667109,-1.49789404547631,
-8.39197675422648));
#367869=CARTESIAN_POINT('Ctrl Pts',(-0.335732616452112,-1.47541280668582,
-8.40433592063249));
#367870=CARTESIAN_POINT('Ctrl Pts',(-0.528166235830199,-1.41794905611572,
-8.41519060275519));
#367871=CARTESIAN_POINT('Ctrl Pts',(-0.874931563379712,-1.23371868116764,
-8.43699186777094));
#367872=CARTESIAN_POINT('Ctrl Pts',(-1.02687455944189,-1.1104542542655,
-8.44772624043583));
#367873=CARTESIAN_POINT('Ctrl Pts',(-1.27456475548438,-0.813962270949951,
-8.46787912897466));
#367874=CARTESIAN_POINT('Ctrl Pts',(-1.36837494747328,-0.64389549964342,
-8.47672802779765));
#367875=CARTESIAN_POINT('Ctrl Pts',(-1.48865925982964,-0.271199995133596,
-8.49743333360375));
#367876=CARTESIAN_POINT('Ctrl Pts',(-1.51147180590034,-0.0714047240208655,
-8.50853307088779));
#367877=CARTESIAN_POINT('Ctrl Pts',(-1.47839353742528,0.317903564515033,
-8.53016130913978));
#367878=CARTESIAN_POINT('Ctrl Pts',(-1.42574097855776,0.503978159891549,
-8.5404987866607));
#367879=CARTESIAN_POINT('Ctrl Pts',(-1.2499967564876,0.852664344843762,
-8.55987024138027));
#367880=CARTESIAN_POINT('Ctrl Pts',(-1.12609565658542,1.01067536499336,
-8.56972834648909));
#367881=CARTESIAN_POINT('Ctrl Pts',(-0.825513299539681,1.26775118754061,
-8.59133111695601));
#367882=CARTESIAN_POINT('Ctrl Pts',(-0.652393827643045,1.3649353924963,
-8.6023598926799));
#367883=CARTESIAN_POINT('Ctrl Pts',(-0.284896137119151,1.48489483651446,
-8.62337334033739));
#367884=CARTESIAN_POINT('Ctrl Pts',(-0.0948174301912979,1.50899482999332,
-8.63268823787429));
#367885=CARTESIAN_POINT('Ctrl Pts',(0.293161477204924,1.48445475357866,
-8.65203655054902));
#367886=CARTESIAN_POINT('Ctrl Pts',(0.487140999572001,1.43255739996276,
-8.66281098782634));
#367887=CARTESIAN_POINT('Ctrl Pts',(0.839523777297171,1.25816376717198,
-8.68460927970198));
#367888=CARTESIAN_POINT('Ctrl Pts',(0.995327430827507,1.13890752447603,
-8.69541805988573));
#367889=CARTESIAN_POINT('Ctrl Pts',(1.25087470635368,0.849706080390263,
-8.71574645735887));
#367890=CARTESIAN_POINT('Ctrl Pts',(1.34902893073365,0.68323363120199,-8.7245425760444));
#367891=CARTESIAN_POINT('Ctrl Pts',(1.48017523509372,0.314599449042532,
-8.74502225283104));
#367892=CARTESIAN_POINT('Ctrl Pts',(1.508862114537,0.11495148166446,-8.75611380657427));
#367893=CARTESIAN_POINT('Ctrl Pts',(1.48680827499995,-0.276247092765537,
-8.77784706070926));
#367894=CARTESIAN_POINT('Ctrl Pts',(1.43924029795828,-0.464239223595349,
-8.78829106797759));
#367895=CARTESIAN_POINT('Ctrl Pts',(1.27368875643019,-0.81640079493658,
-8.80785559971877));
#367896=CARTESIAN_POINT('Ctrl Pts',(1.15560994852043,-0.976409685917739,
-8.81735651503753));
#367897=CARTESIAN_POINT('Ctrl Pts',(0.864123079281189,-1.24185056708233,
-8.8387540413827));
#367898=CARTESIAN_POINT('Ctrl Pts',(0.693524972739318,-1.34459027887538,
-8.84981582749377));
#367899=CARTESIAN_POINT('Ctrl Pts',(0.3448599190496,-1.47007278833151,-8.8700766079735));
#367900=CARTESIAN_POINT('Ctrl Pts',(0.173006288184303,-1.5,-8.87917623107878));
#367901=CARTESIAN_POINT('Ctrl Pts',(-3.00454106039183E-14,-1.5,-8.88750000000001));
#367902=CARTESIAN_POINT('Origin',(0.,0.,0.));
#367903=CARTESIAN_POINT('',(1.,-0.577350269189625,0.));
#367904=CARTESIAN_POINT('',(1.,0.577350269189625,0.));
#367905=CARTESIAN_POINT('Ctrl Pts',(1.,0.577350269189567,-2.89100513080514E-14));
#367906=CARTESIAN_POINT('Ctrl Pts',(1.,0.,-0.288675134594789));
#367907=CARTESIAN_POINT('Ctrl Pts',(1.,-0.577350269189567,-2.89669235401328E-14));
#367908=CARTESIAN_POINT('Origin',(0.,0.,0.));
#367909=CARTESIAN_POINT('Origin',(-9.08513196663917E-30,1.30104260698261E-15,
-2.72083333333333));
#367910=CARTESIAN_POINT('',(1.92031473636372E-14,-2.75,-1.275));
#367911=CARTESIAN_POINT('Origin',(0.,0.,-1.275));
#367912=CARTESIAN_POINT('',(1.48387956900833E-14,-1.5,0.));
#367913=CARTESIAN_POINT('Origin',(0.,0.,0.));
#367914=CARTESIAN_POINT('Origin',(0.,-6.07153216591882E-15,-1.275));
#367915=CARTESIAN_POINT('',(3.5,-6.5001585456204E-15,-1.7));
#367916=CARTESIAN_POINT('Origin',(0.,-6.07153216591882E-15,-1.7));
#367917=CARTESIAN_POINT('',(3.5,-6.5001585456204E-15,-1.275));
#367918=CARTESIAN_POINT('',(3.5,-6.5001585456204E-15,-1.275));
#367919=CARTESIAN_POINT('Origin',(0.,-6.07153216591882E-15,-1.275));
#367920=CARTESIAN_POINT('Origin',(0.,2.16840434497101E-16,-9.7));
#367921=CARTESIAN_POINT('',(1.5,1.26953349192158E-14,-9.325));
#367922=CARTESIAN_POINT('Ctrl Pts',(-0.190653686693144,-1.15967294634849,
-9.64975952641927));
#367923=CARTESIAN_POINT('Ctrl Pts',(-0.0285031007229647,-1.21316517876327,
-9.62328078572229));
#367924=CARTESIAN_POINT('Ctrl Pts',(0.132806008053662,-1.22453687890282,
-9.60193243194212));
#367925=CARTESIAN_POINT('Ctrl Pts',(0.434592435142101,-1.20145478370504,
-9.55661911842553));
#367926=CARTESIAN_POINT('Ctrl Pts',(0.585956558405005,-1.16172879077905,
-9.53296252240899));
#367927=CARTESIAN_POINT('Ctrl Pts',(0.869444002206283,-1.02932614938086,
-9.48665581615357));
#367928=CARTESIAN_POINT('Ctrl Pts',(0.998917957166605,-0.936991063680698,
-9.46438835594032));
#367929=CARTESIAN_POINT('Ctrl Pts',(1.23902375947727,-0.688929844127107,
-9.41953944808946));
#367930=CARTESIAN_POINT('Ctrl Pts',(1.32213455554229,-0.544623881037455,
-9.40019228876427));
#367931=CARTESIAN_POINT('Ctrl Pts',(1.43760433325456,-0.296768134705317,
-9.36480861464899));
#367932=CARTESIAN_POINT('Ctrl Pts',(1.48023592847381,-0.150359031185724,
-9.34476407152631));
#367933=CARTESIAN_POINT('Ctrl Pts',(1.50000000000017,1.24646820642837E-12,
-9.32499999999983));
#367934=CARTESIAN_POINT('',(1.05094390383308,-1.0702882373436,-9.325));
#367935=CARTESIAN_POINT('Origin',(0.,2.06676039130049E-16,-9.325));
#367936=CARTESIAN_POINT('',(1.21964286610306E-11,1.30188293868178,-9.52311706131822));
#367937=CARTESIAN_POINT('Ctrl Pts',(1.05094390383308,-1.0702882373436,-9.325));
#367938=CARTESIAN_POINT('Ctrl Pts',(0.968016858591267,-1.14634172204288,
-9.32883501505143));
#367939=CARTESIAN_POINT('Ctrl Pts',(0.876722528496159,-1.21272862092496,
-9.33278379259671));
#367940=CARTESIAN_POINT('Ctrl Pts',(0.682284006851511,-1.32283847967238,
-9.3407082862428));
#367941=CARTESIAN_POINT('Ctrl Pts',(0.579933643683517,-1.36652156451929,
-9.34465804140652));
#367942=CARTESIAN_POINT('Ctrl Pts',(0.280932987527152,-1.4562425328007,
-9.35560555159769));
#367943=CARTESIAN_POINT('Ctrl Pts',(0.0977811463329117,-1.46852820111501,
-9.3614595719435));
#367944=CARTESIAN_POINT('Ctrl Pts',(-0.246256444951042,-1.44391378849632,
-9.37251106997738));
#367945=CARTESIAN_POINT('Ctrl Pts',(-0.430540842049319,-1.39313332243859,
-9.37917748919023));
#367946=CARTESIAN_POINT('Ctrl Pts',(-0.762425243253192,-1.22606064184007,
-9.39275094465158));
#367947=CARTESIAN_POINT('Ctrl Pts',(-0.908108296131221,-1.11378854845243,
-9.39951694367669));
#367948=CARTESIAN_POINT('Ctrl Pts',(-1.13479032378965,-0.857402666085909,
-9.41172780093104));
#367949=CARTESIAN_POINT('Ctrl Pts',(-1.23935650826235,-0.698870792205104,
-9.41759745728602));
#367950=CARTESIAN_POINT('Ctrl Pts',(-1.3666521923041,-0.328284329478432,
-9.43139532516328));
#367951=CARTESIAN_POINT('Ctrl Pts',(-1.39110799634833,-0.145328529779098,
-9.43829819428533));
#367952=CARTESIAN_POINT('Ctrl Pts',(-1.36804302987891,0.208327411726666,
-9.45185416355787));
#367953=CARTESIAN_POINT('Ctrl Pts',(-1.32502441327286,0.376015034876667,
-9.45837881792392));
#367954=CARTESIAN_POINT('Ctrl Pts',(-1.21566879613637,0.610056988684251,
-9.46760725983284));
#367955=CARTESIAN_POINT('Ctrl Pts',(-1.17108914819411,0.686181342639889,
-9.47051827587565));
#367956=CARTESIAN_POINT('Ctrl Pts',(-1.01610091220513,0.89886764355412,
-9.47976483332994));
#367957=CARTESIAN_POINT('Ctrl Pts',(-0.885644382509459,1.01880653830682,
-9.48649835405591));
#367958=CARTESIAN_POINT('Ctrl Pts',(-0.592130096913835,1.19705002479627,
-9.50008644802564));
#367959=CARTESIAN_POINT('Ctrl Pts',(-0.433365879600623,1.25618399199256,
-9.50680144369053));
#367960=CARTESIAN_POINT('Ctrl Pts',(-0.197295674427518,1.2960635134121,
-9.51595358432894));
#367961=CARTESIAN_POINT('Ctrl Pts',(-0.105956107225097,1.30560664395967,
-9.51939335604232));
#367962=CARTESIAN_POINT('Ctrl Pts',(2.43930167567386E-11,1.30188293868178,
-9.52311706131822));
#367963=CARTESIAN_POINT('',(-1.37772764904077E-16,1.125,-9.7));
#367964=CARTESIAN_POINT('',(-1.37772764904077E-16,1.125,-9.7));
#367965=CARTESIAN_POINT('Origin',(0.,2.16840434497101E-16,-9.7));
#367966=CARTESIAN_POINT('Ctrl Pts',(2.43930167567386E-11,1.30188293868178,
-9.52311706131822));
#367967=CARTESIAN_POINT('Ctrl Pts',(0.0761076165708164,1.29920822421006,
-9.52579177578852));
#367968=CARTESIAN_POINT('Ctrl Pts',(0.159739133609348,1.28946730994931,
-9.52888182473693));
#367969=CARTESIAN_POINT('Ctrl Pts',(0.40287502943865,1.23198478745045,-9.53853482060624));
#367970=CARTESIAN_POINT('Ctrl Pts',(0.549010376213962,1.16703886874139,
-9.54503863078224));
#367971=CARTESIAN_POINT('Ctrl Pts',(0.818389915914693,0.981050906469348,
-9.55859771056026));
#367972=CARTESIAN_POINT('Ctrl Pts',(0.93687656106349,0.858483479453949,
-9.56552845851573));
#367973=CARTESIAN_POINT('Ctrl Pts',(1.116008365168,0.579288345692445,-9.57818164518354));
#367974=CARTESIAN_POINT('Ctrl Pts',(1.17614262990486,0.427743363043572,
-9.58411524905681));
#367975=CARTESIAN_POINT('Ctrl Pts',(1.23203342741208,0.114644612869533,
-9.59739583493339));
#367976=CARTESIAN_POINT('Ctrl Pts',(1.22994817565386,-0.0419119689212186,
-9.60414125823576));
#367977=CARTESIAN_POINT('Ctrl Pts',(1.161346903398,-0.374697918051623,-9.61872246149687));
#367978=CARTESIAN_POINT('Ctrl Pts',(1.08803701736073,-0.523098651946534,
-9.62519803010312));
#367979=CARTESIAN_POINT('Ctrl Pts',(0.926562190370942,-0.75996639628023,
-9.63638853623501));
#367980=CARTESIAN_POINT('Ctrl Pts',(0.816715032446504,-0.868035363199342,
-9.64294180913862));
#367981=CARTESIAN_POINT('Ctrl Pts',(0.689217670442766,-0.951929185124573,
-9.64975952641917));
#367982=CARTESIAN_POINT('Origin',(0.,2.16840434497101E-16,-9.7));
#367983=CARTESIAN_POINT('Ctrl Pts',(-2.99099185042107E-14,-1.5,-8.88750000000001));
#367984=CARTESIAN_POINT('Ctrl Pts',(-0.016764684548797,-1.5,-8.88830659126143));
#367985=CARTESIAN_POINT('Ctrl Pts',(-0.0335394535524549,-1.49971894682661,
-8.88912147474409));
#367986=CARTESIAN_POINT('Ctrl Pts',(-0.249045952375023,-1.49248573428552,
-8.89969095857362));
#367987=CARTESIAN_POINT('Ctrl Pts',(-0.444445184321647,-1.44636830249076,
-8.91037314827601));
#367988=CARTESIAN_POINT('Ctrl Pts',(-0.802322896738174,-1.28229148655965,
-8.93214923707415));
#367989=CARTESIAN_POINT('Ctrl Pts',(-0.961996620200093,-1.16728937111781,
-8.94302604588281));
#367990=CARTESIAN_POINT('Ctrl Pts',(-1.22557574019166,-0.885646162997747,
-8.96353092465391));
#367991=CARTESIAN_POINT('Ctrl Pts',(-1.32815830670805,-0.722770501492501,
-8.9723460832505));
#367992=CARTESIAN_POINT('Ctrl Pts',(-1.47027232381364,-0.358375675815785,
-8.99259024023253));
#367993=CARTESIAN_POINT('Ctrl Pts',(-1.50493256730985,-0.159048108768436,
-9.00366399395739));
#367994=CARTESIAN_POINT('Ctrl Pts',(-1.49414680166945,0.23375615123113,
-9.02548645284625));
#367995=CARTESIAN_POINT('Ctrl Pts',(-1.45180469463996,0.423553061262505,
-9.03603072562577));
#367996=CARTESIAN_POINT('Ctrl Pts',(-1.29656150195308,0.779148072440641,
-9.05578600402455));
#367997=CARTESIAN_POINT('Ctrl Pts',(-1.18422609999239,0.941149075529152,
-9.06500025840822));
#367998=CARTESIAN_POINT('Ctrl Pts',(-0.901907738019758,1.21478504099838,
-9.08618430597254));
#367999=CARTESIAN_POINT('Ctrl Pts',(-0.734004107147856,1.32301696951808,
-9.09726901563823));
#368000=CARTESIAN_POINT('Ctrl Pts',(-0.37267916446526,1.46540646275545,
-9.1186085337495));
#368001=CARTESIAN_POINT('Ctrl Pts',(-0.183777280373563,1.5008253247504,
-9.12863508578802));
#368002=CARTESIAN_POINT('Ctrl Pts',(0.205421062548106,1.49910838576655,
-9.14740809254207));
#368003=CARTESIAN_POINT('Ctrl Pts',(0.402044492391625,1.45871762005048,
-9.1579901074355));
#368004=CARTESIAN_POINT('Ctrl Pts',(0.765033707725997,1.30496455179117,
-9.17972535276377));
#368005=CARTESIAN_POINT('Ctrl Pts',(0.92840545307133,1.19426902615948,-9.19066045523852));
#368006=CARTESIAN_POINT('Ctrl Pts',(1.19982948118002,0.920120487096611,
-9.2113345870758));
#368007=CARTESIAN_POINT('Ctrl Pts',(1.30674059259681,0.760680194257607,
-9.22023998920799));
#368008=CARTESIAN_POINT('Ctrl Pts',(1.4594399044428,0.400508372435874,-9.24024953486476));
#368009=CARTESIAN_POINT('Ctrl Pts',(1.49989618200679,0.201656004166217,
-9.25129688865752));
#368010=CARTESIAN_POINT('Ctrl Pts',(1.50009944355299,-0.192401669391178,
-9.27318898163292));
#368011=CARTESIAN_POINT('Ctrl Pts',(1.46288142732614,-0.383810092514896,
-9.28382278291757));
#368012=CARTESIAN_POINT('Ctrl Pts',(1.35231292083348,-0.656914113380578,
-9.29899522852122));
#368013=CARTESIAN_POINT('Ctrl Pts',(1.30483483328299,-0.746784757003529,
-9.30379845917422));
#368014=CARTESIAN_POINT('Ctrl Pts',(1.19118218895726,-0.91751820480455,
-9.3140091703461));
#368015=CARTESIAN_POINT('Ctrl Pts',(1.12492471439177,-0.997644552077798,
-9.31942271644616));
#368016=CARTESIAN_POINT('Ctrl Pts',(1.05094390383308,-1.07028823734361,
-9.325));
#368017=CARTESIAN_POINT('Ctrl Pts',(1.5,2.08513761812412E-14,-9.325));
#368018=CARTESIAN_POINT('Ctrl Pts',(1.5,0.12960195655018,-9.31779989130277));
#368019=CARTESIAN_POINT('Ctrl Pts',(1.48320505460745,0.258655672138285,
-9.31063024043674));
#368020=CARTESIAN_POINT('Ctrl Pts',(1.41793481240152,0.505154131452618,
-9.29693588158595));
#368021=CARTESIAN_POINT('Ctrl Pts',(1.37076777116574,0.621871157175992,
-9.2904516023791));
#368022=CARTESIAN_POINT('Ctrl Pts',(1.21686069124155,0.897465020181764,
-9.27514083221211));
#368023=CARTESIAN_POINT('Ctrl Pts',(1.09331169914294,1.04446688461033,-9.26525568130039));
#368024=CARTESIAN_POINT('Ctrl Pts',(0.792105738691596,1.28903984869781,
-9.24397020932451));
#368025=CARTESIAN_POINT('Ctrl Pts',(0.615567738611666,1.38207633547858,
-9.23289217398046));
#368026=CARTESIAN_POINT('Ctrl Pts',(0.238269039661259,1.49385235718827,
-9.21163449237153));
#368027=CARTESIAN_POINT('Ctrl Pts',(0.0414182077513572,1.51216394019312,
-9.20233062167712));
#368028=CARTESIAN_POINT('Ctrl Pts',(-0.344911503806603,1.4724470676907,
-9.18264007830506));
#368029=CARTESIAN_POINT('Ctrl Pts',(-0.530828562312111,1.41607458027076,
-9.1721292372288));
#368030=CARTESIAN_POINT('Ctrl Pts',(-0.877887868290141,1.23261868646805,
-9.15033534153446));
#368031=CARTESIAN_POINT('Ctrl Pts',(-1.03431538205672,1.10464573789137,
-9.13925441514218));
#368032=CARTESIAN_POINT('Ctrl Pts',(-1.28197696314223,0.80188845513952,
-9.11892886724566));
#368033=CARTESIAN_POINT('Ctrl Pts',(-1.37356108825293,0.63231503049334,
-9.11012861280517));
#368034=CARTESIAN_POINT('Ctrl Pts',(-1.48931778815661,0.264311081277164,
-9.08968394895983));
#368035=CARTESIAN_POINT('Ctrl Pts',(-1.51101519260302,0.0689319743571016,
-9.07882955413094));
#368036=CARTESIAN_POINT('Ctrl Pts',(-1.47819153152631,-0.323214650039326,
-9.05704363055336));
#368037=CARTESIAN_POINT('Ctrl Pts',(-1.42239168475186,-0.516085078045942,
-9.04632860677521));
#368038=CARTESIAN_POINT('Ctrl Pts',(-1.24289975815323,-0.860977276769388,
-9.02716792906835));
#368039=CARTESIAN_POINT('Ctrl Pts',(-1.12398358187228,-1.01132277704982,
-9.01765205260071));
#368040=CARTESIAN_POINT('Ctrl Pts',(-0.830981507794516,-1.2642343798264,
-8.99652966143954));
#368041=CARTESIAN_POINT('Ctrl Pts',(-0.657919660216403,-1.36233668602944,
-8.98547815535453));
#368042=CARTESIAN_POINT('Ctrl Pts',(-0.318701383774487,-1.4744861624803,
-8.96604224518497));
#368043=CARTESIAN_POINT('Ctrl Pts',(-0.159749516444619,-1.5,-8.95768595219353));
#368044=CARTESIAN_POINT('Ctrl Pts',(2.07899853370503E-13,-1.5,-8.94999999999999));
#368045=CARTESIAN_POINT('Origin',(-1.04744440165294E-14,-1.5,-9.7));
#368046=CARTESIAN_POINT('Origin',(1.92031473636372E-14,-2.75,-1.7));
#368047=CARTESIAN_POINT('',(-0.823407874165093,-0.838564036615816,-1.7));
#368048=CARTESIAN_POINT('Ctrl Pts',(-0.823407874165095,-0.838564036615814,
-1.7));
#368049=CARTESIAN_POINT('Ctrl Pts',(-0.906488444224223,-0.774361328520471,
-1.7));
#368050=CARTESIAN_POINT('Ctrl Pts',(-0.980239661944283,-0.698929860052436,
-1.7));
#368051=CARTESIAN_POINT('Ctrl Pts',(-1.08659688413256,-0.554881140374752,
-1.7));
#368052=CARTESIAN_POINT('Ctrl Pts',(-1.14864632923241,-0.460352743585334,
-1.7));
#368053=CARTESIAN_POINT('Ctrl Pts',(-1.26100849448902,-0.179088137671936,
-1.7));
#368054=CARTESIAN_POINT('Ctrl Pts',(-1.29189652800491,-0.0173593023659969,
-1.7));
#368055=CARTESIAN_POINT('Ctrl Pts',(-1.29108984811542,0.29991757832034,
-1.7));
#368056=CARTESIAN_POINT('Ctrl Pts',(-1.26280816915346,0.452628510455921,
-1.7));
#368057=CARTESIAN_POINT('Ctrl Pts',(-1.15403315966975,0.739009298630757,
-1.7));
#368058=CARTESIAN_POINT('Ctrl Pts',(-1.06946215919407,0.88567669595877,
-1.70000000000001));
#368059=CARTESIAN_POINT('Ctrl Pts',(-0.838257759590746,1.15024353406291,
-1.70000000000001));
#368060=CARTESIAN_POINT('Ctrl Pts',(-0.70010011391448,1.25940600481097,
-1.7));
#368061=CARTESIAN_POINT('Ctrl Pts',(-0.464663729175284,1.38344883181634,
-1.7));
#368062=CARTESIAN_POINT('Ctrl Pts',(-0.379811168312268,1.41817558821392,
-1.69999999991096));
#368063=CARTESIAN_POINT('Ctrl Pts',(-0.197010229499014,1.47315843181175,
-1.69999999991096));
#368064=CARTESIAN_POINT('Ctrl Pts',(-0.0990730826998878,1.49174390977524,
-1.7));
#368065=CARTESIAN_POINT('Ctrl Pts',(3.29540263058496E-12,1.50000000000027,
-1.7));
#368066=CARTESIAN_POINT('',(-1.43925448419918E-16,-1.17524047358083,-1.7));
#368067=CARTESIAN_POINT('Origin',(4.23799807892358E-15,4.71844785465692E-15,
-1.7));
#368068=CARTESIAN_POINT('Ctrl Pts',(1.05094390383305,1.07028823734363,-1.7));
#368069=CARTESIAN_POINT('Ctrl Pts',(1.156452495554,0.945434066171969,-1.7));
#368070=CARTESIAN_POINT('Ctrl Pts',(1.2586537518754,0.783905914653593,-1.7));
#368071=CARTESIAN_POINT('Ctrl Pts',(1.37926337433591,0.431629318194347,
-1.7));
#368072=CARTESIAN_POINT('Ctrl Pts',(1.40434668153212,0.262454779629501,
-1.7));
#368073=CARTESIAN_POINT('Ctrl Pts',(1.39184448034083,-0.0842699563767622,
-1.7));
#368074=CARTESIAN_POINT('Ctrl Pts',(1.35148029165158,-0.258561181463102,
-1.69999999999998));
#368075=CARTESIAN_POINT('Ctrl Pts',(1.22264368235685,-0.547784646368696,
-1.69999999999998));
#368076=CARTESIAN_POINT('Ctrl Pts',(1.13071611052457,-0.704303236236527,
-1.69999999996066));
#368077=CARTESIAN_POINT('Ctrl Pts',(0.870776629029807,-0.949213555039079,
-1.69999999996066));
#368078=CARTESIAN_POINT('Ctrl Pts',(0.741388190020053,-1.03251050868711,
-1.7));
#368079=CARTESIAN_POINT('Ctrl Pts',(0.507415161659025,-1.12806794424744,
-1.7));
#368080=CARTESIAN_POINT('Ctrl Pts',(0.410499846437694,-1.15454479340249,
-1.7));
#368081=CARTESIAN_POINT('Ctrl Pts',(0.208295996222876,-1.18420961712132,
-1.7));
#368082=CARTESIAN_POINT('Ctrl Pts',(0.103670375869531,-1.18626698030435,
-1.7));
#368083=CARTESIAN_POINT('Ctrl Pts',(-1.38777878078145E-16,-1.17524047358083,
-1.7));
#368084=CARTESIAN_POINT('Origin',(0.,-6.07153216591882E-15,-1.275));
#368085=CARTESIAN_POINT('Origin',(1.04744440165294E-14,-1.5,0.));
#368086=CARTESIAN_POINT('',(-0.999999999999999,0.577350269189625,0.));
#368087=CARTESIAN_POINT('',(-0.999999999999999,-0.577350269189627,0.));
#368088=CARTESIAN_POINT('Origin',(0.,0.,0.));
#368089=CARTESIAN_POINT('',(3.25260651745651E-16,1.15470053837925,0.));
#368090=CARTESIAN_POINT('Origin',(0.,0.,0.));
#368091=CARTESIAN_POINT('Origin',(0.,0.,0.));
#368092=CARTESIAN_POINT('',(5.42101086242752E-16,-1.15470053837925,0.));
#368093=CARTESIAN_POINT('Origin',(0.,0.,0.));
#368094=CARTESIAN_POINT('Origin',(0.,0.,0.));
#368095=CARTESIAN_POINT('Origin',(0.,0.,0.));
#368096=CARTESIAN_POINT('Ctrl Pts',(0.999999999999951,0.577350269189654,
-2.7791564077117E-14));
#368097=CARTESIAN_POINT('Ctrl Pts',(0.500000000000001,0.866025403784438,
-0.28867513459479));
#368098=CARTESIAN_POINT('Ctrl Pts',(5.09575199449458E-14,1.15470053837922,
-2.90996254149895E-14));
#368099=CARTESIAN_POINT('Origin',(0.,0.,0.));
#368100=CARTESIAN_POINT('Ctrl Pts',(-4.99717345888679E-14,1.15470053837922,
-2.93650291647028E-14));
#368101=CARTESIAN_POINT('Ctrl Pts',(-0.5,0.866025403784438,-0.288675134594791));
#368102=CARTESIAN_POINT('Ctrl Pts',(-0.999999999999949,0.577350269189654,
-2.94219013967842E-14));
#368103=CARTESIAN_POINT('Origin',(0.,0.,0.));
#368104=CARTESIAN_POINT('Ctrl Pts',(-0.999999999999999,0.577350269189567,
-2.99337514855168E-14));
#368105=CARTESIAN_POINT('Ctrl Pts',(-0.999999999999999,-1.33226762955019E-15,
-0.288675134594791));
#368106=CARTESIAN_POINT('Ctrl Pts',(-0.999999999999999,-0.57735026918957,
-2.85119456834816E-14));
#368107=CARTESIAN_POINT('Origin',(0.,0.,0.));
#368108=CARTESIAN_POINT('Ctrl Pts',(-0.999999999999948,-0.577350269189654,
-2.99906237175983E-14));
#368109=CARTESIAN_POINT('Ctrl Pts',(-0.499999999999999,-0.866025403784438,
-0.288675134594791));
#368110=CARTESIAN_POINT('Ctrl Pts',(-4.92134381611157E-14,-1.15470053837922,
-2.91564976470709E-14));
#368111=CARTESIAN_POINT('Origin',(0.,0.,0.));
#368112=CARTESIAN_POINT('Ctrl Pts',(5.0350882802744E-14,-1.15470053837922,
-2.93650291647027E-14));
#368113=CARTESIAN_POINT('Ctrl Pts',(0.5,-0.866025403784437,-0.288675134594791));
#368114=CARTESIAN_POINT('Ctrl Pts',(0.99999999999995,-0.577350269189653,
-2.91944124684585E-14));
#368115=CARTESIAN_POINT('Origin',(1.,-0.577350269189624,-1.19));
#368116=CARTESIAN_POINT('',(1.9352544089507E-16,-1.15470053837925,-1.19));
#368117=CARTESIAN_POINT('',(1.,-0.577350269189624,-1.19));
#368118=CARTESIAN_POINT('',(1.9352544089507E-16,-1.15470053837925,-1.19));
#368119=CARTESIAN_POINT('',(1.,0.577350269189626,-1.19));
#368120=CARTESIAN_POINT('',(1.,-0.577350269189624,-1.19));
#368121=CARTESIAN_POINT('',(3.85779730129493E-16,1.15470053837925,-1.19));
#368122=CARTESIAN_POINT('',(1.,0.577350269189626,-1.19));
#368123=CARTESIAN_POINT('',(-0.999999999999999,0.577350269189625,-1.19));
#368124=CARTESIAN_POINT('',(3.85779730129493E-16,1.15470053837925,-1.19));
#368125=CARTESIAN_POINT('',(-0.999999999999999,-0.577350269189625,-1.19));
#368126=CARTESIAN_POINT('',(-0.999999999999999,0.577350269189625,-1.19));
#368127=CARTESIAN_POINT('',(-0.999999999999999,-0.577350269189625,-1.19));
#368128=CARTESIAN_POINT('Origin',(1.,-0.577350269189624,-1.19));
#368129=CARTESIAN_POINT('',(1.,-0.577350269189624,-1.19));
#368130=CARTESIAN_POINT('',(1.,0.577350269189626,-1.19));
#368131=CARTESIAN_POINT('Origin',(1.,0.577350269189626,-1.19));
#368132=CARTESIAN_POINT('',(3.85779730129493E-16,1.15470053837925,-1.19));
#368133=CARTESIAN_POINT('Origin',(3.85779730129493E-16,1.15470053837925,
-1.19));
#368134=CARTESIAN_POINT('',(-0.999999999999999,0.577350269189625,-1.19));
#368135=CARTESIAN_POINT('Origin',(-0.999999999999999,0.577350269189625,
-1.19));
#368136=CARTESIAN_POINT('',(-0.999999999999999,-0.577350269189625,-1.19));
#368137=CARTESIAN_POINT('Origin',(-0.999999999999999,-0.577350269189625,
-1.19));
#368138=CARTESIAN_POINT('',(1.9352544089507E-16,-1.15470053837925,-1.19));
#368139=CARTESIAN_POINT('Origin',(1.9352544089507E-16,-1.15470053837925,
-1.19));
#368140=CARTESIAN_POINT('Ctrl Pts',(0.,1.17524047358083,-9.95));
#368141=CARTESIAN_POINT('Ctrl Pts',(-0.678525403784435,1.17524047358083,
-9.90833333333333));
#368142=CARTESIAN_POINT('Ctrl Pts',(-1.01778810567665,0.58762023679042,
-9.86666666666667));
#368143=CARTESIAN_POINT('Ctrl Pts',(-1.35705080756887,5.0380876514183E-15,
-9.825));
#368144=CARTESIAN_POINT('Ctrl Pts',(-1.01778810567665,-0.58762023679041,
-9.78333333333333));
#368145=CARTESIAN_POINT('Ctrl Pts',(-0.678525403784435,-1.17524047358082,
-9.74166666666667));
#368146=CARTESIAN_POINT('Ctrl Pts',(-1.43925448419918E-16,-1.17524047358082,
-9.7));
#368147=CARTESIAN_POINT('Ctrl Pts',(0.678525403784435,-1.17524047358082,
-9.65833333333333));
#368148=CARTESIAN_POINT('Ctrl Pts',(1.01778810567665,-0.58762023679041,
-9.61666666666667));
#368149=CARTESIAN_POINT('Ctrl Pts',(1.35705080756887,4.59643214611782E-15,
-9.575));
#368150=CARTESIAN_POINT('Ctrl Pts',(1.01778810567665,0.587620236790419,
-9.53333333333333));
#368151=CARTESIAN_POINT('Ctrl Pts',(0.678525403784436,1.17524047358083,
-9.49166666666667));
#368152=CARTESIAN_POINT('Ctrl Pts',(0.,1.17524047358083,-9.45));
#368153=CARTESIAN_POINT('Ctrl Pts',(-0.678525403784435,1.17524047358083,
-9.40833333333333));
#368154=CARTESIAN_POINT('Ctrl Pts',(-1.01778810567665,0.58762023679042,
-9.36666666666667));
#368155=CARTESIAN_POINT('Ctrl Pts',(-1.35705080756887,4.81953981192516E-15,
-9.325));
#368156=CARTESIAN_POINT('Ctrl Pts',(-1.01778810567665,-0.58762023679041,
-9.28333333333333));
#368157=CARTESIAN_POINT('Ctrl Pts',(-0.678525403784435,-1.17524047358082,
-9.24166666666667));
#368158=CARTESIAN_POINT('Ctrl Pts',(-1.43925448419918E-16,-1.17524047358082,
-9.2));
#368159=CARTESIAN_POINT('Ctrl Pts',(0.678525403784435,-1.17524047358083,
-9.15833333333333));
#368160=CARTESIAN_POINT('Ctrl Pts',(1.01778810567665,-0.587620236790411,
-9.11666666666667));
#368161=CARTESIAN_POINT('Ctrl Pts',(1.35705080756887,4.37788430662468E-15,
-9.075));
#368162=CARTESIAN_POINT('Ctrl Pts',(1.01778810567665,0.587620236790418,
-9.03333333333333));
#368163=CARTESIAN_POINT('Ctrl Pts',(0.678525403784436,1.17524047358083,
-8.99166666666667));
#368164=CARTESIAN_POINT('Ctrl Pts',(0.,1.17524047358083,-8.95));
#368165=CARTESIAN_POINT('Ctrl Pts',(-0.678525403784435,1.17524047358083,
-8.90833333333333));
#368166=CARTESIAN_POINT('Ctrl Pts',(-1.01778810567665,0.587620236790419,
-8.86666666666667));
#368167=CARTESIAN_POINT('Ctrl Pts',(-1.35705080756887,4.60099197243202E-15,
-8.825));
#368168=CARTESIAN_POINT('Ctrl Pts',(-1.01778810567665,-0.58762023679041,
-8.78333333333333));
#368169=CARTESIAN_POINT('Ctrl Pts',(-0.678525403784435,-1.17524047358082,
-8.74166666666667));
#368170=CARTESIAN_POINT('Ctrl Pts',(-1.43925448419918E-16,-1.17524047358082,
-8.7));
#368171=CARTESIAN_POINT('Ctrl Pts',(0.678525403784435,-1.17524047358083,
-8.65833333333333));
#368172=CARTESIAN_POINT('Ctrl Pts',(1.01778810567665,-0.587620236790411,
-8.61666666666667));
#368173=CARTESIAN_POINT('Ctrl Pts',(1.35705080756887,4.15933646713154E-15,
-8.575));
#368174=CARTESIAN_POINT('Ctrl Pts',(1.01778810567665,0.587620236790418,
-8.53333333333333));
#368175=CARTESIAN_POINT('Ctrl Pts',(0.678525403784436,1.17524047358083,
-8.49166666666667));
#368176=CARTESIAN_POINT('Ctrl Pts',(0.,1.17524047358083,-8.45));
#368177=CARTESIAN_POINT('Ctrl Pts',(-0.678525403784435,1.17524047358083,
-8.40833333333333));
#368178=CARTESIAN_POINT('Ctrl Pts',(-1.01778810567665,0.587620236790419,
-8.36666666666667));
#368179=CARTESIAN_POINT('Ctrl Pts',(-1.35705080756887,4.38244413293887E-15,
-8.325));
#368180=CARTESIAN_POINT('Ctrl Pts',(-1.01778810567665,-0.58762023679041,
-8.28333333333333));
#368181=CARTESIAN_POINT('Ctrl Pts',(-0.678525403784435,-1.17524047358082,
-8.24166666666667));
#368182=CARTESIAN_POINT('Ctrl Pts',(-1.43925448419918E-16,-1.17524047358083,
-8.2));
#368183=CARTESIAN_POINT('Ctrl Pts',(0.678525403784435,-1.17524047358083,
-8.15833333333333));
#368184=CARTESIAN_POINT('Ctrl Pts',(1.01778810567665,-0.587620236790411,
-8.11666666666667));
#368185=CARTESIAN_POINT('Ctrl Pts',(1.35705080756887,3.94078862763839E-15,
-8.075));
#368186=CARTESIAN_POINT('Ctrl Pts',(1.01778810567665,0.587620236790418,
-8.03333333333333));
#368187=CARTESIAN_POINT('Ctrl Pts',(0.678525403784436,1.17524047358083,
-7.99166666666667));
#368188=CARTESIAN_POINT('Ctrl Pts',(0.,1.17524047358083,-7.95));
#368189=CARTESIAN_POINT('Ctrl Pts',(-0.678525403784435,1.17524047358083,
-7.90833333333333));
#368190=CARTESIAN_POINT('Ctrl Pts',(-1.01778810567665,0.587620236790419,
-7.86666666666667));
#368191=CARTESIAN_POINT('Ctrl Pts',(-1.35705080756887,4.16389629344573E-15,
-7.825));
#368192=CARTESIAN_POINT('Ctrl Pts',(-1.01778810567665,-0.58762023679041,
-7.78333333333333));
#368193=CARTESIAN_POINT('Ctrl Pts',(-0.678525403784435,-1.17524047358083,
-7.74166666666667));
#368194=CARTESIAN_POINT('Ctrl Pts',(-1.43925448419918E-16,-1.17524047358083,
-7.7));
#368195=CARTESIAN_POINT('Ctrl Pts',(0.678525403784435,-1.17524047358083,
-7.65833333333333));
#368196=CARTESIAN_POINT('Ctrl Pts',(1.01778810567665,-0.587620236790411,
-7.61666666666667));
#368197=CARTESIAN_POINT('Ctrl Pts',(1.35705080756887,3.72224078814525E-15,
-7.575));
#368198=CARTESIAN_POINT('Ctrl Pts',(1.01778810567665,0.587620236790418,
-7.53333333333333));
#368199=CARTESIAN_POINT('Ctrl Pts',(0.678525403784436,1.17524047358083,
-7.49166666666667));
#368200=CARTESIAN_POINT('Ctrl Pts',(0.,1.17524047358083,-7.45));
#368201=CARTESIAN_POINT('Ctrl Pts',(-0.678525403784435,1.17524047358083,
-7.40833333333333));
#368202=CARTESIAN_POINT('Ctrl Pts',(-1.01778810567665,0.587620236790419,
-7.36666666666667));
#368203=CARTESIAN_POINT('Ctrl Pts',(-1.35705080756887,3.94534845395259E-15,
-7.325));
#368204=CARTESIAN_POINT('Ctrl Pts',(-1.01778810567665,-0.587620236790411,
-7.28333333333333));
#368205=CARTESIAN_POINT('Ctrl Pts',(-0.678525403784435,-1.17524047358083,
-7.24166666666667));
#368206=CARTESIAN_POINT('Ctrl Pts',(-1.43925448419918E-16,-1.17524047358083,
-7.2));
#368207=CARTESIAN_POINT('Ctrl Pts',(0.678525403784435,-1.17524047358083,
-7.15833333333333));
#368208=CARTESIAN_POINT('Ctrl Pts',(1.01778810567665,-0.587620236790411,
-7.11666666666667));
#368209=CARTESIAN_POINT('Ctrl Pts',(1.35705080756887,3.50369294865211E-15,
-7.075));
#368210=CARTESIAN_POINT('Ctrl Pts',(1.01778810567665,0.587620236790417,
-7.03333333333333));
#368211=CARTESIAN_POINT('Ctrl Pts',(0.678525403784436,1.17524047358083,
-6.99166666666667));
#368212=CARTESIAN_POINT('Ctrl Pts',(0.,1.17524047358083,-6.95));
#368213=CARTESIAN_POINT('Ctrl Pts',(-0.678525403784435,1.17524047358083,
-6.90833333333333));
#368214=CARTESIAN_POINT('Ctrl Pts',(-1.01778810567665,0.587620236790418,
-6.86666666666667));
#368215=CARTESIAN_POINT('Ctrl Pts',(-1.35705080756887,3.72680061445945E-15,
-6.825));
#368216=CARTESIAN_POINT('Ctrl Pts',(-1.01778810567665,-0.587620236790411,
-6.78333333333333));
#368217=CARTESIAN_POINT('Ctrl Pts',(-0.678525403784435,-1.17524047358083,
-6.74166666666667));
#368218=CARTESIAN_POINT('Ctrl Pts',(-1.43925448419918E-16,-1.17524047358083,
-6.7));
#368219=CARTESIAN_POINT('Ctrl Pts',(0.678525403784435,-1.17524047358083,
-6.65833333333333));
#368220=CARTESIAN_POINT('Ctrl Pts',(1.01778810567665,-0.587620236790412,
-6.61666666666667));
#368221=CARTESIAN_POINT('Ctrl Pts',(1.35705080756887,3.28514510915897E-15,
-6.575));
#368222=CARTESIAN_POINT('Ctrl Pts',(1.01778810567665,0.587620236790417,
-6.53333333333333));
#368223=CARTESIAN_POINT('Ctrl Pts',(0.678525403784436,1.17524047358083,
-6.49166666666667));
#368224=CARTESIAN_POINT('Ctrl Pts',(0.,1.17524047358083,-6.45));
#368225=CARTESIAN_POINT('Ctrl Pts',(-0.678525403784435,1.17524047358083,
-6.40833333333334));
#368226=CARTESIAN_POINT('Ctrl Pts',(-1.01778810567665,0.587620236790418,
-6.36666666666667));
#368227=CARTESIAN_POINT('Ctrl Pts',(-1.35705080756887,3.50825277496631E-15,
-6.325));
#368228=CARTESIAN_POINT('Ctrl Pts',(-1.01778810567665,-0.587620236790411,
-6.28333333333333));
#368229=CARTESIAN_POINT('Ctrl Pts',(-0.678525403784435,-1.17524047358083,
-6.24166666666667));
#368230=CARTESIAN_POINT('Ctrl Pts',(-1.43925448419918E-16,-1.17524047358083,
-6.2));
#368231=CARTESIAN_POINT('Ctrl Pts',(0.678525403784435,-1.17524047358083,
-6.15833333333333));
#368232=CARTESIAN_POINT('Ctrl Pts',(1.01778810567665,-0.587620236790412,
-6.11666666666667));
#368233=CARTESIAN_POINT('Ctrl Pts',(1.35705080756887,3.06659726966583E-15,
-6.075));
#368234=CARTESIAN_POINT('Ctrl Pts',(1.01778810567665,0.587620236790417,
-6.03333333333333));
#368235=CARTESIAN_POINT('Ctrl Pts',(0.678525403784436,1.17524047358083,
-5.99166666666667));
#368236=CARTESIAN_POINT('Ctrl Pts',(0.,1.17524047358083,-5.95));
#368237=CARTESIAN_POINT('Ctrl Pts',(-0.678525403784435,1.17524047358083,
-5.90833333333333));
#368238=CARTESIAN_POINT('Ctrl Pts',(-1.01778810567665,0.587620236790418,
-5.86666666666667));
#368239=CARTESIAN_POINT('Ctrl Pts',(-1.35705080756887,3.28970493547317E-15,
-5.825));
#368240=CARTESIAN_POINT('Ctrl Pts',(-1.01778810567665,-0.587620236790411,
-5.78333333333333));
#368241=CARTESIAN_POINT('Ctrl Pts',(-0.678525403784435,-1.17524047358083,
-5.74166666666667));
#368242=CARTESIAN_POINT('Ctrl Pts',(-1.43925448419918E-16,-1.17524047358083,
-5.7));
#368243=CARTESIAN_POINT('Ctrl Pts',(0.678525403784435,-1.17524047358083,
-5.65833333333333));
#368244=CARTESIAN_POINT('Ctrl Pts',(1.01778810567665,-0.587620236790412,
-5.61666666666667));
#368245=CARTESIAN_POINT('Ctrl Pts',(1.35705080756887,2.84804943017269E-15,
-5.575));
#368246=CARTESIAN_POINT('Ctrl Pts',(1.01778810567665,0.587620236790417,
-5.53333333333333));
#368247=CARTESIAN_POINT('Ctrl Pts',(0.678525403784436,1.17524047358083,
-5.49166666666667));
#368248=CARTESIAN_POINT('Ctrl Pts',(0.,1.17524047358083,-5.45));
#368249=CARTESIAN_POINT('Ctrl Pts',(-0.678525403784435,1.17524047358083,
-5.40833333333333));
#368250=CARTESIAN_POINT('Ctrl Pts',(-1.01778810567665,0.587620236790418,
-5.36666666666667));
#368251=CARTESIAN_POINT('Ctrl Pts',(-1.35705080756887,3.07115709598003E-15,
-5.325));
#368252=CARTESIAN_POINT('Ctrl Pts',(-1.01778810567665,-0.587620236790411,
-5.28333333333333));
#368253=CARTESIAN_POINT('Ctrl Pts',(-0.678525403784435,-1.17524047358083,
-5.24166666666667));
#368254=CARTESIAN_POINT('Ctrl Pts',(-1.43925448419918E-16,-1.17524047358083,
-5.2));
#368255=CARTESIAN_POINT('Ctrl Pts',(0.678525403784435,-1.17524047358083,
-5.15833333333333));
#368256=CARTESIAN_POINT('Ctrl Pts',(1.01778810567665,-0.587620236790412,
-5.11666666666667));
#368257=CARTESIAN_POINT('Ctrl Pts',(1.35705080756887,2.62950159067955E-15,
-5.075));
#368258=CARTESIAN_POINT('Ctrl Pts',(1.01778810567665,0.587620236790417,
-5.03333333333333));
#368259=CARTESIAN_POINT('Ctrl Pts',(0.678525403784436,1.17524047358083,
-4.99166666666667));
#368260=CARTESIAN_POINT('Ctrl Pts',(0.,1.17524047358083,-4.95));
#368261=CARTESIAN_POINT('Ctrl Pts',(-0.678525403784435,1.17524047358083,
-4.90833333333333));
#368262=CARTESIAN_POINT('Ctrl Pts',(-1.01778810567665,0.587620236790418,
-4.86666666666667));
#368263=CARTESIAN_POINT('Ctrl Pts',(-1.35705080756887,2.85260925648689E-15,
-4.825));
#368264=CARTESIAN_POINT('Ctrl Pts',(-1.01778810567665,-0.587620236790412,
-4.78333333333333));
#368265=CARTESIAN_POINT('Ctrl Pts',(-0.678525403784435,-1.17524047358083,
-4.74166666666667));
#368266=CARTESIAN_POINT('Ctrl Pts',(-1.43925448419918E-16,-1.17524047358083,
-4.7));
#368267=CARTESIAN_POINT('Ctrl Pts',(0.678525403784435,-1.17524047358083,
-4.65833333333333));
#368268=CARTESIAN_POINT('Ctrl Pts',(1.01778810567665,-0.587620236790413,
-4.61666666666667));
#368269=CARTESIAN_POINT('Ctrl Pts',(1.35705080756887,2.41095375118641E-15,
-4.575));
#368270=CARTESIAN_POINT('Ctrl Pts',(1.01778810567665,0.587620236790416,
-4.53333333333333));
#368271=CARTESIAN_POINT('Ctrl Pts',(0.678525403784436,1.17524047358083,
-4.49166666666667));
#368272=CARTESIAN_POINT('Ctrl Pts',(0.,1.17524047358083,-4.45));
#368273=CARTESIAN_POINT('Ctrl Pts',(-0.678525403784435,1.17524047358083,
-4.40833333333333));
#368274=CARTESIAN_POINT('Ctrl Pts',(-1.01778810567665,0.587620236790417,
-4.36666666666667));
#368275=CARTESIAN_POINT('Ctrl Pts',(-1.35705080756887,2.63406141699374E-15,
-4.325));
#368276=CARTESIAN_POINT('Ctrl Pts',(-1.01778810567665,-0.587620236790412,
-4.28333333333333));
#368277=CARTESIAN_POINT('Ctrl Pts',(-0.678525403784435,-1.17524047358083,
-4.24166666666667));
#368278=CARTESIAN_POINT('Ctrl Pts',(-1.43925448419918E-16,-1.17524047358083,
-4.2));
#368279=CARTESIAN_POINT('Ctrl Pts',(0.678525403784435,-1.17524047358083,
-4.15833333333333));
#368280=CARTESIAN_POINT('Ctrl Pts',(1.01778810567665,-0.587620236790413,
-4.11666666666667));
#368281=CARTESIAN_POINT('Ctrl Pts',(1.35705080756887,2.19240591169327E-15,
-4.075));
#368282=CARTESIAN_POINT('Ctrl Pts',(1.01778810567665,0.587620236790416,
-4.03333333333333));
#368283=CARTESIAN_POINT('Ctrl Pts',(0.678525403784436,1.17524047358083,
-3.99166666666667));
#368284=CARTESIAN_POINT('Ctrl Pts',(0.,1.17524047358083,-3.95));
#368285=CARTESIAN_POINT('Ctrl Pts',(-0.678525403784435,1.17524047358083,
-3.90833333333333));
#368286=CARTESIAN_POINT('Ctrl Pts',(-1.01778810567665,0.587620236790417,
-3.86666666666667));
#368287=CARTESIAN_POINT('Ctrl Pts',(-1.35705080756887,2.4155135775006E-15,
-3.825));
#368288=CARTESIAN_POINT('Ctrl Pts',(-1.01778810567665,-0.587620236790412,
-3.78333333333333));
#368289=CARTESIAN_POINT('Ctrl Pts',(-0.678525403784435,-1.17524047358083,
-3.74166666666667));
#368290=CARTESIAN_POINT('Ctrl Pts',(-1.43925448419918E-16,-1.17524047358083,
-3.7));
#368291=CARTESIAN_POINT('Ctrl Pts',(0.678525403784435,-1.17524047358083,
-3.65833333333333));
#368292=CARTESIAN_POINT('Ctrl Pts',(1.01778810567665,-0.587620236790413,
-3.61666666666667));
#368293=CARTESIAN_POINT('Ctrl Pts',(1.35705080756887,1.97385807220012E-15,
-3.575));
#368294=CARTESIAN_POINT('Ctrl Pts',(1.01778810567665,0.587620236790416,
-3.53333333333333));
#368295=CARTESIAN_POINT('Ctrl Pts',(0.678525403784436,1.17524047358083,
-3.49166666666667));
#368296=CARTESIAN_POINT('Ctrl Pts',(0.,1.17524047358083,-3.45));
#368297=CARTESIAN_POINT('Ctrl Pts',(-0.678525403784435,1.17524047358083,
-3.40833333333333));
#368298=CARTESIAN_POINT('Ctrl Pts',(-1.01778810567665,0.587620236790417,
-3.36666666666667));
#368299=CARTESIAN_POINT('Ctrl Pts',(-1.35705080756887,2.19696573800746E-15,
-3.325));
#368300=CARTESIAN_POINT('Ctrl Pts',(-1.01778810567665,-0.587620236790412,
-3.28333333333333));
#368301=CARTESIAN_POINT('Ctrl Pts',(-0.678525403784435,-1.17524047358083,
-3.24166666666667));
#368302=CARTESIAN_POINT('Ctrl Pts',(-1.43925448419918E-16,-1.17524047358083,
-3.2));
#368303=CARTESIAN_POINT('Ctrl Pts',(0.678525403784435,-1.17524047358083,
-3.15833333333333));
#368304=CARTESIAN_POINT('Ctrl Pts',(1.01778810567665,-0.587620236790413,
-3.11666666666667));
#368305=CARTESIAN_POINT('Ctrl Pts',(1.35705080756887,1.75531023270698E-15,
-3.075));
#368306=CARTESIAN_POINT('Ctrl Pts',(1.01778810567665,0.587620236790416,
-3.03333333333333));
#368307=CARTESIAN_POINT('Ctrl Pts',(0.678525403784436,1.17524047358083,
-2.99166666666667));
#368308=CARTESIAN_POINT('Ctrl Pts',(0.,1.17524047358083,-2.95));
#368309=CARTESIAN_POINT('Ctrl Pts',(-0.678525403784435,1.17524047358083,
-2.90833333333333));
#368310=CARTESIAN_POINT('Ctrl Pts',(-1.01778810567665,0.587620236790417,
-2.86666666666667));
#368311=CARTESIAN_POINT('Ctrl Pts',(-1.35705080756887,1.97841789851432E-15,
-2.825));
#368312=CARTESIAN_POINT('Ctrl Pts',(-1.01778810567665,-0.587620236790413,
-2.78333333333333));
#368313=CARTESIAN_POINT('Ctrl Pts',(-0.678525403784435,-1.17524047358083,
-2.74166666666667));
#368314=CARTESIAN_POINT('Ctrl Pts',(-1.43925448419918E-16,-1.17524047358083,
-2.7));
#368315=CARTESIAN_POINT('Ctrl Pts',(0.678525403784435,-1.17524047358083,
-2.65833333333333));
#368316=CARTESIAN_POINT('Ctrl Pts',(1.01778810567665,-0.587620236790414,
-2.61666666666667));
#368317=CARTESIAN_POINT('Ctrl Pts',(1.35705080756887,1.53676239321384E-15,
-2.575));
#368318=CARTESIAN_POINT('Ctrl Pts',(1.01778810567665,0.587620236790415,
-2.53333333333333));
#368319=CARTESIAN_POINT('Ctrl Pts',(0.678525403784436,1.17524047358083,
-2.49166666666667));
#368320=CARTESIAN_POINT('Ctrl Pts',(0.,1.17524047358083,-2.45));
#368321=CARTESIAN_POINT('Ctrl Pts',(-0.678525403784435,1.17524047358083,
-2.40833333333333));
#368322=CARTESIAN_POINT('Ctrl Pts',(-1.01778810567665,0.587620236790416,
-2.36666666666667));
#368323=CARTESIAN_POINT('Ctrl Pts',(-1.35705080756887,1.75987005902118E-15,
-2.325));
#368324=CARTESIAN_POINT('Ctrl Pts',(-1.01778810567665,-0.587620236790413,
-2.28333333333333));
#368325=CARTESIAN_POINT('Ctrl Pts',(-0.678525403784435,-1.17524047358083,
-2.24166666666667));
#368326=CARTESIAN_POINT('Ctrl Pts',(-1.43925448419918E-16,-1.17524047358083,
-2.2));
#368327=CARTESIAN_POINT('Ctrl Pts',(0.678525403784435,-1.17524047358083,
-2.15833333333333));
#368328=CARTESIAN_POINT('Ctrl Pts',(1.01778810567665,-0.587620236790414,
-2.11666666666667));
#368329=CARTESIAN_POINT('Ctrl Pts',(1.35705080756887,1.3182145537207E-15,
-2.075));
#368330=CARTESIAN_POINT('Ctrl Pts',(1.01778810567665,0.587620236790415,
-2.03333333333333));
#368331=CARTESIAN_POINT('Ctrl Pts',(0.678525403784436,1.17524047358083,
-1.99166666666667));
#368332=CARTESIAN_POINT('Ctrl Pts',(0.,1.17524047358083,-1.95));
#368333=CARTESIAN_POINT('Ctrl Pts',(-0.678525403784435,1.17524047358083,
-1.90833333333333));
#368334=CARTESIAN_POINT('Ctrl Pts',(-1.01778810567665,0.587620236790416,
-1.86666666666667));
#368335=CARTESIAN_POINT('Ctrl Pts',(-1.35705080756887,1.54132221952804E-15,
-1.825));
#368336=CARTESIAN_POINT('Ctrl Pts',(-1.01778810567665,-0.587620236790413,
-1.78333333333333));
#368337=CARTESIAN_POINT('Ctrl Pts',(-0.678525403784435,-1.17524047358083,
-1.74166666666667));
#368338=CARTESIAN_POINT('Ctrl Pts',(-1.43925448419918E-16,-1.17524047358083,
-1.7));
#368339=CARTESIAN_POINT('Ctrl Pts',(0.678525403784435,-1.17524047358083,
-1.65833333333333));
#368340=CARTESIAN_POINT('Ctrl Pts',(1.01778810567665,-0.587620236790414,
-1.61666666666667));
#368341=CARTESIAN_POINT('Ctrl Pts',(1.35705080756887,1.09966671422756E-15,
-1.575));
#368342=CARTESIAN_POINT('Ctrl Pts',(1.01778810567665,0.587620236790415,
-1.53333333333333));
#368343=CARTESIAN_POINT('Ctrl Pts',(0.678525403784436,1.17524047358083,
-1.49166666666667));
#368344=CARTESIAN_POINT('Ctrl Pts',(0.,1.17524047358083,-1.45));
#368345=CARTESIAN_POINT('Ctrl Pts',(0.,1.5,-10.1375));
#368346=CARTESIAN_POINT('Ctrl Pts',(-0.866025403784437,1.5,-10.0958333333333));
#368347=CARTESIAN_POINT('Ctrl Pts',(-1.29903810567666,0.750000000000004,
-10.0541666666667));
#368348=CARTESIAN_POINT('Ctrl Pts',(-1.73205080756887,5.14300521871224E-15,
-10.0125));
#368349=CARTESIAN_POINT('Ctrl Pts',(-1.29903810567666,-0.749999999999993,
-9.97083333333333));
#368350=CARTESIAN_POINT('Ctrl Pts',(-0.866025403784437,-1.49999999999999,
-9.92916666666667));
#368351=CARTESIAN_POINT('Ctrl Pts',(-1.83697019872103E-16,-1.49999999999999,
-9.8875));
#368352=CARTESIAN_POINT('Ctrl Pts',(0.866025403784436,-1.49999999999999,
-9.84583333333333));
#368353=CARTESIAN_POINT('Ctrl Pts',(1.29903810567665,-0.749999999999994,
-9.80416666666667));
#368354=CARTESIAN_POINT('Ctrl Pts',(1.73205080756887,4.60950120347571E-15,
-9.7625));
#368355=CARTESIAN_POINT('Ctrl Pts',(1.29903810567666,0.750000000000002,
-9.72083333333333));
#368356=CARTESIAN_POINT('Ctrl Pts',(0.866025403784437,1.5,-9.67916666666667));
#368357=CARTESIAN_POINT('Ctrl Pts',(0.,1.5,-9.6375));
#368358=CARTESIAN_POINT('Ctrl Pts',(-0.866025403784437,1.5,-9.59583333333333));
#368359=CARTESIAN_POINT('Ctrl Pts',(-1.29903810567666,0.750000000000003,
-9.55416666666667));
#368360=CARTESIAN_POINT('Ctrl Pts',(-1.73205080756887,4.9244573792191E-15,
-9.5125));
#368361=CARTESIAN_POINT('Ctrl Pts',(-1.29903810567666,-0.749999999999993,
-9.47083333333333));
#368362=CARTESIAN_POINT('Ctrl Pts',(-0.866025403784437,-1.49999999999999,
-9.42916666666667));
#368363=CARTESIAN_POINT('Ctrl Pts',(-1.83697019872103E-16,-1.49999999999999,
-9.3875));
#368364=CARTESIAN_POINT('Ctrl Pts',(0.866025403784436,-1.49999999999999,
-9.34583333333333));
#368365=CARTESIAN_POINT('Ctrl Pts',(1.29903810567665,-0.749999999999994,
-9.30416666666667));
#368366=CARTESIAN_POINT('Ctrl Pts',(1.73205080756887,4.39095336398257E-15,
-9.2625));
#368367=CARTESIAN_POINT('Ctrl Pts',(1.29903810567666,0.750000000000002,
-9.22083333333333));
#368368=CARTESIAN_POINT('Ctrl Pts',(0.866025403784437,1.5,-9.17916666666667));
#368369=CARTESIAN_POINT('Ctrl Pts',(0.,1.5,-9.1375));
#368370=CARTESIAN_POINT('Ctrl Pts',(-0.866025403784437,1.5,-9.09583333333333));
#368371=CARTESIAN_POINT('Ctrl Pts',(-1.29903810567666,0.750000000000003,
-9.05416666666667));
#368372=CARTESIAN_POINT('Ctrl Pts',(-1.73205080756887,4.70590953972596E-15,
-9.0125));
#368373=CARTESIAN_POINT('Ctrl Pts',(-1.29903810567666,-0.749999999999993,
-8.97083333333333));
#368374=CARTESIAN_POINT('Ctrl Pts',(-0.866025403784437,-1.49999999999999,
-8.92916666666667));
#368375=CARTESIAN_POINT('Ctrl Pts',(-1.83697019872103E-16,-1.49999999999999,
-8.8875));
#368376=CARTESIAN_POINT('Ctrl Pts',(0.866025403784436,-1.49999999999999,
-8.84583333333333));
#368377=CARTESIAN_POINT('Ctrl Pts',(1.29903810567665,-0.749999999999994,
-8.80416666666667));
#368378=CARTESIAN_POINT('Ctrl Pts',(1.73205080756887,4.17240552448942E-15,
-8.7625));
#368379=CARTESIAN_POINT('Ctrl Pts',(1.29903810567666,0.750000000000002,
-8.72083333333333));
#368380=CARTESIAN_POINT('Ctrl Pts',(0.866025403784437,1.5,-8.67916666666667));
#368381=CARTESIAN_POINT('Ctrl Pts',(0.,1.5,-8.6375));
#368382=CARTESIAN_POINT('Ctrl Pts',(-0.866025403784437,1.5,-8.59583333333333));
#368383=CARTESIAN_POINT('Ctrl Pts',(-1.29903810567666,0.750000000000003,
-8.55416666666667));
#368384=CARTESIAN_POINT('Ctrl Pts',(-1.73205080756887,4.48736170023282E-15,
-8.5125));
#368385=CARTESIAN_POINT('Ctrl Pts',(-1.29903810567666,-0.749999999999994,
-8.47083333333333));
#368386=CARTESIAN_POINT('Ctrl Pts',(-0.866025403784437,-1.49999999999999,
-8.42916666666667));
#368387=CARTESIAN_POINT('Ctrl Pts',(-1.83697019872103E-16,-1.49999999999999,
-8.3875));
#368388=CARTESIAN_POINT('Ctrl Pts',(0.866025403784436,-1.49999999999999,
-8.34583333333333));
#368389=CARTESIAN_POINT('Ctrl Pts',(1.29903810567665,-0.749999999999995,
-8.30416666666667));
#368390=CARTESIAN_POINT('Ctrl Pts',(1.73205080756887,3.95385768499628E-15,
-8.2625));
#368391=CARTESIAN_POINT('Ctrl Pts',(1.29903810567666,0.750000000000002,
-8.22083333333333));
#368392=CARTESIAN_POINT('Ctrl Pts',(0.866025403784437,1.5,-8.17916666666667));
#368393=CARTESIAN_POINT('Ctrl Pts',(0.,1.5,-8.1375));
#368394=CARTESIAN_POINT('Ctrl Pts',(-0.866025403784437,1.5,-8.09583333333333));
#368395=CARTESIAN_POINT('Ctrl Pts',(-1.29903810567666,0.750000000000003,
-8.05416666666667));
#368396=CARTESIAN_POINT('Ctrl Pts',(-1.73205080756887,4.26881386073967E-15,
-8.0125));
#368397=CARTESIAN_POINT('Ctrl Pts',(-1.29903810567666,-0.749999999999994,
-7.97083333333333));
#368398=CARTESIAN_POINT('Ctrl Pts',(-0.866025403784437,-1.49999999999999,
-7.92916666666667));
#368399=CARTESIAN_POINT('Ctrl Pts',(-1.83697019872103E-16,-1.49999999999999,
-7.8875));
#368400=CARTESIAN_POINT('Ctrl Pts',(0.866025403784436,-1.49999999999999,
-7.84583333333333));
#368401=CARTESIAN_POINT('Ctrl Pts',(1.29903810567665,-0.749999999999995,
-7.80416666666667));
#368402=CARTESIAN_POINT('Ctrl Pts',(1.73205080756887,3.73530984550314E-15,
-7.7625));
#368403=CARTESIAN_POINT('Ctrl Pts',(1.29903810567666,0.750000000000001,
-7.72083333333333));
#368404=CARTESIAN_POINT('Ctrl Pts',(0.866025403784437,1.5,-7.67916666666667));
#368405=CARTESIAN_POINT('Ctrl Pts',(0.,1.5,-7.6375));
#368406=CARTESIAN_POINT('Ctrl Pts',(-0.866025403784437,1.5,-7.59583333333333));
#368407=CARTESIAN_POINT('Ctrl Pts',(-1.29903810567666,0.750000000000003,
-7.55416666666667));
#368408=CARTESIAN_POINT('Ctrl Pts',(-1.73205080756887,4.05026602124653E-15,
-7.5125));
#368409=CARTESIAN_POINT('Ctrl Pts',(-1.29903810567666,-0.749999999999994,
-7.47083333333333));
#368410=CARTESIAN_POINT('Ctrl Pts',(-0.866025403784437,-1.49999999999999,
-7.42916666666667));
#368411=CARTESIAN_POINT('Ctrl Pts',(-1.83697019872103E-16,-1.49999999999999,
-7.3875));
#368412=CARTESIAN_POINT('Ctrl Pts',(0.866025403784436,-1.49999999999999,
-7.34583333333334));
#368413=CARTESIAN_POINT('Ctrl Pts',(1.29903810567665,-0.749999999999995,
-7.30416666666667));
#368414=CARTESIAN_POINT('Ctrl Pts',(1.73205080756887,3.51676200601E-15,
-7.2625));
#368415=CARTESIAN_POINT('Ctrl Pts',(1.29903810567666,0.750000000000001,
-7.22083333333333));
#368416=CARTESIAN_POINT('Ctrl Pts',(0.866025403784437,1.5,-7.17916666666667));
#368417=CARTESIAN_POINT('Ctrl Pts',(0.,1.5,-7.1375));
#368418=CARTESIAN_POINT('Ctrl Pts',(-0.866025403784437,1.5,-7.09583333333333));
#368419=CARTESIAN_POINT('Ctrl Pts',(-1.29903810567666,0.750000000000002,
-7.05416666666667));
#368420=CARTESIAN_POINT('Ctrl Pts',(-1.73205080756887,3.83171818175339E-15,
-7.0125));
#368421=CARTESIAN_POINT('Ctrl Pts',(-1.29903810567666,-0.749999999999994,
-6.97083333333333));
#368422=CARTESIAN_POINT('Ctrl Pts',(-0.866025403784437,-1.49999999999999,
-6.92916666666667));
#368423=CARTESIAN_POINT('Ctrl Pts',(-1.83697019872103E-16,-1.49999999999999,
-6.8875));
#368424=CARTESIAN_POINT('Ctrl Pts',(0.866025403784436,-1.49999999999999,
-6.84583333333333));
#368425=CARTESIAN_POINT('Ctrl Pts',(1.29903810567665,-0.749999999999995,
-6.80416666666667));
#368426=CARTESIAN_POINT('Ctrl Pts',(1.73205080756887,3.29821416651686E-15,
-6.7625));
#368427=CARTESIAN_POINT('Ctrl Pts',(1.29903810567666,0.750000000000001,
-6.72083333333333));
#368428=CARTESIAN_POINT('Ctrl Pts',(0.866025403784437,1.5,-6.67916666666667));
#368429=CARTESIAN_POINT('Ctrl Pts',(0.,1.5,-6.6375));
#368430=CARTESIAN_POINT('Ctrl Pts',(-0.866025403784437,1.5,-6.59583333333333));
#368431=CARTESIAN_POINT('Ctrl Pts',(-1.29903810567666,0.750000000000002,
-6.55416666666667));
#368432=CARTESIAN_POINT('Ctrl Pts',(-1.73205080756887,3.61317034226025E-15,
-6.5125));
#368433=CARTESIAN_POINT('Ctrl Pts',(-1.29903810567666,-0.749999999999994,
-6.47083333333333));
#368434=CARTESIAN_POINT('Ctrl Pts',(-0.866025403784437,-1.49999999999999,
-6.42916666666667));
#368435=CARTESIAN_POINT('Ctrl Pts',(-1.83697019872103E-16,-1.49999999999999,
-6.3875));
#368436=CARTESIAN_POINT('Ctrl Pts',(0.866025403784436,-1.49999999999999,
-6.34583333333333));
#368437=CARTESIAN_POINT('Ctrl Pts',(1.29903810567665,-0.749999999999996,
-6.30416666666667));
#368438=CARTESIAN_POINT('Ctrl Pts',(1.73205080756887,3.07966632702372E-15,
-6.2625));
#368439=CARTESIAN_POINT('Ctrl Pts',(1.29903810567666,0.750000000000001,
-6.22083333333333));
#368440=CARTESIAN_POINT('Ctrl Pts',(0.866025403784437,1.5,-6.17916666666667));
#368441=CARTESIAN_POINT('Ctrl Pts',(0.,1.5,-6.1375));
#368442=CARTESIAN_POINT('Ctrl Pts',(-0.866025403784437,1.5,-6.09583333333334));
#368443=CARTESIAN_POINT('Ctrl Pts',(-1.29903810567666,0.750000000000002,
-6.05416666666667));
#368444=CARTESIAN_POINT('Ctrl Pts',(-1.73205080756887,3.39462250276711E-15,
-6.0125));
#368445=CARTESIAN_POINT('Ctrl Pts',(-1.29903810567666,-0.749999999999995,
-5.97083333333333));
#368446=CARTESIAN_POINT('Ctrl Pts',(-0.866025403784437,-1.49999999999999,
-5.92916666666667));
#368447=CARTESIAN_POINT('Ctrl Pts',(-1.83697019872103E-16,-1.49999999999999,
-5.8875));
#368448=CARTESIAN_POINT('Ctrl Pts',(0.866025403784436,-1.49999999999999,
-5.84583333333333));
#368449=CARTESIAN_POINT('Ctrl Pts',(1.29903810567665,-0.749999999999996,
-5.80416666666667));
#368450=CARTESIAN_POINT('Ctrl Pts',(1.73205080756887,2.86111848753058E-15,
-5.7625));
#368451=CARTESIAN_POINT('Ctrl Pts',(1.29903810567666,0.75,-5.72083333333333));
#368452=CARTESIAN_POINT('Ctrl Pts',(0.866025403784437,1.5,-5.67916666666667));
#368453=CARTESIAN_POINT('Ctrl Pts',(0.,1.5,-5.6375));
#368454=CARTESIAN_POINT('Ctrl Pts',(-0.866025403784437,1.5,-5.59583333333333));
#368455=CARTESIAN_POINT('Ctrl Pts',(-1.29903810567666,0.750000000000002,
-5.55416666666667));
#368456=CARTESIAN_POINT('Ctrl Pts',(-1.73205080756887,3.17607466327397E-15,
-5.5125));
#368457=CARTESIAN_POINT('Ctrl Pts',(-1.29903810567666,-0.749999999999995,
-5.47083333333333));
#368458=CARTESIAN_POINT('Ctrl Pts',(-0.866025403784437,-1.49999999999999,
-5.42916666666667));
#368459=CARTESIAN_POINT('Ctrl Pts',(-1.83697019872103E-16,-1.49999999999999,
-5.3875));
#368460=CARTESIAN_POINT('Ctrl Pts',(0.866025403784436,-1.49999999999999,
-5.34583333333333));
#368461=CARTESIAN_POINT('Ctrl Pts',(1.29903810567665,-0.749999999999996,
-5.30416666666667));
#368462=CARTESIAN_POINT('Ctrl Pts',(1.73205080756887,2.64257064803744E-15,
-5.2625));
#368463=CARTESIAN_POINT('Ctrl Pts',(1.29903810567666,0.75,-5.22083333333333));
#368464=CARTESIAN_POINT('Ctrl Pts',(0.866025403784437,1.5,-5.17916666666667));
#368465=CARTESIAN_POINT('Ctrl Pts',(0.,1.5,-5.1375));
#368466=CARTESIAN_POINT('Ctrl Pts',(-0.866025403784437,1.5,-5.09583333333333));
#368467=CARTESIAN_POINT('Ctrl Pts',(-1.29903810567666,0.750000000000002,
-5.05416666666667));
#368468=CARTESIAN_POINT('Ctrl Pts',(-1.73205080756887,2.95752682378083E-15,
-5.0125));
#368469=CARTESIAN_POINT('Ctrl Pts',(-1.29903810567666,-0.749999999999995,
-4.97083333333333));
#368470=CARTESIAN_POINT('Ctrl Pts',(-0.866025403784437,-1.49999999999999,
-4.92916666666667));
#368471=CARTESIAN_POINT('Ctrl Pts',(-1.83697019872103E-16,-1.49999999999999,
-4.8875));
#368472=CARTESIAN_POINT('Ctrl Pts',(0.866025403784436,-1.49999999999999,
-4.84583333333333));
#368473=CARTESIAN_POINT('Ctrl Pts',(1.29903810567665,-0.749999999999996,
-4.80416666666667));
#368474=CARTESIAN_POINT('Ctrl Pts',(1.73205080756887,2.4240228085443E-15,
-4.7625));
#368475=CARTESIAN_POINT('Ctrl Pts',(1.29903810567666,0.75,-4.72083333333333));
#368476=CARTESIAN_POINT('Ctrl Pts',(0.866025403784437,1.5,-4.67916666666667));
#368477=CARTESIAN_POINT('Ctrl Pts',(0.,1.5,-4.6375));
#368478=CARTESIAN_POINT('Ctrl Pts',(-0.866025403784437,1.5,-4.59583333333333));
#368479=CARTESIAN_POINT('Ctrl Pts',(-1.29903810567666,0.750000000000001,
-4.55416666666667));
#368480=CARTESIAN_POINT('Ctrl Pts',(-1.73205080756887,2.73897898428769E-15,
-4.5125));
#368481=CARTESIAN_POINT('Ctrl Pts',(-1.29903810567666,-0.749999999999995,
-4.47083333333333));
#368482=CARTESIAN_POINT('Ctrl Pts',(-0.866025403784437,-1.49999999999999,
-4.42916666666667));
#368483=CARTESIAN_POINT('Ctrl Pts',(-1.83697019872103E-16,-1.49999999999999,
-4.3875));
#368484=CARTESIAN_POINT('Ctrl Pts',(0.866025403784436,-1.49999999999999,
-4.34583333333333));
#368485=CARTESIAN_POINT('Ctrl Pts',(1.29903810567665,-0.749999999999996,
-4.30416666666667));
#368486=CARTESIAN_POINT('Ctrl Pts',(1.73205080756887,2.20547496905115E-15,
-4.2625));
#368487=CARTESIAN_POINT('Ctrl Pts',(1.29903810567666,0.75,-4.22083333333333));
#368488=CARTESIAN_POINT('Ctrl Pts',(0.866025403784437,1.5,-4.17916666666667));
#368489=CARTESIAN_POINT('Ctrl Pts',(0.,1.5,-4.1375));
#368490=CARTESIAN_POINT('Ctrl Pts',(-0.866025403784437,1.5,-4.09583333333333));
#368491=CARTESIAN_POINT('Ctrl Pts',(-1.29903810567666,0.750000000000001,
-4.05416666666667));
#368492=CARTESIAN_POINT('Ctrl Pts',(-1.73205080756887,2.52043114479455E-15,
-4.0125));
#368493=CARTESIAN_POINT('Ctrl Pts',(-1.29903810567666,-0.749999999999996,
-3.97083333333333));
#368494=CARTESIAN_POINT('Ctrl Pts',(-0.866025403784437,-1.49999999999999,
-3.92916666666667));
#368495=CARTESIAN_POINT('Ctrl Pts',(-1.83697019872103E-16,-1.49999999999999,
-3.8875));
#368496=CARTESIAN_POINT('Ctrl Pts',(0.866025403784436,-1.49999999999999,
-3.84583333333333));
#368497=CARTESIAN_POINT('Ctrl Pts',(1.29903810567665,-0.749999999999997,
-3.80416666666667));
#368498=CARTESIAN_POINT('Ctrl Pts',(1.73205080756887,1.98692712955801E-15,
-3.7625));
#368499=CARTESIAN_POINT('Ctrl Pts',(1.29903810567666,0.749999999999999,
-3.72083333333333));
#368500=CARTESIAN_POINT('Ctrl Pts',(0.866025403784437,1.5,-3.67916666666667));
#368501=CARTESIAN_POINT('Ctrl Pts',(0.,1.5,-3.6375));
#368502=CARTESIAN_POINT('Ctrl Pts',(-0.866025403784437,1.5,-3.59583333333333));
#368503=CARTESIAN_POINT('Ctrl Pts',(-1.29903810567666,0.750000000000001,
-3.55416666666667));
#368504=CARTESIAN_POINT('Ctrl Pts',(-1.73205080756887,2.3018833053014E-15,
-3.5125));
#368505=CARTESIAN_POINT('Ctrl Pts',(-1.29903810567666,-0.749999999999996,
-3.47083333333333));
#368506=CARTESIAN_POINT('Ctrl Pts',(-0.866025403784437,-1.49999999999999,
-3.42916666666667));
#368507=CARTESIAN_POINT('Ctrl Pts',(-1.83697019872103E-16,-1.49999999999999,
-3.3875));
#368508=CARTESIAN_POINT('Ctrl Pts',(0.866025403784436,-1.5,-3.34583333333333));
#368509=CARTESIAN_POINT('Ctrl Pts',(1.29903810567665,-0.749999999999997,
-3.30416666666667));
#368510=CARTESIAN_POINT('Ctrl Pts',(1.73205080756887,1.76837929006487E-15,
-3.2625));
#368511=CARTESIAN_POINT('Ctrl Pts',(1.29903810567666,0.749999999999999,
-3.22083333333333));
#368512=CARTESIAN_POINT('Ctrl Pts',(0.866025403784437,1.5,-3.17916666666667));
#368513=CARTESIAN_POINT('Ctrl Pts',(0.,1.5,-3.1375));
#368514=CARTESIAN_POINT('Ctrl Pts',(-0.866025403784437,1.5,-3.09583333333333));
#368515=CARTESIAN_POINT('Ctrl Pts',(-1.29903810567666,0.750000000000001,
-3.05416666666667));
#368516=CARTESIAN_POINT('Ctrl Pts',(-1.73205080756887,2.08333546580826E-15,
-3.0125));
#368517=CARTESIAN_POINT('Ctrl Pts',(-1.29903810567666,-0.749999999999996,
-2.97083333333333));
#368518=CARTESIAN_POINT('Ctrl Pts',(-0.866025403784437,-1.49999999999999,
-2.92916666666667));
#368519=CARTESIAN_POINT('Ctrl Pts',(-1.83697019872103E-16,-1.49999999999999,
-2.8875));
#368520=CARTESIAN_POINT('Ctrl Pts',(0.866025403784436,-1.5,-2.84583333333333));
#368521=CARTESIAN_POINT('Ctrl Pts',(1.29903810567665,-0.749999999999997,
-2.80416666666667));
#368522=CARTESIAN_POINT('Ctrl Pts',(1.73205080756887,1.54983145057173E-15,
-2.7625));
#368523=CARTESIAN_POINT('Ctrl Pts',(1.29903810567666,0.749999999999999,
-2.72083333333333));
#368524=CARTESIAN_POINT('Ctrl Pts',(0.866025403784437,1.5,-2.67916666666667));
#368525=CARTESIAN_POINT('Ctrl Pts',(0.,1.5,-2.6375));
#368526=CARTESIAN_POINT('Ctrl Pts',(-0.866025403784437,1.5,-2.59583333333333));
#368527=CARTESIAN_POINT('Ctrl Pts',(-1.29903810567666,0.75,-2.55416666666667));
#368528=CARTESIAN_POINT('Ctrl Pts',(-1.73205080756887,1.86478762631512E-15,
-2.5125));
#368529=CARTESIAN_POINT('Ctrl Pts',(-1.29903810567666,-0.749999999999996,
-2.47083333333333));
#368530=CARTESIAN_POINT('Ctrl Pts',(-0.866025403784437,-1.49999999999999,
-2.42916666666667));
#368531=CARTESIAN_POINT('Ctrl Pts',(-1.83697019872103E-16,-1.5,-2.3875));
#368532=CARTESIAN_POINT('Ctrl Pts',(0.866025403784436,-1.5,-2.34583333333333));
#368533=CARTESIAN_POINT('Ctrl Pts',(1.29903810567665,-0.749999999999997,
-2.30416666666667));
#368534=CARTESIAN_POINT('Ctrl Pts',(1.73205080756887,1.33128361107859E-15,
-2.2625));
#368535=CARTESIAN_POINT('Ctrl Pts',(1.29903810567666,0.749999999999999,
-2.22083333333333));
#368536=CARTESIAN_POINT('Ctrl Pts',(0.866025403784437,1.5,-2.17916666666667));
#368537=CARTESIAN_POINT('Ctrl Pts',(0.,1.5,-2.1375));
#368538=CARTESIAN_POINT('Ctrl Pts',(-0.866025403784437,1.5,-2.09583333333333));
#368539=CARTESIAN_POINT('Ctrl Pts',(-1.29903810567666,0.75,-2.05416666666667));
#368540=CARTESIAN_POINT('Ctrl Pts',(-1.73205080756887,1.64623978682198E-15,
-2.0125));
#368541=CARTESIAN_POINT('Ctrl Pts',(-1.29903810567666,-0.749999999999996,
-1.97083333333333));
#368542=CARTESIAN_POINT('Ctrl Pts',(-0.866025403784437,-1.49999999999999,
-1.92916666666667));
#368543=CARTESIAN_POINT('Ctrl Pts',(-1.83697019872103E-16,-1.5,-1.8875));
#368544=CARTESIAN_POINT('Ctrl Pts',(0.866025403784436,-1.5,-1.84583333333334));
#368545=CARTESIAN_POINT('Ctrl Pts',(1.29903810567665,-0.749999999999998,
-1.80416666666667));
#368546=CARTESIAN_POINT('Ctrl Pts',(1.73205080756887,1.11273577158545E-15,
-1.7625));
#368547=CARTESIAN_POINT('Ctrl Pts',(1.29903810567666,0.749999999999999,
-1.72083333333333));
#368548=CARTESIAN_POINT('Ctrl Pts',(0.866025403784437,1.5,-1.67916666666667));
#368549=CARTESIAN_POINT('Ctrl Pts',(0.,1.5,-1.6375));
#368550=CARTESIAN_POINT('Ctrl Pts',(-1.43925448419918E-16,-1.17524047358083,
-2.2));
#368551=CARTESIAN_POINT('Ctrl Pts',(0.678525403784435,-1.17524047358083,
-2.15833333333333));
#368552=CARTESIAN_POINT('Ctrl Pts',(1.01778810567665,-0.587620236790414,
-2.11666666666667));
#368553=CARTESIAN_POINT('Ctrl Pts',(1.35705080756887,1.3182145537207E-15,
-2.075));
#368554=CARTESIAN_POINT('Ctrl Pts',(1.01778810567665,0.587620236790415,
-2.03333333333333));
#368555=CARTESIAN_POINT('Ctrl Pts',(0.678525403784436,1.17524047358083,
-1.99166666666667));
#368556=CARTESIAN_POINT('Ctrl Pts',(0.,1.17524047358083,-1.95));
#368557=CARTESIAN_POINT('Ctrl Pts',(-0.678525403784435,1.17524047358083,
-1.90833333333333));
#368558=CARTESIAN_POINT('Ctrl Pts',(-1.01778810567665,0.587620236790416,
-1.86666666666667));
#368559=CARTESIAN_POINT('Ctrl Pts',(-1.35705080756887,1.54132221952804E-15,
-1.825));
#368560=CARTESIAN_POINT('Ctrl Pts',(-1.01778810567665,-0.587620236790413,
-1.78333333333333));
#368561=CARTESIAN_POINT('Ctrl Pts',(-0.678525403784426,-1.17524047358084,
-1.74166666666667));
#368562=CARTESIAN_POINT('Ctrl Pts',(-1.43925448419918E-16,-1.17524047358083,
-1.7));
#368563=CARTESIAN_POINT('Origin',(0.,-7.56339435525888E-14,-9.91875));
#368564=CARTESIAN_POINT('Ctrl Pts',(-1.43925448419918E-16,-1.17524047358083,
-2.1375));
#368565=CARTESIAN_POINT('Ctrl Pts',(0.678525403784435,-1.17524047358083,
-2.09583333333333));
#368566=CARTESIAN_POINT('Ctrl Pts',(1.01778810567665,-0.587620236790414,
-2.05416666666667));
#368567=CARTESIAN_POINT('Ctrl Pts',(1.35705080756887,1.29089607378406E-15,
-2.0125));
#368568=CARTESIAN_POINT('Ctrl Pts',(1.01778810567665,0.587620236790415,
-1.97083333333333));
#368569=CARTESIAN_POINT('Ctrl Pts',(0.678525403784436,1.17524047358083,
-1.92916666666667));
#368570=CARTESIAN_POINT('Ctrl Pts',(0.,1.17524047358083,-1.8875));
#368571=CARTESIAN_POINT('Ctrl Pts',(-0.678525403784435,1.17524047358083,
-1.84583333333333));
#368572=CARTESIAN_POINT('Ctrl Pts',(-1.01778810567665,0.587620236790416,
-1.80416666666667));
#368573=CARTESIAN_POINT('Ctrl Pts',(-1.35705080756887,1.5140037395914E-15,
-1.7625));
#368574=CARTESIAN_POINT('Ctrl Pts',(-1.01778810567665,-0.587620236790413,
-1.72083333333333));
#368575=CARTESIAN_POINT('Ctrl Pts',(-0.937699045799841,-0.726338557627476,
-1.71099716760418));
#368576=CARTESIAN_POINT('Ctrl Pts',(-0.823407874165093,-0.838564036615816,
-1.7));
#368577=CARTESIAN_POINT('Ctrl Pts',(0.,1.50000767573777,-9.69999556841073));
#368578=CARTESIAN_POINT('Ctrl Pts',(-0.866029835373706,1.50000767573777,
-9.65832890174406));
#368579=CARTESIAN_POINT('Ctrl Pts',(-1.29904475306056,0.75000383786889,
-9.6166622350774));
#368580=CARTESIAN_POINT('Ctrl Pts',(-1.73205967074741,4.95177446484038E-15,
-9.57499556841073));
#368581=CARTESIAN_POINT('Ctrl Pts',(-1.29904475306056,-0.75000383786888,
-9.53332890174407));
#368582=CARTESIAN_POINT('Ctrl Pts',(-0.866029835373706,-1.50000767573776,
-9.4916622350774));
#368583=CARTESIAN_POINT('Ctrl Pts',(-1.83697959878872E-16,-1.50000767573776,
-9.44999556841073));
#368584=CARTESIAN_POINT('Ctrl Pts',(0.866029835373705,-1.50000767573776,
-9.40832890174407));
#368585=CARTESIAN_POINT('Ctrl Pts',(1.29904475306056,-0.75000383786888,
-9.3666622350774));
#368586=CARTESIAN_POINT('Ctrl Pts',(1.73205967074741,4.4182682787512E-15,
-9.32499556841073));
#368587=CARTESIAN_POINT('Ctrl Pts',(1.29904475306056,0.750003837868888,
-9.28332890174407));
#368588=CARTESIAN_POINT('Ctrl Pts',(0.866029835373707,1.50000767573777,
-9.2416622350774));
#368589=CARTESIAN_POINT('Ctrl Pts',(0.,1.50000767573777,-9.19999556841073));
#368590=CARTESIAN_POINT('Ctrl Pts',(-0.866029835373706,1.50000767573777,
-9.15832890174407));
#368591=CARTESIAN_POINT('Ctrl Pts',(-1.29904475306056,0.750003837868889,
-9.1166622350774));
#368592=CARTESIAN_POINT('Ctrl Pts',(-1.73205967074741,4.73322662534724E-15,
-9.07499556841073));
#368593=CARTESIAN_POINT('Ctrl Pts',(-1.29904475306056,-0.75000383786888,
-9.03332890174407));
#368594=CARTESIAN_POINT('Ctrl Pts',(-0.866029835373706,-1.50000767573776,
-8.9916622350774));
#368595=CARTESIAN_POINT('Ctrl Pts',(-1.83697959878872E-16,-1.50000767573776,
-8.94999556841073));
#368596=CARTESIAN_POINT('Ctrl Pts',(0.866029835373705,-1.50000767573776,
-8.90832890174407));
#368597=CARTESIAN_POINT('Ctrl Pts',(1.29904475306056,-0.750003837868881,
-8.8666622350774));
#368598=CARTESIAN_POINT('Ctrl Pts',(1.73205967074741,4.19972043925806E-15,
-8.82499556841073));
#368599=CARTESIAN_POINT('Ctrl Pts',(1.29904475306056,0.750003837868888,
-8.78332890174407));
#368600=CARTESIAN_POINT('Ctrl Pts',(0.866029835373707,1.50000767573777,
-8.7416622350774));
#368601=CARTESIAN_POINT('Ctrl Pts',(0.,1.50000767573777,-8.69999556841073));
#368602=CARTESIAN_POINT('Ctrl Pts',(-0.866029835373706,1.50000767573777,
-8.65832890174407));
#368603=CARTESIAN_POINT('Ctrl Pts',(-1.29904475306056,0.750003837868889,
-8.6166622350774));
#368604=CARTESIAN_POINT('Ctrl Pts',(-1.73205967074741,4.5146787858541E-15,
-8.57499556841073));
#368605=CARTESIAN_POINT('Ctrl Pts',(-1.29904475306056,-0.75000383786888,
-8.53332890174406));
#368606=CARTESIAN_POINT('Ctrl Pts',(-0.866029835373706,-1.50000767573776,
-8.4916622350774));
#368607=CARTESIAN_POINT('Ctrl Pts',(-1.83697959878872E-16,-1.50000767573776,
-8.44999556841073));
#368608=CARTESIAN_POINT('Ctrl Pts',(0.866029835373705,-1.50000767573776,
-8.40832890174406));
#368609=CARTESIAN_POINT('Ctrl Pts',(1.29904475306056,-0.750003837868881,
-8.3666622350774));
#368610=CARTESIAN_POINT('Ctrl Pts',(1.73205967074741,3.98117259976492E-15,
-8.32499556841073));
#368611=CARTESIAN_POINT('Ctrl Pts',(1.29904475306056,0.750003837868888,
-8.28332890174407));
#368612=CARTESIAN_POINT('Ctrl Pts',(0.866029835373707,1.50000767573777,
-8.2416622350774));
#368613=CARTESIAN_POINT('Ctrl Pts',(0.,1.50000767573777,-8.19999556841073));
#368614=CARTESIAN_POINT('Ctrl Pts',(-0.866029835373706,1.50000767573777,
-8.15832890174407));
#368615=CARTESIAN_POINT('Ctrl Pts',(-1.29904475306056,0.750003837868889,
-8.1166622350774));
#368616=CARTESIAN_POINT('Ctrl Pts',(-1.73205967074741,4.29613094636096E-15,
-8.07499556841073));
#368617=CARTESIAN_POINT('Ctrl Pts',(-1.29904475306056,-0.75000383786888,
-8.03332890174407));
#368618=CARTESIAN_POINT('Ctrl Pts',(-0.866029835373706,-1.50000767573776,
-7.9916622350774));
#368619=CARTESIAN_POINT('Ctrl Pts',(-1.83697959878872E-16,-1.50000767573776,
-7.94999556841073));
#368620=CARTESIAN_POINT('Ctrl Pts',(0.866029835373705,-1.50000767573776,
-7.90832890174407));
#368621=CARTESIAN_POINT('Ctrl Pts',(1.29904475306056,-0.750003837868881,
-7.8666622350774));
#368622=CARTESIAN_POINT('Ctrl Pts',(1.73205967074741,3.76262476027178E-15,
-7.82499556841073));
#368623=CARTESIAN_POINT('Ctrl Pts',(1.29904475306056,0.750003837868888,
-7.78332890174406));
#368624=CARTESIAN_POINT('Ctrl Pts',(0.866029835373707,1.50000767573777,
-7.7416622350774));
#368625=CARTESIAN_POINT('Ctrl Pts',(0.,1.50000767573777,-7.69999556841073));
#368626=CARTESIAN_POINT('Ctrl Pts',(-0.866029835373706,1.50000767573777,
-7.65832890174406));
#368627=CARTESIAN_POINT('Ctrl Pts',(-1.29904475306056,0.750003837868889,
-7.6166622350774));
#368628=CARTESIAN_POINT('Ctrl Pts',(-1.73205967074741,4.07758310686782E-15,
-7.57499556841073));
#368629=CARTESIAN_POINT('Ctrl Pts',(-1.29904475306056,-0.75000383786888,
-7.53332890174407));
#368630=CARTESIAN_POINT('Ctrl Pts',(-0.866029835373706,-1.50000767573776,
-7.4916622350774));
#368631=CARTESIAN_POINT('Ctrl Pts',(-1.83697959878872E-16,-1.50000767573777,
-7.44999556841073));
#368632=CARTESIAN_POINT('Ctrl Pts',(0.866029835373705,-1.50000767573777,
-7.40832890174406));
#368633=CARTESIAN_POINT('Ctrl Pts',(1.29904475306056,-0.750003837868881,
-7.3666622350774));
#368634=CARTESIAN_POINT('Ctrl Pts',(1.73205967074741,3.54407692077864E-15,
-7.32499556841073));
#368635=CARTESIAN_POINT('Ctrl Pts',(1.29904475306056,0.750003837868887,
-7.28332890174406));
#368636=CARTESIAN_POINT('Ctrl Pts',(0.866029835373707,1.50000767573777,
-7.2416622350774));
#368637=CARTESIAN_POINT('Ctrl Pts',(0.,1.50000767573777,-7.19999556841073));
#368638=CARTESIAN_POINT('Ctrl Pts',(-0.866029835373706,1.50000767573777,
-7.15832890174407));
#368639=CARTESIAN_POINT('Ctrl Pts',(-1.29904475306056,0.750003837868889,
-7.1166622350774));
#368640=CARTESIAN_POINT('Ctrl Pts',(-1.73205967074741,3.85903526737468E-15,
-7.07499556841073));
#368641=CARTESIAN_POINT('Ctrl Pts',(-1.29904475306056,-0.750003837868881,
-7.03332890174407));
#368642=CARTESIAN_POINT('Ctrl Pts',(-0.866029835373706,-1.50000767573776,
-6.9916622350774));
#368643=CARTESIAN_POINT('Ctrl Pts',(-1.83697959878872E-16,-1.50000767573777,
-6.94999556841073));
#368644=CARTESIAN_POINT('Ctrl Pts',(0.866029835373705,-1.50000767573777,
-6.90832890174407));
#368645=CARTESIAN_POINT('Ctrl Pts',(1.29904475306056,-0.750003837868882,
-6.8666622350774));
#368646=CARTESIAN_POINT('Ctrl Pts',(1.73205967074741,3.3255290812855E-15,
-6.82499556841073));
#368647=CARTESIAN_POINT('Ctrl Pts',(1.29904475306056,0.750003837868887,
-6.78332890174407));
#368648=CARTESIAN_POINT('Ctrl Pts',(0.866029835373707,1.50000767573777,
-6.7416622350774));
#368649=CARTESIAN_POINT('Ctrl Pts',(0.,1.50000767573777,-6.69999556841073));
#368650=CARTESIAN_POINT('Ctrl Pts',(-0.866029835373706,1.50000767573777,
-6.65832890174406));
#368651=CARTESIAN_POINT('Ctrl Pts',(-1.29904475306056,0.750003837868888,
-6.6166622350774));
#368652=CARTESIAN_POINT('Ctrl Pts',(-1.73205967074741,3.64048742788154E-15,
-6.57499556841073));
#368653=CARTESIAN_POINT('Ctrl Pts',(-1.29904475306056,-0.750003837868881,
-6.53332890174406));
#368654=CARTESIAN_POINT('Ctrl Pts',(-0.866029835373706,-1.50000767573776,
-6.4916622350774));
#368655=CARTESIAN_POINT('Ctrl Pts',(-1.83697959878872E-16,-1.50000767573777,
-6.44999556841073));
#368656=CARTESIAN_POINT('Ctrl Pts',(0.866029835373705,-1.50000767573777,
-6.40832890174407));
#368657=CARTESIAN_POINT('Ctrl Pts',(1.29904475306056,-0.750003837868882,
-6.3666622350774));
#368658=CARTESIAN_POINT('Ctrl Pts',(1.73205967074741,3.10698124179236E-15,
-6.32499556841073));
#368659=CARTESIAN_POINT('Ctrl Pts',(1.29904475306056,0.750003837868887,
-6.28332890174407));
#368660=CARTESIAN_POINT('Ctrl Pts',(0.866029835373707,1.50000767573777,
-6.2416622350774));
#368661=CARTESIAN_POINT('Ctrl Pts',(0.,1.50000767573777,-6.19999556841073));
#368662=CARTESIAN_POINT('Ctrl Pts',(-0.866029835373706,1.50000767573777,
-6.15832890174407));
#368663=CARTESIAN_POINT('Ctrl Pts',(-1.29904475306056,0.750003837868888,
-6.1166622350774));
#368664=CARTESIAN_POINT('Ctrl Pts',(-1.73205967074741,3.42193958838839E-15,
-6.07499556841073));
#368665=CARTESIAN_POINT('Ctrl Pts',(-1.29904475306056,-0.750003837868881,
-6.03332890174406));
#368666=CARTESIAN_POINT('Ctrl Pts',(-0.866029835373706,-1.50000767573776,
-5.9916622350774));
#368667=CARTESIAN_POINT('Ctrl Pts',(-1.83697959878872E-16,-1.50000767573777,
-5.94999556841073));
#368668=CARTESIAN_POINT('Ctrl Pts',(0.866029835373705,-1.50000767573777,
-5.90832890174406));
#368669=CARTESIAN_POINT('Ctrl Pts',(1.29904475306056,-0.750003837868882,
-5.8666622350774));
#368670=CARTESIAN_POINT('Ctrl Pts',(1.73205967074741,2.88843340229921E-15,
-5.82499556841073));
#368671=CARTESIAN_POINT('Ctrl Pts',(1.29904475306056,0.750003837868887,
-5.78332890174407));
#368672=CARTESIAN_POINT('Ctrl Pts',(0.866029835373707,1.50000767573777,
-5.7416622350774));
#368673=CARTESIAN_POINT('Ctrl Pts',(0.,1.50000767573777,-5.69999556841073));
#368674=CARTESIAN_POINT('Ctrl Pts',(-0.866029835373706,1.50000767573777,
-5.65832890174406));
#368675=CARTESIAN_POINT('Ctrl Pts',(-1.29904475306056,0.750003837868888,
-5.6166622350774));
#368676=CARTESIAN_POINT('Ctrl Pts',(-1.73205967074741,3.20339174889525E-15,
-5.57499556841073));
#368677=CARTESIAN_POINT('Ctrl Pts',(-1.29904475306056,-0.750003837868881,
-5.53332890174407));
#368678=CARTESIAN_POINT('Ctrl Pts',(-0.866029835373706,-1.50000767573776,
-5.4916622350774));
#368679=CARTESIAN_POINT('Ctrl Pts',(-1.83697959878872E-16,-1.50000767573777,
-5.44999556841073));
#368680=CARTESIAN_POINT('Ctrl Pts',(0.866029835373705,-1.50000767573777,
-5.40832890174406));
#368681=CARTESIAN_POINT('Ctrl Pts',(1.29904475306056,-0.750003837868882,
-5.3666622350774));
#368682=CARTESIAN_POINT('Ctrl Pts',(1.73205967074741,2.66988556280607E-15,
-5.32499556841073));
#368683=CARTESIAN_POINT('Ctrl Pts',(1.29904475306056,0.750003837868886,
-5.28332890174406));
#368684=CARTESIAN_POINT('Ctrl Pts',(0.866029835373707,1.50000767573777,
-5.2416622350774));
#368685=CARTESIAN_POINT('Ctrl Pts',(0.,1.50000767573777,-5.19999556841073));
#368686=CARTESIAN_POINT('Ctrl Pts',(-0.866029835373706,1.50000767573777,
-5.15832890174406));
#368687=CARTESIAN_POINT('Ctrl Pts',(-1.29904475306056,0.750003837868888,
-5.1166622350774));
#368688=CARTESIAN_POINT('Ctrl Pts',(-1.73205967074741,2.98484390940211E-15,
-5.07499556841073));
#368689=CARTESIAN_POINT('Ctrl Pts',(-1.29904475306056,-0.750003837868881,
-5.03332890174407));
#368690=CARTESIAN_POINT('Ctrl Pts',(-0.866029835373706,-1.50000767573777,
-4.9916622350774));
#368691=CARTESIAN_POINT('Ctrl Pts',(-1.83697959878872E-16,-1.50000767573777,
-4.94999556841073));
#368692=CARTESIAN_POINT('Ctrl Pts',(0.866029835373705,-1.50000767573777,
-4.90832890174407));
#368693=CARTESIAN_POINT('Ctrl Pts',(1.29904475306056,-0.750003837868882,
-4.8666622350774));
#368694=CARTESIAN_POINT('Ctrl Pts',(1.73205967074741,2.45133772331293E-15,
-4.82499556841073));
#368695=CARTESIAN_POINT('Ctrl Pts',(1.29904475306056,0.750003837868886,
-4.78332890174407));
#368696=CARTESIAN_POINT('Ctrl Pts',(0.866029835373707,1.50000767573777,
-4.7416622350774));
#368697=CARTESIAN_POINT('Ctrl Pts',(0.,1.50000767573777,-4.69999556841073));
#368698=CARTESIAN_POINT('Ctrl Pts',(-0.866029835373706,1.50000767573777,
-4.65832890174406));
#368699=CARTESIAN_POINT('Ctrl Pts',(-1.29904475306056,0.750003837868888,
-4.6166622350774));
#368700=CARTESIAN_POINT('Ctrl Pts',(-1.73205967074741,2.76629606990897E-15,
-4.57499556841073));
#368701=CARTESIAN_POINT('Ctrl Pts',(-1.29904475306056,-0.750003837868882,
-4.53332890174406));
#368702=CARTESIAN_POINT('Ctrl Pts',(-0.866029835373706,-1.50000767573777,
-4.4916622350774));
#368703=CARTESIAN_POINT('Ctrl Pts',(-1.83697959878872E-16,-1.50000767573777,
-4.44999556841073));
#368704=CARTESIAN_POINT('Ctrl Pts',(0.866029835373705,-1.50000767573777,
-4.40832890174406));
#368705=CARTESIAN_POINT('Ctrl Pts',(1.29904475306056,-0.750003837868883,
-4.3666622350774));
#368706=CARTESIAN_POINT('Ctrl Pts',(1.73205967074741,2.23278988381979E-15,
-4.32499556841073));
#368707=CARTESIAN_POINT('Ctrl Pts',(1.29904475306056,0.750003837868886,
-4.28332890174406));
#368708=CARTESIAN_POINT('Ctrl Pts',(0.866029835373707,1.50000767573777,
-4.2416622350774));
#368709=CARTESIAN_POINT('Ctrl Pts',(0.,1.50000767573777,-4.19999556841073));
#368710=CARTESIAN_POINT('Ctrl Pts',(-0.866029835373706,1.50000767573777,
-4.15832890174406));
#368711=CARTESIAN_POINT('Ctrl Pts',(-1.29904475306056,0.750003837868887,
-4.1166622350774));
#368712=CARTESIAN_POINT('Ctrl Pts',(-1.73205967074741,2.54774823041583E-15,
-4.07499556841073));
#368713=CARTESIAN_POINT('Ctrl Pts',(-1.29904475306056,-0.750003837868882,
-4.03332890174407));
#368714=CARTESIAN_POINT('Ctrl Pts',(-0.866029835373706,-1.50000767573777,
-3.9916622350774));
#368715=CARTESIAN_POINT('Ctrl Pts',(-1.83697959878872E-16,-1.50000767573777,
-3.94999556841073));
#368716=CARTESIAN_POINT('Ctrl Pts',(0.866029835373705,-1.50000767573777,
-3.90832890174407));
#368717=CARTESIAN_POINT('Ctrl Pts',(1.29904475306056,-0.750003837868883,
-3.8666622350774));
#368718=CARTESIAN_POINT('Ctrl Pts',(1.73205967074741,2.01424204432665E-15,
-3.82499556841073));
#368719=CARTESIAN_POINT('Ctrl Pts',(1.29904475306056,0.750003837868886,
-3.78332890174407));
#368720=CARTESIAN_POINT('Ctrl Pts',(0.866029835373707,1.50000767573777,
-3.7416622350774));
#368721=CARTESIAN_POINT('Ctrl Pts',(0.,1.50000767573777,-3.69999556841073));
#368722=CARTESIAN_POINT('Ctrl Pts',(-0.866029835373706,1.50000767573777,
-3.65832890174407));
#368723=CARTESIAN_POINT('Ctrl Pts',(-1.29904475306056,0.750003837868887,
-3.6166622350774));
#368724=CARTESIAN_POINT('Ctrl Pts',(-1.73205967074741,2.32920039092269E-15,
-3.57499556841073));
#368725=CARTESIAN_POINT('Ctrl Pts',(-1.29904475306056,-0.750003837868882,
-3.53332890174406));
#368726=CARTESIAN_POINT('Ctrl Pts',(-0.866029835373706,-1.50000767573777,
-3.4916622350774));
#368727=CARTESIAN_POINT('Ctrl Pts',(-1.83697959878872E-16,-1.50000767573777,
-3.44999556841073));
#368728=CARTESIAN_POINT('Ctrl Pts',(0.866029835373705,-1.50000767573777,
-3.40832890174406));
#368729=CARTESIAN_POINT('Ctrl Pts',(1.29904475306056,-0.750003837868883,
-3.3666622350774));
#368730=CARTESIAN_POINT('Ctrl Pts',(1.73205967074741,1.79569420483351E-15,
-3.32499556841073));
#368731=CARTESIAN_POINT('Ctrl Pts',(1.29904475306056,0.750003837868886,
-3.28332890174406));
#368732=CARTESIAN_POINT('Ctrl Pts',(0.866029835373707,1.50000767573777,
-3.2416622350774));
#368733=CARTESIAN_POINT('Ctrl Pts',(0.,1.50000767573777,-3.19999556841073));
#368734=CARTESIAN_POINT('Ctrl Pts',(-0.866029835373706,1.50000767573777,
-3.15832890174406));
#368735=CARTESIAN_POINT('Ctrl Pts',(-1.29904475306056,0.750003837868887,
-3.1166622350774));
#368736=CARTESIAN_POINT('Ctrl Pts',(-1.73205967074741,2.11065255142955E-15,
-3.07499556841073));
#368737=CARTESIAN_POINT('Ctrl Pts',(-1.29904475306056,-0.750003837868882,
-3.03332890174407));
#368738=CARTESIAN_POINT('Ctrl Pts',(-0.866029835373706,-1.50000767573777,
-2.9916622350774));
#368739=CARTESIAN_POINT('Ctrl Pts',(-1.83697959878872E-16,-1.50000767573777,
-2.94999556841073));
#368740=CARTESIAN_POINT('Ctrl Pts',(0.866029835373705,-1.50000767573777,
-2.90832890174406));
#368741=CARTESIAN_POINT('Ctrl Pts',(1.29904475306056,-0.750003837868883,
-2.8666622350774));
#368742=CARTESIAN_POINT('Ctrl Pts',(1.73205967074741,1.57714636534037E-15,
-2.82499556841073));
#368743=CARTESIAN_POINT('Ctrl Pts',(1.29904475306056,0.750003837868885,
-2.78332890174406));
#368744=CARTESIAN_POINT('Ctrl Pts',(0.866029835373707,1.50000767573777,
-2.7416622350774));
#368745=CARTESIAN_POINT('Ctrl Pts',(0.,1.50000767573777,-2.69999556841073));
#368746=CARTESIAN_POINT('Ctrl Pts',(-0.866029835373706,1.50000767573777,
-2.65832890174406));
#368747=CARTESIAN_POINT('Ctrl Pts',(-1.29904475306056,0.750003837868887,
-2.6166622350774));
#368748=CARTESIAN_POINT('Ctrl Pts',(-1.73205967074741,1.89210471193641E-15,
-2.57499556841073));
#368749=CARTESIAN_POINT('Ctrl Pts',(-1.29904475306056,-0.750003837868882,
-2.53332890174406));
#368750=CARTESIAN_POINT('Ctrl Pts',(-0.866029835373706,-1.50000767573777,
-2.4916622350774));
#368751=CARTESIAN_POINT('Ctrl Pts',(-1.83697959878872E-16,-1.50000767573777,
-2.44999556841073));
#368752=CARTESIAN_POINT('Ctrl Pts',(0.866029835373705,-1.50000767573777,
-2.40832890174406));
#368753=CARTESIAN_POINT('Ctrl Pts',(1.29904475306056,-0.750003837868884,
-2.3666622350774));
#368754=CARTESIAN_POINT('Ctrl Pts',(1.73205967074741,1.35859852584723E-15,
-2.32499556841073));
#368755=CARTESIAN_POINT('Ctrl Pts',(1.29904475306056,0.750003837868885,
-2.28332890174407));
#368756=CARTESIAN_POINT('Ctrl Pts',(0.866029835373707,1.50000767573777,
-2.2416622350774));
#368757=CARTESIAN_POINT('Ctrl Pts',(0.,1.50000767573777,-2.19999556841073));
#368758=CARTESIAN_POINT('Ctrl Pts',(-0.866029835373706,1.50000767573777,
-2.15832890174407));
#368759=CARTESIAN_POINT('Ctrl Pts',(-1.29904475306056,0.750003837868886,
-2.1166622350774));
#368760=CARTESIAN_POINT('Ctrl Pts',(-1.73205967074741,1.67355687244326E-15,
-2.07499556841073));
#368761=CARTESIAN_POINT('Ctrl Pts',(-1.29904475306056,-0.750003837868883,
-2.03332890174407));
#368762=CARTESIAN_POINT('Ctrl Pts',(-0.866029835373706,-1.50000767573777,
-1.9916622350774));
#368763=CARTESIAN_POINT('Ctrl Pts',(-1.83697959878872E-16,-1.50000767573777,
-1.94999556841073));
#368764=CARTESIAN_POINT('Ctrl Pts',(0.866029835373705,-1.50000767573777,
-1.90832890174406));
#368765=CARTESIAN_POINT('Ctrl Pts',(1.29904475306056,-0.750003837868884,
-1.8666622350774));
#368766=CARTESIAN_POINT('Ctrl Pts',(1.73205967074741,1.14005068635409E-15,
-1.82499556841073));
#368767=CARTESIAN_POINT('Ctrl Pts',(1.29904475306056,0.750003837868885,
-1.78332890174407));
#368768=CARTESIAN_POINT('Ctrl Pts',(0.866029835373707,1.50000767573777,
-1.7416622350774));
#368769=CARTESIAN_POINT('Ctrl Pts',(0.,1.50000767573777,-1.69999556841073));
#368770=CARTESIAN_POINT('Ctrl Pts',(-0.866029835373706,1.50000767573777,
-1.65832890174407));
#368771=CARTESIAN_POINT('Ctrl Pts',(-1.29904475306056,0.750003837868886,
-1.6166622350774));
#368772=CARTESIAN_POINT('Ctrl Pts',(-1.73205967074741,1.45500903295012E-15,
-1.57499556841073));
#368773=CARTESIAN_POINT('Ctrl Pts',(-1.29904475306056,-0.750003837868883,
-1.53332890174407));
#368774=CARTESIAN_POINT('Ctrl Pts',(-0.866029835373706,-1.50000767573777,
-1.4916622350774));
#368775=CARTESIAN_POINT('Ctrl Pts',(-1.83697959878872E-16,-1.50000767573777,
-1.44999556841073));
#368776=CARTESIAN_POINT('Ctrl Pts',(0.866029835373705,-1.50000767573777,
-1.40832890174407));
#368777=CARTESIAN_POINT('Ctrl Pts',(1.29904475306056,-0.750003837868884,
-1.3666622350774));
#368778=CARTESIAN_POINT('Ctrl Pts',(1.73205967074741,9.21502846860943E-16,
-1.32499556841073));
#368779=CARTESIAN_POINT('Ctrl Pts',(1.29904475306056,0.750003837868885,
-1.28332890174407));
#368780=CARTESIAN_POINT('Ctrl Pts',(0.866029835373707,1.50000767573777,
-1.2416622350774));
#368781=CARTESIAN_POINT('Ctrl Pts',(0.,1.50000767573777,-1.19999556841073));
#368782=CARTESIAN_POINT('Ctrl Pts',(0.,1.17524047358083,-9.8875));
#368783=CARTESIAN_POINT('Ctrl Pts',(-0.678525403784435,1.17524047358083,
-9.84583333333333));
#368784=CARTESIAN_POINT('Ctrl Pts',(-1.01778810567665,0.58762023679042,
-9.80416666666667));
#368785=CARTESIAN_POINT('Ctrl Pts',(-1.35705080756887,5.01076917148166E-15,
-9.7625));
#368786=CARTESIAN_POINT('Ctrl Pts',(-1.01778810567665,-0.58762023679041,
-9.72083333333333));
#368787=CARTESIAN_POINT('Ctrl Pts',(-0.678525403784435,-1.17524047358082,
-9.67916666666667));
#368788=CARTESIAN_POINT('Ctrl Pts',(-1.43925448419918E-16,-1.17524047358082,
-9.6375));
#368789=CARTESIAN_POINT('Ctrl Pts',(0.678525403784435,-1.17524047358082,
-9.59583333333333));
#368790=CARTESIAN_POINT('Ctrl Pts',(1.01778810567665,-0.58762023679041,
-9.55416666666667));
#368791=CARTESIAN_POINT('Ctrl Pts',(1.35705080756887,4.56911366618118E-15,
-9.5125));
#368792=CARTESIAN_POINT('Ctrl Pts',(1.01778810567665,0.587620236790419,
-9.47083333333333));
#368793=CARTESIAN_POINT('Ctrl Pts',(0.678525403784436,1.17524047358083,
-9.42916666666667));
#368794=CARTESIAN_POINT('Ctrl Pts',(0.,1.17524047358083,-9.3875));
#368795=CARTESIAN_POINT('Ctrl Pts',(-0.678525403784435,1.17524047358083,
-9.34583333333333));
#368796=CARTESIAN_POINT('Ctrl Pts',(-1.01778810567665,0.58762023679042,
-9.30416666666667));
#368797=CARTESIAN_POINT('Ctrl Pts',(-1.35705080756887,4.79222133198851E-15,
-9.2625));
#368798=CARTESIAN_POINT('Ctrl Pts',(-1.01778810567665,-0.58762023679041,
-9.22083333333333));
#368799=CARTESIAN_POINT('Ctrl Pts',(-0.678525403784435,-1.17524047358082,
-9.17916666666667));
#368800=CARTESIAN_POINT('Ctrl Pts',(-1.43925448419918E-16,-1.17524047358082,
-9.1375));
#368801=CARTESIAN_POINT('Ctrl Pts',(0.678525403784435,-1.17524047358083,
-9.09583333333333));
#368802=CARTESIAN_POINT('Ctrl Pts',(1.01778810567665,-0.587620236790411,
-9.05416666666667));
#368803=CARTESIAN_POINT('Ctrl Pts',(1.35705080756887,4.35056582668803E-15,
-9.0125));
#368804=CARTESIAN_POINT('Ctrl Pts',(1.01778810567665,0.587620236790418,
-8.97083333333333));
#368805=CARTESIAN_POINT('Ctrl Pts',(0.678525403784436,1.17524047358083,
-8.92916666666667));
#368806=CARTESIAN_POINT('Ctrl Pts',(0.,1.17524047358083,-8.8875));
#368807=CARTESIAN_POINT('Ctrl Pts',(-0.678525403784435,1.17524047358083,
-8.84583333333333));
#368808=CARTESIAN_POINT('Ctrl Pts',(-1.01778810567665,0.587620236790419,
-8.80416666666667));
#368809=CARTESIAN_POINT('Ctrl Pts',(-1.35705080756887,4.57367349249537E-15,
-8.7625));
#368810=CARTESIAN_POINT('Ctrl Pts',(-1.01778810567665,-0.58762023679041,
-8.72083333333333));
#368811=CARTESIAN_POINT('Ctrl Pts',(-0.678525403784435,-1.17524047358082,
-8.67916666666667));
#368812=CARTESIAN_POINT('Ctrl Pts',(-1.43925448419918E-16,-1.17524047358082,
-8.6375));
#368813=CARTESIAN_POINT('Ctrl Pts',(0.678525403784435,-1.17524047358083,
-8.59583333333333));
#368814=CARTESIAN_POINT('Ctrl Pts',(1.01778810567665,-0.587620236790411,
-8.55416666666667));
#368815=CARTESIAN_POINT('Ctrl Pts',(1.35705080756887,4.13201798719489E-15,
-8.5125));
#368816=CARTESIAN_POINT('Ctrl Pts',(1.01778810567665,0.587620236790418,
-8.47083333333333));
#368817=CARTESIAN_POINT('Ctrl Pts',(0.678525403784436,1.17524047358083,
-8.42916666666667));
#368818=CARTESIAN_POINT('Ctrl Pts',(0.,1.17524047358083,-8.3875));
#368819=CARTESIAN_POINT('Ctrl Pts',(-0.678525403784435,1.17524047358083,
-8.34583333333333));
#368820=CARTESIAN_POINT('Ctrl Pts',(-1.01778810567665,0.587620236790419,
-8.30416666666667));
#368821=CARTESIAN_POINT('Ctrl Pts',(-1.35705080756887,4.35512565300223E-15,
-8.2625));
#368822=CARTESIAN_POINT('Ctrl Pts',(-1.01778810567665,-0.58762023679041,
-8.22083333333333));
#368823=CARTESIAN_POINT('Ctrl Pts',(-0.678525403784435,-1.17524047358082,
-8.17916666666667));
#368824=CARTESIAN_POINT('Ctrl Pts',(-1.43925448419918E-16,-1.17524047358083,
-8.1375));
#368825=CARTESIAN_POINT('Ctrl Pts',(0.678525403784435,-1.17524047358083,
-8.09583333333333));
#368826=CARTESIAN_POINT('Ctrl Pts',(1.01778810567665,-0.587620236790411,
-8.05416666666667));
#368827=CARTESIAN_POINT('Ctrl Pts',(1.35705080756887,3.91347014770175E-15,
-8.0125));
#368828=CARTESIAN_POINT('Ctrl Pts',(1.01778810567665,0.587620236790418,
-7.97083333333333));
#368829=CARTESIAN_POINT('Ctrl Pts',(0.678525403784436,1.17524047358083,
-7.92916666666667));
#368830=CARTESIAN_POINT('Ctrl Pts',(0.,1.17524047358083,-7.8875));
#368831=CARTESIAN_POINT('Ctrl Pts',(-0.678525403784435,1.17524047358083,
-7.84583333333333));
#368832=CARTESIAN_POINT('Ctrl Pts',(-1.01778810567665,0.587620236790419,
-7.80416666666667));
#368833=CARTESIAN_POINT('Ctrl Pts',(-1.35705080756887,4.13657781350909E-15,
-7.7625));
#368834=CARTESIAN_POINT('Ctrl Pts',(-1.01778810567665,-0.58762023679041,
-7.72083333333333));
#368835=CARTESIAN_POINT('Ctrl Pts',(-0.678525403784435,-1.17524047358083,
-7.67916666666667));
#368836=CARTESIAN_POINT('Ctrl Pts',(-1.43925448419918E-16,-1.17524047358083,
-7.6375));
#368837=CARTESIAN_POINT('Ctrl Pts',(0.678525403784435,-1.17524047358083,
-7.59583333333333));
#368838=CARTESIAN_POINT('Ctrl Pts',(1.01778810567665,-0.587620236790411,
-7.55416666666667));
#368839=CARTESIAN_POINT('Ctrl Pts',(1.35705080756887,3.69492230820861E-15,
-7.5125));
#368840=CARTESIAN_POINT('Ctrl Pts',(1.01778810567665,0.587620236790418,
-7.47083333333333));
#368841=CARTESIAN_POINT('Ctrl Pts',(0.678525403784436,1.17524047358083,
-7.42916666666667));
#368842=CARTESIAN_POINT('Ctrl Pts',(0.,1.17524047358083,-7.3875));
#368843=CARTESIAN_POINT('Ctrl Pts',(-0.678525403784435,1.17524047358083,
-7.34583333333334));
#368844=CARTESIAN_POINT('Ctrl Pts',(-1.01778810567665,0.587620236790419,
-7.30416666666667));
#368845=CARTESIAN_POINT('Ctrl Pts',(-1.35705080756887,3.91802997401595E-15,
-7.2625));
#368846=CARTESIAN_POINT('Ctrl Pts',(-1.01778810567665,-0.587620236790411,
-7.22083333333333));
#368847=CARTESIAN_POINT('Ctrl Pts',(-0.678525403784435,-1.17524047358083,
-7.17916666666667));
#368848=CARTESIAN_POINT('Ctrl Pts',(-1.43925448419918E-16,-1.17524047358083,
-7.1375));
#368849=CARTESIAN_POINT('Ctrl Pts',(0.678525403784435,-1.17524047358083,
-7.09583333333333));
#368850=CARTESIAN_POINT('Ctrl Pts',(1.01778810567665,-0.587620236790411,
-7.05416666666667));
#368851=CARTESIAN_POINT('Ctrl Pts',(1.35705080756887,3.47637446871547E-15,
-7.0125));
#368852=CARTESIAN_POINT('Ctrl Pts',(1.01778810567665,0.587620236790417,
-6.97083333333333));
#368853=CARTESIAN_POINT('Ctrl Pts',(0.678525403784436,1.17524047358083,
-6.92916666666667));
#368854=CARTESIAN_POINT('Ctrl Pts',(0.,1.17524047358083,-6.8875));
#368855=CARTESIAN_POINT('Ctrl Pts',(-0.678525403784435,1.17524047358083,
-6.84583333333333));
#368856=CARTESIAN_POINT('Ctrl Pts',(-1.01778810567665,0.587620236790418,
-6.80416666666667));
#368857=CARTESIAN_POINT('Ctrl Pts',(-1.35705080756887,3.69948213452281E-15,
-6.7625));
#368858=CARTESIAN_POINT('Ctrl Pts',(-1.01778810567665,-0.587620236790411,
-6.72083333333333));
#368859=CARTESIAN_POINT('Ctrl Pts',(-0.678525403784435,-1.17524047358083,
-6.67916666666667));
#368860=CARTESIAN_POINT('Ctrl Pts',(-1.43925448419918E-16,-1.17524047358083,
-6.6375));
#368861=CARTESIAN_POINT('Ctrl Pts',(0.678525403784435,-1.17524047358083,
-6.59583333333333));
#368862=CARTESIAN_POINT('Ctrl Pts',(1.01778810567665,-0.587620236790412,
-6.55416666666667));
#368863=CARTESIAN_POINT('Ctrl Pts',(1.35705080756887,3.25782662922233E-15,
-6.5125));
#368864=CARTESIAN_POINT('Ctrl Pts',(1.01778810567665,0.587620236790417,
-6.47083333333333));
#368865=CARTESIAN_POINT('Ctrl Pts',(0.678525403784436,1.17524047358083,
-6.42916666666667));
#368866=CARTESIAN_POINT('Ctrl Pts',(0.,1.17524047358083,-6.3875));
#368867=CARTESIAN_POINT('Ctrl Pts',(-0.678525403784435,1.17524047358083,
-6.34583333333333));
#368868=CARTESIAN_POINT('Ctrl Pts',(-1.01778810567665,0.587620236790418,
-6.30416666666667));
#368869=CARTESIAN_POINT('Ctrl Pts',(-1.35705080756887,3.48093429502967E-15,
-6.2625));
#368870=CARTESIAN_POINT('Ctrl Pts',(-1.01778810567665,-0.587620236790411,
-6.22083333333333));
#368871=CARTESIAN_POINT('Ctrl Pts',(-0.678525403784435,-1.17524047358083,
-6.17916666666667));
#368872=CARTESIAN_POINT('Ctrl Pts',(-1.43925448419918E-16,-1.17524047358083,
-6.1375));
#368873=CARTESIAN_POINT('Ctrl Pts',(0.678525403784435,-1.17524047358083,
-6.09583333333333));
#368874=CARTESIAN_POINT('Ctrl Pts',(1.01778810567665,-0.587620236790412,
-6.05416666666667));
#368875=CARTESIAN_POINT('Ctrl Pts',(1.35705080756887,3.03927878972919E-15,
-6.0125));
#368876=CARTESIAN_POINT('Ctrl Pts',(1.01778810567665,0.587620236790417,
-5.97083333333333));
#368877=CARTESIAN_POINT('Ctrl Pts',(0.678525403784436,1.17524047358083,
-5.92916666666667));
#368878=CARTESIAN_POINT('Ctrl Pts',(0.,1.17524047358083,-5.8875));
#368879=CARTESIAN_POINT('Ctrl Pts',(-0.678525403784435,1.17524047358083,
-5.84583333333333));
#368880=CARTESIAN_POINT('Ctrl Pts',(-1.01778810567665,0.587620236790418,
-5.80416666666667));
#368881=CARTESIAN_POINT('Ctrl Pts',(-1.35705080756887,3.26238645553653E-15,
-5.7625));
#368882=CARTESIAN_POINT('Ctrl Pts',(-1.01778810567665,-0.587620236790411,
-5.72083333333333));
#368883=CARTESIAN_POINT('Ctrl Pts',(-0.678525403784435,-1.17524047358083,
-5.67916666666667));
#368884=CARTESIAN_POINT('Ctrl Pts',(-1.43925448419918E-16,-1.17524047358083,
-5.6375));
#368885=CARTESIAN_POINT('Ctrl Pts',(0.678525403784435,-1.17524047358083,
-5.59583333333333));
#368886=CARTESIAN_POINT('Ctrl Pts',(1.01778810567665,-0.587620236790412,
-5.55416666666667));
#368887=CARTESIAN_POINT('Ctrl Pts',(1.35705080756887,2.82073095023605E-15,
-5.5125));
#368888=CARTESIAN_POINT('Ctrl Pts',(1.01778810567665,0.587620236790417,
-5.47083333333333));
#368889=CARTESIAN_POINT('Ctrl Pts',(0.678525403784436,1.17524047358083,
-5.42916666666667));
#368890=CARTESIAN_POINT('Ctrl Pts',(0.,1.17524047358083,-5.3875));
#368891=CARTESIAN_POINT('Ctrl Pts',(-0.678525403784435,1.17524047358083,
-5.34583333333333));
#368892=CARTESIAN_POINT('Ctrl Pts',(-1.01778810567665,0.587620236790418,
-5.30416666666667));
#368893=CARTESIAN_POINT('Ctrl Pts',(-1.35705080756887,3.04383861604338E-15,
-5.2625));
#368894=CARTESIAN_POINT('Ctrl Pts',(-1.01778810567665,-0.587620236790411,
-5.22083333333333));
#368895=CARTESIAN_POINT('Ctrl Pts',(-0.678525403784435,-1.17524047358083,
-5.17916666666667));
#368896=CARTESIAN_POINT('Ctrl Pts',(-1.43925448419918E-16,-1.17524047358083,
-5.1375));
#368897=CARTESIAN_POINT('Ctrl Pts',(0.678525403784435,-1.17524047358083,
-5.09583333333333));
#368898=CARTESIAN_POINT('Ctrl Pts',(1.01778810567665,-0.587620236790412,
-5.05416666666667));
#368899=CARTESIAN_POINT('Ctrl Pts',(1.35705080756887,2.6021831107429E-15,
-5.0125));
#368900=CARTESIAN_POINT('Ctrl Pts',(1.01778810567665,0.587620236790417,
-4.97083333333333));
#368901=CARTESIAN_POINT('Ctrl Pts',(0.678525403784436,1.17524047358083,
-4.92916666666667));
#368902=CARTESIAN_POINT('Ctrl Pts',(0.,1.17524047358083,-4.8875));
#368903=CARTESIAN_POINT('Ctrl Pts',(-0.678525403784435,1.17524047358083,
-4.84583333333333));
#368904=CARTESIAN_POINT('Ctrl Pts',(-1.01778810567665,0.587620236790418,
-4.80416666666667));
#368905=CARTESIAN_POINT('Ctrl Pts',(-1.35705080756887,2.82529077655024E-15,
-4.7625));
#368906=CARTESIAN_POINT('Ctrl Pts',(-1.01778810567665,-0.587620236790412,
-4.72083333333333));
#368907=CARTESIAN_POINT('Ctrl Pts',(-0.678525403784435,-1.17524047358083,
-4.67916666666667));
#368908=CARTESIAN_POINT('Ctrl Pts',(-1.43925448419918E-16,-1.17524047358083,
-4.6375));
#368909=CARTESIAN_POINT('Ctrl Pts',(0.678525403784435,-1.17524047358083,
-4.59583333333333));
#368910=CARTESIAN_POINT('Ctrl Pts',(1.01778810567665,-0.587620236790413,
-4.55416666666667));
#368911=CARTESIAN_POINT('Ctrl Pts',(1.35705080756887,2.38363527124976E-15,
-4.5125));
#368912=CARTESIAN_POINT('Ctrl Pts',(1.01778810567665,0.587620236790416,
-4.47083333333333));
#368913=CARTESIAN_POINT('Ctrl Pts',(0.678525403784436,1.17524047358083,
-4.42916666666667));
#368914=CARTESIAN_POINT('Ctrl Pts',(0.,1.17524047358083,-4.3875));
#368915=CARTESIAN_POINT('Ctrl Pts',(-0.678525403784435,1.17524047358083,
-4.34583333333333));
#368916=CARTESIAN_POINT('Ctrl Pts',(-1.01778810567665,0.587620236790417,
-4.30416666666667));
#368917=CARTESIAN_POINT('Ctrl Pts',(-1.35705080756887,2.6067429370571E-15,
-4.2625));
#368918=CARTESIAN_POINT('Ctrl Pts',(-1.01778810567665,-0.587620236790412,
-4.22083333333333));
#368919=CARTESIAN_POINT('Ctrl Pts',(-0.678525403784435,-1.17524047358083,
-4.17916666666667));
#368920=CARTESIAN_POINT('Ctrl Pts',(-1.43925448419918E-16,-1.17524047358083,
-4.1375));
#368921=CARTESIAN_POINT('Ctrl Pts',(0.678525403784435,-1.17524047358083,
-4.09583333333333));
#368922=CARTESIAN_POINT('Ctrl Pts',(1.01778810567665,-0.587620236790413,
-4.05416666666667));
#368923=CARTESIAN_POINT('Ctrl Pts',(1.35705080756887,2.16508743175662E-15,
-4.0125));
#368924=CARTESIAN_POINT('Ctrl Pts',(1.01778810567665,0.587620236790416,
-3.97083333333333));
#368925=CARTESIAN_POINT('Ctrl Pts',(0.678525403784436,1.17524047358083,
-3.92916666666667));
#368926=CARTESIAN_POINT('Ctrl Pts',(0.,1.17524047358083,-3.8875));
#368927=CARTESIAN_POINT('Ctrl Pts',(-0.678525403784435,1.17524047358083,
-3.84583333333333));
#368928=CARTESIAN_POINT('Ctrl Pts',(-1.01778810567665,0.587620236790417,
-3.80416666666667));
#368929=CARTESIAN_POINT('Ctrl Pts',(-1.35705080756887,2.38819509756396E-15,
-3.7625));
#368930=CARTESIAN_POINT('Ctrl Pts',(-1.01778810567665,-0.587620236790412,
-3.72083333333333));
#368931=CARTESIAN_POINT('Ctrl Pts',(-0.678525403784435,-1.17524047358083,
-3.67916666666667));
#368932=CARTESIAN_POINT('Ctrl Pts',(-1.43925448419918E-16,-1.17524047358083,
-3.6375));
#368933=CARTESIAN_POINT('Ctrl Pts',(0.678525403784435,-1.17524047358083,
-3.59583333333333));
#368934=CARTESIAN_POINT('Ctrl Pts',(1.01778810567665,-0.587620236790413,
-3.55416666666667));
#368935=CARTESIAN_POINT('Ctrl Pts',(1.35705080756887,1.94653959226348E-15,
-3.5125));
#368936=CARTESIAN_POINT('Ctrl Pts',(1.01778810567665,0.587620236790416,
-3.47083333333333));
#368937=CARTESIAN_POINT('Ctrl Pts',(0.678525403784436,1.17524047358083,
-3.42916666666667));
#368938=CARTESIAN_POINT('Ctrl Pts',(0.,1.17524047358083,-3.3875));
#368939=CARTESIAN_POINT('Ctrl Pts',(-0.678525403784435,1.17524047358083,
-3.34583333333333));
#368940=CARTESIAN_POINT('Ctrl Pts',(-1.01778810567665,0.587620236790417,
-3.30416666666667));
#368941=CARTESIAN_POINT('Ctrl Pts',(-1.35705080756887,2.16964725807082E-15,
-3.2625));
#368942=CARTESIAN_POINT('Ctrl Pts',(-1.01778810567665,-0.587620236790412,
-3.22083333333333));
#368943=CARTESIAN_POINT('Ctrl Pts',(-0.678525403784435,-1.17524047358083,
-3.17916666666667));
#368944=CARTESIAN_POINT('Ctrl Pts',(-1.43925448419918E-16,-1.17524047358083,
-3.1375));
#368945=CARTESIAN_POINT('Ctrl Pts',(0.678525403784435,-1.17524047358083,
-3.09583333333333));
#368946=CARTESIAN_POINT('Ctrl Pts',(1.01778810567665,-0.587620236790413,
-3.05416666666667));
#368947=CARTESIAN_POINT('Ctrl Pts',(1.35705080756887,1.72799175277034E-15,
-3.0125));
#368948=CARTESIAN_POINT('Ctrl Pts',(1.01778810567665,0.587620236790416,
-2.97083333333333));
#368949=CARTESIAN_POINT('Ctrl Pts',(0.678525403784436,1.17524047358083,
-2.92916666666667));
#368950=CARTESIAN_POINT('Ctrl Pts',(0.,1.17524047358083,-2.8875));
#368951=CARTESIAN_POINT('Ctrl Pts',(-0.678525403784435,1.17524047358083,
-2.84583333333333));
#368952=CARTESIAN_POINT('Ctrl Pts',(-1.01778810567665,0.587620236790417,
-2.80416666666667));
#368953=CARTESIAN_POINT('Ctrl Pts',(-1.35705080756887,1.95109941857768E-15,
-2.7625));
#368954=CARTESIAN_POINT('Ctrl Pts',(-1.01778810567665,-0.587620236790413,
-2.72083333333333));
#368955=CARTESIAN_POINT('Ctrl Pts',(-0.678525403784435,-1.17524047358083,
-2.67916666666667));
#368956=CARTESIAN_POINT('Ctrl Pts',(-1.43925448419918E-16,-1.17524047358083,
-2.6375));
#368957=CARTESIAN_POINT('Ctrl Pts',(0.678525403784435,-1.17524047358083,
-2.59583333333333));
#368958=CARTESIAN_POINT('Ctrl Pts',(1.01778810567665,-0.587620236790414,
-2.55416666666667));
#368959=CARTESIAN_POINT('Ctrl Pts',(1.35705080756887,1.5094439132772E-15,
-2.5125));
#368960=CARTESIAN_POINT('Ctrl Pts',(1.01778810567665,0.587620236790415,
-2.47083333333333));
#368961=CARTESIAN_POINT('Ctrl Pts',(0.678525403784436,1.17524047358083,
-2.42916666666667));
#368962=CARTESIAN_POINT('Ctrl Pts',(0.,1.17524047358083,-2.3875));
#368963=CARTESIAN_POINT('Ctrl Pts',(-0.678525403784435,1.17524047358083,
-2.34583333333333));
#368964=CARTESIAN_POINT('Ctrl Pts',(-1.01778810567665,0.587620236790416,
-2.30416666666667));
#368965=CARTESIAN_POINT('Ctrl Pts',(-1.35705080756887,1.73255157908454E-15,
-2.2625));
#368966=CARTESIAN_POINT('Ctrl Pts',(-1.01778810567665,-0.587620236790413,
-2.22083333333333));
#368967=CARTESIAN_POINT('Ctrl Pts',(-0.678525403784435,-1.17524047358083,
-2.17916666666667));
#368968=CARTESIAN_POINT('Ctrl Pts',(-1.43925448419918E-16,-1.17524047358083,
-2.1375));
#368969=CARTESIAN_POINT('Ctrl Pts',(0.678525403784435,-1.17524047358083,
-2.09583333333333));
#368970=CARTESIAN_POINT('Ctrl Pts',(1.01778810567665,-0.587620236790414,
-2.05416666666667));
#368971=CARTESIAN_POINT('Ctrl Pts',(1.35705080756887,1.29089607378406E-15,
-2.0125));
#368972=CARTESIAN_POINT('Ctrl Pts',(1.01778810567665,0.587620236790415,
-1.97083333333333));
#368973=CARTESIAN_POINT('Ctrl Pts',(0.678525403784436,1.17524047358083,
-1.92916666666667));
#368974=CARTESIAN_POINT('Ctrl Pts',(0.,1.17524047358083,-1.8875));
#368975=CARTESIAN_POINT('Ctrl Pts',(-0.678525403784435,1.17524047358083,
-1.84583333333334));
#368976=CARTESIAN_POINT('Ctrl Pts',(-1.01778810567665,0.587620236790416,
-1.80416666666667));
#368977=CARTESIAN_POINT('Ctrl Pts',(-1.35705080756887,1.5140037395914E-15,
-1.7625));
#368978=CARTESIAN_POINT('Ctrl Pts',(-1.01778810567665,-0.587620236790413,
-1.72083333333333));
#368979=CARTESIAN_POINT('Ctrl Pts',(-0.678525403784435,-1.17524047358083,
-1.67916666666667));
#368980=CARTESIAN_POINT('Ctrl Pts',(-1.43925448419918E-16,-1.17524047358083,
-1.6375));
#368981=CARTESIAN_POINT('Ctrl Pts',(0.678525403784435,-1.17524047358083,
-1.59583333333333));
#368982=CARTESIAN_POINT('Ctrl Pts',(1.01778810567665,-0.587620236790414,
-1.55416666666667));
#368983=CARTESIAN_POINT('Ctrl Pts',(1.35705080756887,1.07234823429092E-15,
-1.5125));
#368984=CARTESIAN_POINT('Ctrl Pts',(1.01778810567665,0.587620236790415,
-1.47083333333333));
#368985=CARTESIAN_POINT('Ctrl Pts',(0.678525403784436,1.17524047358083,
-1.42916666666667));
#368986=CARTESIAN_POINT('Ctrl Pts',(0.,1.17524047358083,-1.3875));
#459206=UNCERTAINTY_MEASURE_WITH_UNIT(LENGTH_MEASURE(0.01),#459243,
'DISTANCE_ACCURACY_VALUE',
'Maximum model space distance between geometric entities at asserted c
onnectivities');
#459216=UNCERTAINTY_MEASURE_WITH_UNIT(LENGTH_MEASURE(0.01),#459243,
'DISTANCE_ACCURACY_VALUE',
'Maximum model space distance between geometric entities at asserted c
onnectivities');
#459232=(
GEOMETRIC_REPRESENTATION_CONTEXT(3)
GLOBAL_UNCERTAINTY_ASSIGNED_CONTEXT((#459206))
GLOBAL_UNIT_ASSIGNED_CONTEXT((#459243,#459245,#459246))
REPRESENTATION_CONTEXT('','3D')
);
#459242=(
GEOMETRIC_REPRESENTATION_CONTEXT(3)
GLOBAL_UNCERTAINTY_ASSIGNED_CONTEXT((#459216))
GLOBAL_UNIT_ASSIGNED_CONTEXT((#459243,#459245,#459246))
REPRESENTATION_CONTEXT('','3D')
);
#459243=(
LENGTH_UNIT()
NAMED_UNIT(*)
SI_UNIT(.MILLI.,.METRE.)
);
#459245=(
NAMED_UNIT(*)
PLANE_ANGLE_UNIT()
SI_UNIT($,.RADIAN.)
);
#459246=(
NAMED_UNIT(*)
SI_UNIT($,.STERADIAN.)
SOLID_ANGLE_UNIT()
);
#459262=SHAPE_DEFINITION_REPRESENTATION(#459289,#459343);
#459289=PRODUCT_DEFINITION_SHAPE('',$,#459369);
#459343=SHAPE_REPRESENTATION('',(#99248),#459232);
#459353=PRODUCT_DEFINITION_CONTEXT('part definition',#459430,'design');
#459369=PRODUCT_DEFINITION('Assembly Screw 1','Assembly Screw 1',#459394,
#459353);
#459394=PRODUCT_DEFINITION_FORMATION('',$,#459447);
#459430=APPLICATION_CONTEXT(
'Core Data for Automotive Mechanical Design Process');
#459431=PRODUCT_CONTEXT('part definition',#459430,'mechanical');
#459447=PRODUCT('Assembly Screw 1','Assembly Screw 1',$,(#459431));
#459527=COLOUR_RGB('Black',0.12,0.14,0.17);
#459528=FILL_AREA_STYLE_COLOUR('',#459527);
#459529=FILL_AREA_STYLE('',(#459528));
#459530=SURFACE_STYLE_FILL_AREA(#459529);
#459531=SURFACE_SIDE_STYLE('',(#459530));
#459532=SURFACE_STYLE_USAGE(.BOTH.,#459531);
#459533=PRESENTATION_STYLE_ASSIGNMENT((#459532));
ENDSEC;
END-ISO-10303-21;
